ISO-10303-21;
HEADER;
FILE_DESCRIPTION (('STEP AP214'),
    '1' );
FILE_NAME ('5537T808_T-Slotted Framing_5537T808.step',
    '2026-10-09T16:01:55',
    ( '' ),
    ( '' ),
    'SwSTEP 2.0',
    'SolidWorks 2024',
    '' );
FILE_SCHEMA (( 'AUTOMOTIVE_DESIGN' ));
ENDSEC;

DATA;
#1=DIRECTION ( 'NONE',  ( 1.836970198721029934E-16, 1.836970198721010706E-16, -1.000000000000000000 ) ) ;
#7=DIRECTION ( 'NONE',  ( 0.7071067811865422437, -0.7071067811865527908, 0.000000000000000000 ) ) ;
#8=LINE ( 'NONE', #43125, #47900 ) ;
#16=FACE_OUTER_BOUND ( 'NONE', #57290, .T. ) ;
#24=VECTOR ( 'NONE', #20692, 1000.000000000000000 ) ;
#34=ORIENTED_EDGE ( 'NONE', *, *, #62391, .F. ) ;
#37=FACE_OUTER_BOUND ( 'NONE', #4535, .T. ) ;
#41=ORIENTED_EDGE ( 'NONE', *, *, #17643, .F. ) ;
#42=EDGE_CURVE ( 'NONE', #51075, #15946, #66798, .T. ) ;
#54=ORIENTED_EDGE ( 'NONE', *, *, #29068, .T. ) ;
#60=VECTOR ( 'NONE', #58581, 1000.000000000000000 ) ;
#61=ORIENTED_EDGE ( 'NONE', *, *, #49040, .T. ) ;
#63=CARTESIAN_POINT ( 'NONE',  ( -7.605476262117258024, 9.722976262117178692, 54.00000000000000711 ) ) ;
#67=DIRECTION ( 'NONE',  ( 2.478176394252584099E-15, 1.000000000000000000, 0.000000000000000000 ) ) ;
#68=( LENGTH_UNIT ( ) NAMED_UNIT ( * ) SI_UNIT ( .MILLI., .METRE. ) );
#74=ORIENTED_EDGE ( 'NONE', *, *, #13941, .F. ) ;
#77=AXIS2_PLACEMENT_3D ( 'NONE', #40976, #13759, #8096 ) ;
#83=ORIENTED_EDGE ( 'NONE', *, *, #7597, .F. ) ;
#86=VERTEX_POINT ( 'NONE', #37468 ) ;
#87=DIRECTION ( 'NONE',  ( 0.000000000000000000, -3.673940397442059868E-16, 1.000000000000000000 ) ) ;
#96=VERTEX_POINT ( 'NONE', #36776 ) ;
#97=VERTEX_POINT ( 'NONE', #64001 ) ;
#104=EDGE_LOOP ( 'NONE', ( #32156, #26137, #19889, #8846 ) ) ;
#113=EDGE_CURVE ( 'NONE', #43177, #7725, #15895, .T. ) ;
#114=VERTEX_POINT ( 'NONE', #53041 ) ;
#133=CARTESIAN_POINT ( 'NONE',  ( 1.480523737882788238, -9.404523737882794165, 54.00000000000000711 ) ) ;
#142=DIRECTION ( 'NONE',  ( 1.836970198721029934E-16, 1.836970198721010706E-16, -1.000000000000000000 ) ) ;
#150=EDGE_LOOP ( 'NONE', ( #65077, #13580, #38197, #52160, #31394, #37304, #41041, #48083 ) ) ;
#155=ORIENTED_EDGE ( 'NONE', *, *, #10566, .T. ) ;
#165=LINE ( 'NONE', #32674, #35413 ) ;
#167=VERTEX_POINT ( 'NONE', #1968 ) ;
#177=PLANE ( 'NONE',  #17503 ) ;
#192=ORIENTED_EDGE ( 'NONE', *, *, #64535, .T. ) ;
#207=AXIS2_PLACEMENT_3D ( 'NONE', #51978, #16234, #48423 ) ;
#208=DIRECTION ( 'NONE',  ( -1.000000000000000000, 3.491481338843133355E-15, 1.836970198721036344E-16 ) ) ;
#211=AXIS2_PLACEMENT_3D ( 'NONE', #34304, #7442, #6750 ) ;
#221=LINE ( 'NONE', #21784, #62152 ) ;
#222=DIRECTION ( 'NONE',  ( -0.000000000000000000, -0.000000000000000000, -1.000000000000000000 ) ) ;
#227=EDGE_CURVE ( 'NONE', #15964, #12532, #53311, .T. ) ;
#229=EDGE_CURVE ( 'NONE', #49648, #8082, #14853, .T. ) ;
#252=ORIENTED_EDGE ( 'NONE', *, *, #3134, .T. ) ;
#254=CARTESIAN_POINT ( 'NONE',  ( -6.775514141871385121, 7.394232575409538377, 26.00000000000000711 ) ) ;
#255=ORIENTED_EDGE ( 'NONE', *, *, #43723, .F. ) ;
#256=CIRCLE ( 'NONE', #3484, 0.3499999999999996447 ) ;
#257=DIRECTION ( 'NONE',  ( -1.836970198721029934E-16, 1.836970198721036590E-16, -1.000000000000000000 ) ) ;
#264=CARTESIAN_POINT ( 'NONE',  ( 8.711985858128686644, 8.079219948824833963, 54.00000000000000711 ) ) ;
#266=ORIENTED_EDGE ( 'NONE', *, *, #48155, .T. ) ;
#268=VERTEX_POINT ( 'NONE', #57103 ) ;
#271=EDGE_LOOP ( 'NONE', ( #35321, #22155, #8372, #56356 ) ) ;
#287=VECTOR ( 'NONE', #16206, 1000.000000000000000 ) ;
#291=CARTESIAN_POINT ( 'NONE',  ( -9.722976262117237312, 7.605476262117214503, 54.00000000000000711 ) ) ;
#294=ORIENTED_EDGE ( 'NONE', *, *, #44456, .F. ) ;
#297=CARTESIAN_POINT ( 'NONE',  ( -6.651770455163783957, -7.532023737882790115, 54.00000000000000711 ) ) ;
#300=LINE ( 'NONE', #16908, #68047 ) ;
#303=CARTESIAN_POINT ( 'NONE',  ( 0.9555237378828163042, 9.390476262117214645, 54.00000000000000711 ) ) ;
#316=CARTESIAN_POINT ( 'NONE',  ( 5.257023737882819070, -4.032023737882826531, 54.00000000000000711 ) ) ;
#319=PLANE ( 'NONE',  #6241 ) ;
#324=VECTOR ( 'NONE', #38964, 1000.000000000000000 ) ;
#330=VERTEX_POINT ( 'NONE', #52509 ) ;
#336=ORIENTED_EDGE ( 'NONE', *, *, #64829, .F. ) ;
#347=AXIS2_PLACEMENT_3D ( 'NONE', #37839, #1052, #32875 ) ;
#348=DIRECTION ( 'NONE',  ( -0.000000000000000000, 3.673940397442059868E-16, -1.000000000000000000 ) ) ;
#355=VERTEX_POINT ( 'NONE', #24929 ) ;
#360=ORIENTED_EDGE ( 'NONE', *, *, #15360, .T. ) ;
#363=VECTOR ( 'NONE', #30317, 1000.000000000000000 ) ;
#364=CARTESIAN_POINT ( 'NONE',  ( 3.682023737882785586, -9.912023737882801555, 26.00000000000000000 ) ) ;
#368=CARTESIAN_POINT ( 'NONE',  ( 8.612468434717177601, 1.466476262117168972, 26.00000000000000711 ) ) ;
#374=EDGE_CURVE ( 'NONE', #1632, #1811, #9368, .T. ) ;
#383=CARTESIAN_POINT ( 'NONE',  ( -4.141586236041100655, 5.779227145995200488, 26.00000000000000711 ) ) ;
#390=CIRCLE ( 'NONE', #36469, 1.224999999999998757 ) ;
#398=FACE_OUTER_BOUND ( 'NONE', #65165, .T. ) ;
#405=DIRECTION ( 'NONE',  ( -0.000000000000000000, -0.000000000000000000, -1.000000000000000000 ) ) ;
#412=ORIENTED_EDGE ( 'NONE', *, *, #18461, .T. ) ;
#418=VECTOR ( 'NONE', #29526, 1000.000000000000000 ) ;
#429=ORIENTED_EDGE ( 'NONE', *, *, #55499, .F. ) ;
#430=ORIENTED_EDGE ( 'NONE', *, *, #65625, .F. ) ;
#436=DIRECTION ( 'NONE',  ( 1.000000000000000000, 0.000000000000000000, 0.000000000000000000 ) ) ;
#440=CARTESIAN_POINT ( 'NONE',  ( 9.404523737882817258, -1.480523737882825985, 54.00000000000000711 ) ) ;
#442=EDGE_LOOP ( 'NONE', ( #22286, #68727, #54112, #64195 ) ) ;
#451=ORIENTED_EDGE ( 'NONE', *, *, #36674, .F. ) ;
#479=LINE ( 'NONE', #69082, #25901 ) ;
#482=FACE_OUTER_BOUND ( 'NONE', #63046, .T. ) ;
#503=LINE ( 'NONE', #22069, #24410 ) ;
#515=CARTESIAN_POINT ( 'NONE',  ( -9.689726262117227762, 9.689726262117183353, 54.00000000000000711 ) ) ;
#516=ORIENTED_EDGE ( 'NONE', *, *, #65064, .F. ) ;
#521=EDGE_LOOP ( 'NONE', ( #59602, #68123, #42949, #33400 ) ) ;
#523=VERTEX_POINT ( 'NONE', #48252 ) ;
#525=DIRECTION ( 'NONE',  ( 0.000000000000000000, -3.673940397442059868E-16, 1.000000000000000000 ) ) ;
#526=ORIENTED_EDGE ( 'NONE', *, *, #44380, .T. ) ;
#529=VECTOR ( 'NONE', #27230, 1000.000000000000000 ) ;
#531=ORIENTED_EDGE ( 'NONE', *, *, #58938, .T. ) ;
#535=LINE ( 'NONE', #21059, #41754 ) ;
#539=ORIENTED_EDGE ( 'NONE', *, *, #11824, .T. ) ;
#540=CARTESIAN_POINT ( 'NONE',  ( -7.342976262117259623, 4.947141984184421304, 26.00000000000000711 ) ) ;
#542=CARTESIAN_POINT ( 'NONE',  ( -7.394232575409614761, 3.710438382363058896, 26.00000000000000711 ) ) ;
#545=EDGE_CURVE ( 'NONE', #32184, #13431, #27723, .T. ) ;
#548=CARTESIAN_POINT ( 'NONE',  ( 3.724485858128685045, 7.394232575409559693, 54.00000000000000711 ) ) ;
#550=DIRECTION ( 'NONE',  ( -1.261617073437657735E-14, -1.000000000000000000, 0.000000000000000000 ) ) ;
#552=VECTOR ( 'NONE', #39215, 1000.000000000000000 ) ;
#561=DIRECTION ( 'NONE',  ( -1.000000000000000000, 0.000000000000000000, 0.000000000000000000 ) ) ;
#568=EDGE_CURVE ( 'NONE', #4457, #43741, #22425, .T. ) ;
#569=AXIS2_PLACEMENT_3D ( 'NONE', #12617, #13330, #56464 ) ;
#570=EDGE_LOOP ( 'NONE', ( #1915, #32078, #8129, #192 ) ) ;
#572=DIRECTION ( 'NONE',  ( -4.956352788505168198E-15, -1.000000000000000000, 0.000000000000000000 ) ) ;
#574=LINE ( 'NONE', #22144, #58360 ) ;
#577=DIRECTION ( 'NONE',  ( -2.439149994343049068E-15, -1.000000000000000000, 0.000000000000000000 ) ) ;
#579=ADVANCED_FACE ( 'NONE', ( #13181 ), #1883, .F. ) ;
#582=LINE ( 'NONE', #16497, #34375 ) ;
#583=CARTESIAN_POINT ( 'NONE',  ( -7.517976262117294084, -6.665817930929260449, 54.00000000000000711 ) ) ;
#589=ORIENTED_EDGE ( 'NONE', *, *, #57565, .F. ) ;
#597=CIRCLE ( 'NONE', #14164, 1.224999999999998757 ) ;
#603=FACE_OUTER_BOUND ( 'NONE', #10615, .T. ) ;
#608=AXIS2_PLACEMENT_3D ( 'NONE', #9316, #63413, #57045 ) ;
#614=VECTOR ( 'NONE', #18317, 1000.000000000000000 ) ;
#616=ORIENTED_EDGE ( 'NONE', *, *, #25208, .T. ) ;
#617=ORIENTED_EDGE ( 'NONE', *, *, #68183, .T. ) ;
#627=ORIENTED_EDGE ( 'NONE', *, *, #34864, .F. ) ;
#629=ADVANCED_FACE ( 'NONE', ( #34381 ), #67286, .F. ) ;
#638=PLANE ( 'NONE',  #53910 ) ;
#639=LINE ( 'NONE', #27506, #3790 ) ;
#641=ORIENTED_EDGE ( 'NONE', *, *, #13313, .T. ) ;
#648=ORIENTED_EDGE ( 'NONE', *, *, #3440, .F. ) ;
#649=CARTESIAN_POINT ( 'NONE',  ( -10.49297626211726175, 3.650476262117184234, 54.00000000000000711 ) ) ;
#653=EDGE_LOOP ( 'NONE', ( #42784, #54327, #4173, #68157 ) ) ;
#656=VECTOR ( 'NONE', #33989, 1000.000000000000000 ) ;
#658=DIRECTION ( 'NONE',  ( 0.7671651518152939886, -0.6414496315691644579, -2.587583378555133721E-16 ) ) ;
#659=CARTESIAN_POINT ( 'NONE',  ( 10.31452373788281562, -6.849523737882823760, 54.00000000000000711 ) ) ;
#661=CIRCLE ( 'NONE', #35613, 0.1749999999999993783 ) ;
#665=CARTESIAN_POINT ( 'NONE',  ( -8.697938382363103571, -2.420780051175099423, 54.00000000000000711 ) ) ;
#688=FACE_OUTER_BOUND ( 'NONE', #35087, .T. ) ;
#689=ORIENTED_EDGE ( 'NONE', *, *, #63377, .F. ) ;
#696=EDGE_LOOP ( 'NONE', ( #30041, #28566, #64326, #7292 ) ) ;
#697=CARTESIAN_POINT ( 'NONE',  ( 1.634292677759874302, 8.227189898828697778, 54.00000000000000711 ) ) ;
#698=LINE ( 'NONE', #23621, #5377 ) ;
#708=ORIENTED_EDGE ( 'NONE', *, *, #57409, .F. ) ;
#730=ORIENTED_EDGE ( 'NONE', *, *, #44793, .F. ) ;
#739=EDGE_CURVE ( 'NONE', #268, #19808, #12478, .T. ) ;
#746=ORIENTED_EDGE ( 'NONE', *, *, #15039, .F. ) ;
#751=ORIENTED_EDGE ( 'NONE', *, *, #28929, .T. ) ;
#756=ORIENTED_EDGE ( 'NONE', *, *, #15619, .T. ) ;
#766=CARTESIAN_POINT ( 'NONE',  ( 7.357023737882797398, 5.538810540049960984, 26.00000000000000711 ) ) ;
#773=FACE_OUTER_BOUND ( 'NONE', #49623, .T. ) ;
#776=ORIENTED_EDGE ( 'NONE', *, *, #46433, .T. ) ;
#779=CARTESIAN_POINT ( 'NONE',  ( 4.149127210878726046, 6.822336235477391320, 54.00000000000000711 ) ) ;
#781=ADVANCED_FACE ( 'NONE', ( #68330 ), #9995, .F. ) ;
#783=FACE_OUTER_BOUND ( 'NONE', #23681, .T. ) ;
#786=EDGE_CURVE ( 'NONE', #9283, #69426, #58073, .T. ) ;
#790=EDGE_CURVE ( 'NONE', #45723, #45427, #9640, .T. ) ;
#793=CYLINDRICAL_SURFACE ( 'NONE', #25893, 1.929199999999997139 ) ;
#802=ORIENTED_EDGE ( 'NONE', *, *, #11052, .F. ) ;
#807=DIRECTION ( 'NONE',  ( 3.540251991789405856E-15, 1.000000000000000000, 0.000000000000000000 ) ) ;
#810=AXIS2_PLACEMENT_3D ( 'NONE', #56558, #8104, #44904 ) ;
#811=ORIENTED_EDGE ( 'NONE', *, *, #65786, .F. ) ;
#817=CIRCLE ( 'NONE', #40302, 0.1749999999999998224 ) ;
#827=EDGE_CURVE ( 'NONE', #44516, #18842, #55470, .T. ) ;
#829=VERTEX_POINT ( 'NONE', #69030 ) ;
#834=VECTOR ( 'NONE', #69668, 1000.000000000000000 ) ;
#840=EDGE_LOOP ( 'NONE', ( #34414, #10179, #35438, #60528 ) ) ;
#853=ORIENTED_EDGE ( 'NONE', *, *, #17034, .T. ) ;
#858=CARTESIAN_POINT ( 'NONE',  ( 6.358413763958946419, 4.706725378239151603, 54.00000000000000711 ) ) ;
#860=ORIENTED_EDGE ( 'NONE', *, *, #23793, .F. ) ;
#864=AXIS2_PLACEMENT_3D ( 'NONE', #67353, #65696, #3001 ) ;
#867=CARTESIAN_POINT ( 'NONE',  ( -7.955476262117259445, 9.547976262117179758, 26.00000000000000711 ) ) ;
#875=EDGE_CURVE ( 'NONE', #38341, #57811, #5399, .T. ) ;
#880=CIRCLE ( 'NONE', #44900, 1.929199999999998028 ) ;
#885=FACE_OUTER_BOUND ( 'NONE', #64182, .T. ) ;
#890=DIRECTION ( 'NONE',  ( -0.000000000000000000, 3.673940397442059868E-16, -1.000000000000000000 ) ) ;
#900=ORIENTED_EDGE ( 'NONE', *, *, #47319, .T. ) ;
#902=VERTEX_POINT ( 'NONE', #65471 ) ;
#907=DIRECTION ( 'NONE',  ( -0.000000000000000000, 3.673940397442059868E-16, -1.000000000000000000 ) ) ;
#917=CARTESIAN_POINT ( 'NONE',  ( -10.30047626211725742, 3.842976262117182351, 54.00000000000000711 ) ) ;
#918=CARTESIAN_POINT ( 'NONE',  ( 6.665817930929288870, 7.342976262117195674, 54.00000000000000711 ) ) ;
#920=ORIENTED_EDGE ( 'NONE', *, *, #10649, .T. ) ;
#922=AXIS2_PLACEMENT_3D ( 'NONE', #63291, #58689, #9198 ) ;
#929=DIRECTION ( 'NONE',  ( -0.000000000000000000, 3.673940397442059868E-16, -1.000000000000000000 ) ) ;
#930=DIRECTION ( 'NONE',  ( 9.912705577010344285E-15, 1.000000000000000000, 0.000000000000000000 ) ) ;
#931=EDGE_CURVE ( 'NONE', #9404, #31249, #5735, .T. ) ;
#932=CARTESIAN_POINT ( 'NONE',  ( 5.257023737882801306, 5.242976262117200470, 54.00000000000000711 ) ) ;
#933=DIRECTION ( 'NONE',  ( -1.836970198721029934E-16, 1.836970198721036344E-16, -1.000000000000000000 ) ) ;
#935=DIRECTION ( 'NONE',  ( -1.000000000000000000, 0.000000000000000000, 0.000000000000000000 ) ) ;
#936=LINE ( 'NONE', #5876, #27757 ) ;
#941=CARTESIAN_POINT ( 'NONE',  ( 9.737023737882783081, 3.667976262117152775, 54.00000000000000711 ) ) ;
#945=FACE_OUTER_BOUND ( 'NONE', #29269, .T. ) ;
#957=DIRECTION ( 'NONE',  ( 1.047444401652940007E-14, 1.000000000000000000, 1.836970198721029934E-16 ) ) ;
#958=ORIENTED_EDGE ( 'NONE', *, *, #875, .F. ) ;
#959=LINE ( 'NONE', #22850, #22115 ) ;
#960=ORIENTED_EDGE ( 'NONE', *, *, #2716, .F. ) ;
#961=VERTEX_POINT ( 'NONE', #49550 ) ;
#962=PLANE ( 'NONE',  #48707 ) ;
#964=DIRECTION ( 'NONE',  ( -7.665540703601096574E-15, -1.000000000000000000, -3.673940397442059868E-16 ) ) ;
#965=VECTOR ( 'NONE', #30411, 1000.000000000000000 ) ;
#971=VECTOR ( 'NONE', #50877, 1000.000000000000000 ) ;
#989=CARTESIAN_POINT ( 'NONE',  ( 8.835729544836338434, -8.144523737882822800, 54.00000000000000711 ) ) ;
#990=EDGE_CURVE ( 'NONE', #32081, #28477, #18203, .T. ) ;
#993=EDGE_CURVE ( 'NONE', #54687, #42154, #12053, .T. ) ;
#998=ORIENTED_EDGE ( 'NONE', *, *, #30275, .F. ) ;
#1011=LINE ( 'NONE', #46125, #12079 ) ;
#1014=AXIS2_PLACEMENT_3D ( 'NONE', #63250, #5857, #48299 ) ;
#1015=DIRECTION ( 'NONE',  ( -1.000000000000000000, 0.000000000000000000, 0.000000000000000000 ) ) ;
#1019=ORIENTED_EDGE ( 'NONE', *, *, #9468, .F. ) ;
#1023=LINE ( 'NONE', #53727, #59201 ) ;
#1027=FACE_OUTER_BOUND ( 'NONE', #62770, .T. ) ;
#1028=EDGE_CURVE ( 'NONE', #14072, #47780, #49890, .T. ) ;
#1030=CARTESIAN_POINT ( 'NONE',  ( -4.135079735113203370, -3.677663764522608236, 26.00000000000000711 ) ) ;
#1035=AXIS2_PLACEMENT_3D ( 'NONE', #17679, #56207, #51240 ) ;
#1049=CARTESIAN_POINT ( 'NONE',  ( -10.03972626211731978, -8.930623737882752877, 54.00000000000000711 ) ) ;
#1052=DIRECTION ( 'NONE',  ( -1.836970198721029934E-16, -1.836970198721010706E-16, 1.000000000000000000 ) ) ;
#1055=AXIS2_PLACEMENT_3D ( 'NONE', #65789, #64755, #5720 ) ;
#1083=DIRECTION ( 'NONE',  ( -1.000000000000000000, 0.000000000000000000, 0.000000000000000000 ) ) ;
#1086=ORIENTED_EDGE ( 'NONE', *, *, #68428, .T. ) ;
#1088=LINE ( 'NONE', #64406, #5175 ) ;
#1090=PLANE ( 'NONE',  #16351 ) ;
#1098=DIRECTION ( 'NONE',  ( 1.836970198721029934E-16, 1.836970198721010706E-16, -1.000000000000000000 ) ) ;
#1103=AXIS2_PLACEMENT_3D ( 'NONE', #34668, #8490, #13452 ) ;
#1109=ADVANCED_FACE ( 'NONE', ( #55890 ), #39281, .F. ) ;
#1110=CIRCLE ( 'NONE', #40610, 1.224999999999999423 ) ;
#1114=VECTOR ( 'NONE', #19093, 1000.000000000000000 ) ;
#1115=CARTESIAN_POINT ( 'NONE',  ( 10.05377373788281581, 8.916576262117182239, 54.00000000000000711 ) ) ;
#1116=CARTESIAN_POINT ( 'NONE',  ( -1.620245201994373385, -8.241237374594328813, 54.00000000000000711 ) ) ;
#1118=ORIENTED_EDGE ( 'NONE', *, *, #34633, .F. ) ;
#1127=AXIS2_PLACEMENT_3D ( 'NONE', #13585, #57769, #40806 ) ;
#1138=CARTESIAN_POINT ( 'NONE',  ( 6.501044194225443995, 2.617976262117186703, 54.00000000000000711 ) ) ;
#1142=EDGE_LOOP ( 'NONE', ( #69661, #33730, #30512, #11876 ) ) ;
#1151=AXIS2_PLACEMENT_3D ( 'NONE', #37394, #52971, #63572 ) ;
#1154=ADVANCED_FACE ( 'NONE', ( #29703 ), #30772, .T. ) ;
#1155=CARTESIAN_POINT ( 'NONE',  ( -6.350872789121313922, -3.677663764522584255, 26.00000000000000711 ) ) ;
#1172=ADVANCED_FACE ( 'NONE', ( #68609 ), #20162, .F. ) ;
#1180=AXIS2_PLACEMENT_3D ( 'NONE', #39575, #65093, #55169 ) ;
#1186=CARTESIAN_POINT ( 'NONE',  ( 2.544523737882815162, 8.821682069070730492, 54.00000000000000711 ) ) ;
#1187=ORIENTED_EDGE ( 'NONE', *, *, #58222, .F. ) ;
#1198=DIRECTION ( 'NONE',  ( 0.000000000000000000, 1.000000000000000000, 0.000000000000000000 ) ) ;
#1206=CARTESIAN_POINT ( 'NONE',  ( -6.822336235477489019, -6.364920264886855250, 54.00000000000000711 ) ) ;
#1212=ORIENTED_EDGE ( 'NONE', *, *, #35563, .T. ) ;
#1226=ORIENTED_EDGE ( 'NONE', *, *, #66324, .T. ) ;
#1233=CARTESIAN_POINT ( 'NONE',  ( 5.552858015815581361, -7.357023737882814274, 26.00000000000000000 ) ) ;
#1239=DIRECTION ( 'NONE',  ( 1.000000000000000000, -1.883404846338789915E-14, 1.836970198720995421E-16 ) ) ;
#1242=LINE ( 'NONE', #22803, #31158 ) ;
#1245=VERTEX_POINT ( 'NONE', #46323 ) ;
#1254=LINE ( 'NONE', #34102, #2536 ) ;
#1256=VECTOR ( 'NONE', #44307, 1000.000000000000000 ) ;
#1259=CARTESIAN_POINT ( 'NONE',  ( 10.31452373788281562, -6.657023737882815873, 26.00000000000000000 ) ) ;
#1283=FACE_OUTER_BOUND ( 'NONE', #43184, .T. ) ;
#1287=ORIENTED_EDGE ( 'NONE', *, *, #46603, .T. ) ;
#1303=ORIENTED_EDGE ( 'NONE', *, *, #34868, .T. ) ;
#1304=CIRCLE ( 'NONE', #61135, 0.5249999999999994671 ) ;
#1312=VECTOR ( 'NONE', #19189, 1000.000000000000000 ) ;
#1313=EDGE_CURVE ( 'NONE', #1245, #29373, #256, .T. ) ;
#1317=ORIENTED_EDGE ( 'NONE', *, *, #31913, .T. ) ;
#1319=CIRCLE ( 'NONE', #46434, 0.1749999999999989342 ) ;
#1321=DIRECTION ( 'NONE',  ( -1.053224967557348291E-14, -1.000000000000000000, 0.000000000000000000 ) ) ;
#1329=ORIENTED_EDGE ( 'NONE', *, *, #11998, .F. ) ;
#1338=CARTESIAN_POINT ( 'NONE',  ( 6.657023737882818537, -9.912023737882819319, 54.00000000000000711 ) ) ;
#1341=DIRECTION ( 'NONE',  ( -0.000000000000000000, 3.673940397442059868E-16, -1.000000000000000000 ) ) ;
#1351=CARTESIAN_POINT ( 'NONE',  ( -6.467976262117274722, -5.257023737882803083, 26.00000000000000711 ) ) ;
#1360=ORIENTED_EDGE ( 'NONE', *, *, #2181, .F. ) ;
#1366=EDGE_CURVE ( 'NONE', #22769, #43177, #26876, .T. ) ;
#1371=VERTEX_POINT ( 'NONE', #69662 ) ;
#1376=DIRECTION ( 'NONE',  ( 0.7071067811865486830, 0.7071067811865464625, 0.000000000000000000 ) ) ;
#1378=CARTESIAN_POINT ( 'NONE',  ( -5.242976262117259978, 5.242976262117182706, 54.00000000000000711 ) ) ;
#1385=VERTEX_POINT ( 'NONE', #50502 ) ;
#1387=VERTEX_POINT ( 'NONE', #28925 ) ;
#1388=PLANE ( 'NONE',  #58139 ) ;
#1390=DIRECTION ( 'NONE',  ( 1.000000000000000000, 0.000000000000000000, 0.000000000000000000 ) ) ;
#1400=EDGE_LOOP ( 'NONE', ( #29351, #65718, #23483, #8254 ) ) ;
#1421=DIRECTION ( 'NONE',  ( 1.836970198721029934E-16, -1.836970198721036344E-16, 1.000000000000000000 ) ) ;
#1426=AXIS2_PLACEMENT_3D ( 'NONE', #25719, #57522, #15457 ) ;
#1427=EDGE_LOOP ( 'NONE', ( #23899, #9021, #40035, #61175, #33660, #14173, #23433, #811, #34516, #4708, #47273, #5222, #68139, #6145, #12426, #39969, #23820 ) ) ;
#1435=VERTEX_POINT ( 'NONE', #49472 ) ;
#1440=CARTESIAN_POINT ( 'NONE',  ( -8.566576262117260754, 8.916576262117214213, 54.00000000000000711 ) ) ;
#1444=ORIENTED_EDGE ( 'NONE', *, *, #39819, .T. ) ;
#1445=EDGE_CURVE ( 'NONE', #59664, #10161, #34093, .T. ) ;
#1447=EDGE_CURVE ( 'NONE', #37532, #3798, #20437, .T. ) ;
#1454=CARTESIAN_POINT ( 'NONE',  ( -6.651770455163739548, 7.342976262117183239, 54.00000000000000711 ) ) ;
#1456=CARTESIAN_POINT ( 'NONE',  ( -1.991476262117235274, 8.598420958951582094, 54.00000000000000711 ) ) ;
#1459=VERTEX_POINT ( 'NONE', #28236 ) ;
#1468=FACE_OUTER_BOUND ( 'NONE', #19907, .T. ) ;
#1473=VECTOR ( 'NONE', #43632, 1000.000000000000000 ) ;
#1481=VECTOR ( 'NONE', #33559, 1000.000000000000000 ) ;
#1488=CARTESIAN_POINT ( 'NONE',  ( 4.149127210878725158, 6.822336235477391320, 54.00000000000000711 ) ) ;
#1494=LINE ( 'NONE', #28367, #26018 ) ;
#1495=ORIENTED_EDGE ( 'NONE', *, *, #61365, .T. ) ;
#1497=DIRECTION ( 'NONE',  ( 1.000000000000000000, -1.813998472013049822E-14, 0.000000000000000000 ) ) ;
#1505=AXIS2_PLACEMENT_3D ( 'NONE', #583, #23529, #38412 ) ;
#1514=CARTESIAN_POINT ( 'NONE',  ( 6.836383711242970840, 4.135079735113107446, 26.00000000000000711 ) ) ;
#1517=DIRECTION ( 'NONE',  ( -1.000000000000000000, 0.000000000000000000, 0.000000000000000000 ) ) ;
#1527=EDGE_CURVE ( 'NONE', #3937, #22000, #44835, .T. ) ;
#1529=DIRECTION ( 'NONE',  ( -0.000000000000000000, 3.673940397442059868E-16, -1.000000000000000000 ) ) ;
#1538=ORIENTED_EDGE ( 'NONE', *, *, #59245, .T. ) ;
#1539=ORIENTED_EDGE ( 'NONE', *, *, #26792, .T. ) ;
#1541=ORIENTED_EDGE ( 'NONE', *, *, #827, .F. ) ;
#1549=CARTESIAN_POINT ( 'NONE',  ( -10.30047626211729472, -6.849523737882750929, 54.00000000000000711 ) ) ;
#1550=EDGE_LOOP ( 'NONE', ( #4888, #5831, #20049, #32762 ) ) ;
#1576=CARTESIAN_POINT ( 'NONE',  ( -9.722976262117294155, -6.832023737882757963, 54.00000000000000711 ) ) ;
#1579=CARTESIAN_POINT ( 'NONE',  ( -9.689726262117325462, -9.703773737882725570, 54.00000000000000711 ) ) ;
#1584=ORIENTED_EDGE ( 'NONE', *, *, #53447, .F. ) ;
#1585=EDGE_CURVE ( 'NONE', #26989, #55919, #9467, .T. ) ;
#1591=AXIS2_PLACEMENT_3D ( 'NONE', #14961, #30871, #52446 ) ;
#1607=ORIENTED_EDGE ( 'NONE', *, *, #69112, .T. ) ;
#1610=ADVANCED_FACE ( 'NONE', ( #40929 ), #46582, .T. ) ;
#1611=FACE_OUTER_BOUND ( 'NONE', #65405, .T. ) ;
#1615=ORIENTED_EDGE ( 'NONE', *, *, #28816, .F. ) ;
#1621=DIRECTION ( 'NONE',  ( -1.000000000000000000, 1.671920889371702854E-15, 6.142537696789956391E-31 ) ) ;
#1632=VERTEX_POINT ( 'NONE', #4175 ) ;
#1634=DIRECTION ( 'NONE',  ( -0.7071067811865486830, -0.7071067811865464625, -2.597868168706476160E-16 ) ) ;
#1636=CARTESIAN_POINT ( 'NONE',  ( 6.358413763958968623, -5.793274621760859944, 54.00000000000000711 ) ) ;
#1638=CARTESIAN_POINT ( 'NONE',  ( -3.842976262117224984, 9.897976262117168744, 26.00000000000000711 ) ) ;
#1640=AXIS2_PLACEMENT_3D ( 'NONE', #8943, #8593, #25581 ) ;
#1641=CYLINDRICAL_SURFACE ( 'NONE', #38486, 0.3499999999999996447 ) ;
#1647=DIRECTION ( 'NONE',  ( 3.491481338843133355E-15, 1.000000000000000000, 1.836970198721029934E-16 ) ) ;
#1650=EDGE_CURVE ( 'NONE', #57266, #62681, #23812, .T. ) ;
#1658=AXIS2_PLACEMENT_3D ( 'NONE', #22273, #7, #53407 ) ;
#1660=PLANE ( 'NONE',  #56748 ) ;
#1661=EDGE_CURVE ( 'NONE', #3520, #47586, #3115, .T. ) ;
#1669=CARTESIAN_POINT ( 'NONE',  ( -8.566576262117358453, -9.703773737882738004, 54.00000000000000711 ) ) ;
#1675=EDGE_CURVE ( 'NONE', #14837, #20832, #52186, .T. ) ;
#1683=CARTESIAN_POINT ( 'NONE',  ( 6.872275254348426010, -3.003254798005762449, 54.00000000000000711 ) ) ;
#1692=CARTESIAN_POINT ( 'NONE',  ( -9.689726262117325462, -10.05377373788272166, 26.00000000000000000 ) ) ;
#1700=EDGE_CURVE ( 'NONE', #65232, #34832, #54010, .T. ) ;
#1701=VECTOR ( 'NONE', #44410, 1000.000000000000000 ) ;
#1704=AXIS2_PLACEMENT_3D ( 'NONE', #52680, #4582, #31107 ) ;
#1711=ORIENTED_EDGE ( 'NONE', *, *, #61698, .F. ) ;
#1718=FACE_OUTER_BOUND ( 'NONE', #696, .T. ) ;
#1721=VERTEX_POINT ( 'NONE', #254 ) ;
#1729=VERTEX_POINT ( 'NONE', #54348 ) ;
#1756=FACE_OUTER_BOUND ( 'NONE', #63411, .T. ) ;
#1763=DIRECTION ( 'NONE',  ( -0.6414496315691617934, -0.7671651518152962090, -2.818519042763987834E-16 ) ) ;
#1769=CARTESIAN_POINT ( 'NONE',  ( -7.447976262117260049, 9.880476262117177555, 54.00000000000000711 ) ) ;
#1775=FACE_OUTER_BOUND ( 'NONE', #49116, .T. ) ;
#1778=LINE ( 'NONE', #766, #55320 ) ;
#1782=VERTEX_POINT ( 'NONE', #58259 ) ;
#1788=VECTOR ( 'NONE', #25866, 1000.000000000000000 ) ;
#1789=CARTESIAN_POINT ( 'NONE',  ( 8.930623737882843471, 8.566576262117187923, 54.00000000000000711 ) ) ;
#1798=VECTOR ( 'NONE', #69775, 1000.000000000000000 ) ;
#1803=CARTESIAN_POINT ( 'NONE',  ( 9.737023737882804397, 6.817976262117185549, 54.00000000000000711 ) ) ;
#1805=AXIS2_PLACEMENT_3D ( 'NONE', #44579, #17373, #38942 ) ;
#1807=DIRECTION ( 'NONE',  ( -3.540251991789403884E-15, -1.000000000000000000, 0.000000000000000000 ) ) ;
#1808=CARTESIAN_POINT ( 'NONE',  ( -8.227189898828745740, 1.620245201994245043, 54.00000000000000711 ) ) ;
#1811=VERTEX_POINT ( 'NONE', #49039 ) ;
#1825=VERTEX_POINT ( 'NONE', #32082 ) ;
#1826=DIRECTION ( 'NONE',  ( -4.745709458399858621E-16, -1.000000000000000000, 0.000000000000000000 ) ) ;
#1832=CARTESIAN_POINT ( 'NONE',  ( 6.364920264886885448, -3.677663764522618450, 26.00000000000000711 ) ) ;
#1834=ORIENTED_EDGE ( 'NONE', *, *, #11388, .T. ) ;
#1836=DIRECTION ( 'NONE',  ( 2.478176394252584099E-15, 1.000000000000000000, 0.000000000000000000 ) ) ;
#1843=DIRECTION ( 'NONE',  ( 0.000000000000000000, 0.000000000000000000, 1.000000000000000000 ) ) ;
#1845=AXIS2_PLACEMENT_3D ( 'NONE', #32567, #54131, #58738 ) ;
#1849=FACE_OUTER_BOUND ( 'NONE', #5558, .T. ) ;
#1850=ORIENTED_EDGE ( 'NONE', *, *, #6567, .T. ) ;
#1854=VECTOR ( 'NONE', #50629, 1000.000000000000000 ) ;
#1863=CARTESIAN_POINT ( 'NONE',  ( 3.157023737882804770, 6.486996718459879574, 54.00000000000000711 ) ) ;
#1878=ORIENTED_EDGE ( 'NONE', *, *, #36967, .F. ) ;
#1883=PLANE ( 'NONE',  #41894 ) ;
#1885=ADVANCED_FACE ( 'NONE', ( #16862 ), #962, .F. ) ;
#1915=ORIENTED_EDGE ( 'NONE', *, *, #64017, .T. ) ;
#1923=DIRECTION ( 'NONE',  ( 1.000000000000000000, 0.000000000000000000, 0.000000000000000000 ) ) ;
#1928=CARTESIAN_POINT ( 'NONE',  ( 3.003254798005744242, -6.872275254348403806, 26.00000000000000000 ) ) ;
#1937=FACE_OUTER_BOUND ( 'NONE', #59015, .T. ) ;
#1938=DIRECTION ( 'NONE',  ( 0.000000000000000000, 1.000000000000000000, 0.000000000000000000 ) ) ;
#1942=DIRECTION ( 'NONE',  ( -1.836970198721029934E-16, -1.836970198721010706E-16, 1.000000000000000000 ) ) ;
#1948=DIRECTION ( 'NONE',  ( -1.836970198721029934E-16, 1.836970198721036590E-16, -1.000000000000000000 ) ) ;
#1950=CARTESIAN_POINT ( 'NONE',  ( 9.562023737882761054, 2.530476262117158370, 26.00000000000000711 ) ) ;
#1953=VERTEX_POINT ( 'NONE', #23194 ) ;
#1957=AXIS2_PLACEMENT_3D ( 'NONE', #1579, #1942, #23149 ) ;
#1960=CARTESIAN_POINT ( 'NONE',  ( 3.664523737882781518, -10.31452373788279964, 26.00000000000000000 ) ) ;
#1968=CARTESIAN_POINT ( 'NONE',  ( 8.144523737882806813, 8.821682069070714505, 26.00000000000000711 ) ) ;
#1989=EDGE_CURVE ( 'NONE', #56362, #44739, #47548, .T. ) ;
#2014=FACE_OUTER_BOUND ( 'NONE', #23892, .T. ) ;
#2029=FACE_OUTER_BOUND ( 'NONE', #16923, .T. ) ;
#2034=AXIS2_PLACEMENT_3D ( 'NONE', #68676, #52055, #52410 ) ;
#2039=DIRECTION ( 'NONE',  ( -1.000000000000000000, 1.819560449471430698E-15, 1.836970198721033385E-16 ) ) ;
#2053=ORIENTED_EDGE ( 'NONE', *, *, #14448, .F. ) ;
#2056=EDGE_CURVE ( 'NONE', #59501, #58190, #49801, .T. ) ;
#2058=DIRECTION ( 'NONE',  ( -1.000000000000000000, 1.088659024508174415E-14, 0.000000000000000000 ) ) ;
#2060=ORIENTED_EDGE ( 'NONE', *, *, #64688, .F. ) ;
#2062=ORIENTED_EDGE ( 'NONE', *, *, #67652, .T. ) ;
#2066=CYLINDRICAL_SURFACE ( 'NONE', #48548, 0.3499999999999996447 ) ;
#2067=CARTESIAN_POINT ( 'NONE',  ( -10.30047626211725742, 6.642976262117184838, 54.00000000000000711 ) ) ;
#2090=EDGE_CURVE ( 'NONE', #55737, #53865, #67391, .T. ) ;
#2093=CARTESIAN_POINT ( 'NONE',  ( -6.642976262117260333, 9.897976262117179402, 26.00000000000000711 ) ) ;
#2094=CARTESIAN_POINT ( 'NONE',  ( 9.703773737882810835, 9.689726262117158484, 26.00000000000000711 ) ) ;
#2095=DIRECTION ( 'NONE',  ( -0.000000000000000000, -0.000000000000000000, -1.000000000000000000 ) ) ;
#2101=CARTESIAN_POINT ( 'NONE',  ( 9.562023737882814345, -2.544523737882825820, 54.00000000000000711 ) ) ;
#2102=CARTESIAN_POINT ( 'NONE',  ( 9.737023737882783081, 3.667976262117152775, 54.00000000000000711 ) ) ;
#2105=ORIENTED_EDGE ( 'NONE', *, *, #10566, .F. ) ;
#2108=CARTESIAN_POINT ( 'NONE',  ( 9.562023737882812569, -2.369523737882825998, 54.00000000000000711 ) ) ;
#2116=CARTESIAN_POINT ( 'NONE',  ( -4.031976262117253462, -3.157023737882814096, 26.00000000000000711 ) ) ;
#2123=VERTEX_POINT ( 'NONE', #5748 ) ;
#2125=LINE ( 'NONE', #45243, #38508 ) ;
#2129=FACE_BOUND ( 'NONE', #68189, .T. ) ;
#2138=EDGE_CURVE ( 'NONE', #5502, #8082, #32955, .T. ) ;
#2140=CARTESIAN_POINT ( 'NONE',  ( -10.49297626211726175, 6.835476262117182955, 26.00000000000000711 ) ) ;
#2141=LINE ( 'NONE', #23705, #51303 ) ;
#2146=CIRCLE ( 'NONE', #17934, 0.1749999999999980738 ) ;
#2147=ADVANCED_FACE ( 'NONE', ( #44243 ), #32619, .F. ) ;
#2148=CARTESIAN_POINT ( 'NONE',  ( 3.848229544836323512, -7.357023737882812497, 54.00000000000000711 ) ) ;
#2154=LINE ( 'NONE', #13808, #20810 ) ;
#2159=ORIENTED_EDGE ( 'NONE', *, *, #34968, .T. ) ;
#2163=ADVANCED_FACE ( 'NONE', ( #21658 ), #21999, .F. ) ;
#2181=EDGE_CURVE ( 'NONE', #66583, #36010, #60164, .T. ) ;
#2188=DIRECTION ( 'NONE',  ( -1.000000000000000000, -2.135044278125301343E-15, 0.000000000000000000 ) ) ;
#2194=FACE_OUTER_BOUND ( 'NONE', #18891, .T. ) ;
#2196=EDGE_LOOP ( 'NONE', ( #38925, #20069, #46346, #38174 ) ) ;
#2199=CARTESIAN_POINT ( 'NONE',  ( -9.390476262117209316, -1.480523737882732060, 54.00000000000000711 ) ) ;
#2202=PLANE ( 'NONE',  #24225 ) ;
#2203=PLANE ( 'NONE',  #61687 ) ;
#2209=VECTOR ( 'NONE', #42059, 1000.000000000000114 ) ;
#2214=ORIENTED_EDGE ( 'NONE', *, *, #35787, .F. ) ;
#2224=CARTESIAN_POINT ( 'NONE',  ( -6.350872789121327244, 6.822336235477381550, 54.00000000000000711 ) ) ;
#2234=AXIS2_PLACEMENT_3D ( 'NONE', #48982, #69493, #59234 ) ;
#2240=ORIENTED_EDGE ( 'NONE', *, *, #46153, .F. ) ;
#2241=ORIENTED_EDGE ( 'NONE', *, *, #59283, .T. ) ;
#2242=ADVANCED_FACE ( 'NONE', ( #40688 ), #17732, .F. ) ;
#2256=ORIENTED_EDGE ( 'NONE', *, *, #22911, .T. ) ;
#2260=ORIENTED_EDGE ( 'NONE', *, *, #66512, .F. ) ;
#2264=ORIENTED_EDGE ( 'NONE', *, *, #25922, .T. ) ;
#2271=DIRECTION ( 'NONE',  ( 7.457533623526253657E-15, 1.000000000000000000, 0.000000000000000000 ) ) ;
#2278=DIRECTION ( 'NONE',  ( 2.135044278125299371E-15, 1.000000000000000000, 0.000000000000000000 ) ) ;
#2301=CARTESIAN_POINT ( 'NONE',  ( 10.31452373788280674, 6.835476262117182067, 54.00000000000000711 ) ) ;
#2313=ORIENTED_EDGE ( 'NONE', *, *, #68299, .F. ) ;
#2344=DIRECTION ( 'NONE',  ( -1.000000000000000000, 0.000000000000000000, 0.000000000000000000 ) ) ;
#2345=VERTEX_POINT ( 'NONE', #13462 ) ;
#2346=CARTESIAN_POINT ( 'NONE',  ( -8.130476262117316111, -8.835729544836294025, 54.00000000000000711 ) ) ;
#2350=EDGE_LOOP ( 'NONE', ( #756, #58061, #29808, #46109 ) ) ;
#2372=DIRECTION ( 'NONE',  ( 1.000000000000000000, -5.163402228214836012E-15, -1.836970198721039548E-16 ) ) ;
#2374=DIRECTION ( 'NONE',  ( -3.491481338843133355E-15, -1.000000000000000000, 0.000000000000000000 ) ) ;
#2377=CYLINDRICAL_SURFACE ( 'NONE', #19870, 0.1749999999999998224 ) ;
#2380=LINE ( 'NONE', #46903, #22864 ) ;
#2385=ORIENTED_EDGE ( 'NONE', *, *, #45734, .F. ) ;
#2387=DIRECTION ( 'NONE',  ( 0.000000000000000000, 3.673940397442059868E-16, -1.000000000000000000 ) ) ;
#2389=LINE ( 'NONE', #8379, #24068 ) ;
#2395=VERTEX_POINT ( 'NONE', #15228 ) ;
#2396=DIRECTION ( 'NONE',  ( 1.073876437509453175E-14, 1.000000000000000000, 0.000000000000000000 ) ) ;
#2407=VECTOR ( 'NONE', #5030, 1000.000000000000000 ) ;
#2410=CARTESIAN_POINT ( 'NONE',  ( -10.49297626211729018, -6.849523737882743823, 26.00000000000000000 ) ) ;
#2421=DIRECTION ( 'NONE',  ( -0.000000000000000000, 3.673940397442059868E-16, -1.000000000000000000 ) ) ;
#2429=EDGE_CURVE ( 'NONE', #3011, #6950, #52358, .T. ) ;
#2439=FACE_OUTER_BOUND ( 'NONE', #38568, .T. ) ;
#2440=DIRECTION ( 'NONE',  ( 0.000000000000000000, -1.000000000000000000, -3.673940397442059868E-16 ) ) ;
#2456=ORIENTED_EDGE ( 'NONE', *, *, #33545, .T. ) ;
#2460=EDGE_LOOP ( 'NONE', ( #4758, #41144, #40239, #41807 ) ) ;
#2482=EDGE_CURVE ( 'NONE', #57396, #55087, #36799, .T. ) ;
#2486=VERTEX_POINT ( 'NONE', #3214 ) ;
#2487=VERTEX_POINT ( 'NONE', #19464 ) ;
#2490=ORIENTED_EDGE ( 'NONE', *, *, #22488, .F. ) ;
#2492=CARTESIAN_POINT ( 'NONE',  ( -9.722976262117249746, -3.682023737882726522, 54.00000000000000711 ) ) ;
#2494=EDGE_CURVE ( 'NONE', #38025, #9849, #62592, .T. ) ;
#2499=LINE ( 'NONE', #61901, #38927 ) ;
#2503=VERTEX_POINT ( 'NONE', #5666 ) ;
#2504=VERTEX_POINT ( 'NONE', #33216 ) ;
#2509=EDGE_CURVE ( 'NONE', #21898, #47065, #43241, .T. ) ;
#2510=DIRECTION ( 'NONE',  ( -1.000000000000000000, 0.000000000000000000, 0.000000000000000000 ) ) ;
#2516=DIRECTION ( 'NONE',  ( -0.000000000000000000, 3.673940397442059868E-16, -1.000000000000000000 ) ) ;
#2517=ORIENTED_EDGE ( 'NONE', *, *, #16738, .F. ) ;
#2523=DIRECTION ( 'NONE',  ( 0.8660254037844358210, -0.5000000000000049960, 0.000000000000000000 ) ) ;
#2528=DIRECTION ( 'NONE',  ( -1.000000000000000000, 0.000000000000000000, 0.000000000000000000 ) ) ;
#2529=LINE ( 'NONE', #13490, #62251 ) ;
#2536=VECTOR ( 'NONE', #33763, 1000.000000000000000 ) ;
#2541=ORIENTED_EDGE ( 'NONE', *, *, #2672, .F. ) ;
#2543=CARTESIAN_POINT ( 'NONE',  ( -8.821682069070780230, 8.130476262117182884, 54.00000000000000711 ) ) ;
#2548=EDGE_CURVE ( 'NONE', #55844, #32281, #12724, .T. ) ;
#2556=CIRCLE ( 'NONE', #42093, 0.3499999999999996447 ) ;
#2570=EDGE_CURVE ( 'NONE', #7476, #5949, #50038, .T. ) ;
#2574=DIRECTION ( 'NONE',  ( -1.000000000000000000, 0.000000000000000000, 0.000000000000000000 ) ) ;
#2575=ORIENTED_EDGE ( 'NONE', *, *, #29145, .T. ) ;
#2584=DIRECTION ( 'NONE',  ( -1.000000000000000000, 0.000000000000000000, 0.000000000000000000 ) ) ;
#2593=EDGE_CURVE ( 'NONE', #22404, #37400, #22277, .T. ) ;
#2605=ORIENTED_EDGE ( 'NONE', *, *, #14448, .T. ) ;
#2608=VERTEX_POINT ( 'NONE', #15589 ) ;
#2614=DIRECTION ( 'NONE',  ( 1.000000000000000000, -7.457533623526253657E-15, 1.836970198721015882E-16 ) ) ;
#2635=VECTOR ( 'NONE', #63375, 1000.000000000000000 ) ;
#2644=CARTESIAN_POINT ( 'NONE',  ( -4.706725378239251967, -4.155633711806651753, 54.00000000000000711 ) ) ;
#2672=EDGE_CURVE ( 'NONE', #56266, #21095, #65739, .T. ) ;
#2674=DIRECTION ( 'NONE',  ( 1.836970198721029934E-16, -1.836970198721036344E-16, 1.000000000000000000 ) ) ;
#2675=CARTESIAN_POINT ( 'NONE',  ( 10.50702373788281996, -6.849523737882814878, 26.00000000000000000 ) ) ;
#2679=EDGE_CURVE ( 'NONE', #44308, #34611, #39211, .T. ) ;
#2687=ORIENTED_EDGE ( 'NONE', *, *, #58098, .T. ) ;
#2690=ORIENTED_EDGE ( 'NONE', *, *, #67987, .T. ) ;
#2692=ORIENTED_EDGE ( 'NONE', *, *, #40418, .F. ) ;
#2698=CARTESIAN_POINT ( 'NONE',  ( 3.857023737882817827, 9.897976262117204271, 54.00000000000000711 ) ) ;
#2701=VERTEX_POINT ( 'NONE', #60419 ) ;
#2703=CARTESIAN_POINT ( 'NONE',  ( 3.157023737882797665, 4.031976262117209053, 54.00000000000000711 ) ) ;
#2708=CARTESIAN_POINT ( 'NONE',  ( -10.49297626211726175, 6.835476262117182955, 54.00000000000000711 ) ) ;
#2716=EDGE_CURVE ( 'NONE', #68424, #29039, #34928, .T. ) ;
#2720=ADVANCED_FACE ( 'NONE', ( #28940 ), #45192, .F. ) ;
#2726=CARTESIAN_POINT ( 'NONE',  ( 8.144523737882817471, -8.835729544836334881, 26.00000000000000000 ) ) ;
#2736=ORIENTED_EDGE ( 'NONE', *, *, #38625, .F. ) ;
#2737=DIRECTION ( 'NONE',  ( -9.050731179009442381E-15, -1.000000000000000000, 0.000000000000000000 ) ) ;
#2743=LINE ( 'NONE', #57809, #15256 ) ;
#2745=ORIENTED_EDGE ( 'NONE', *, *, #58098, .F. ) ;
#2750=PRODUCT_DEFINITION_CONTEXT ( 'detailed design', #44027, 'design' ) ;
#2752=CARTESIAN_POINT ( 'NONE',  ( 6.657023737882821202, 10.30047626211719347, 54.00000000000000711 ) ) ;
#2756=VERTEX_POINT ( 'NONE', #56510 ) ;
#2763=AXIS2_PLACEMENT_3D ( 'NONE', #55945, #29415, #56294 ) ;
#2767=ORIENTED_EDGE ( 'NONE', *, *, #16069, .T. ) ;
#2772=VERTEX_POINT ( 'NONE', #18319 ) ;
#2776=ORIENTED_EDGE ( 'NONE', *, *, #11169, .T. ) ;
#2777=ORIENTED_EDGE ( 'NONE', *, *, #34728, .T. ) ;
#2779=DIRECTION ( 'NONE',  ( 0.000000000000000000, -3.673940397442059868E-16, 1.000000000000000000 ) ) ;
#2781=EDGE_LOOP ( 'NONE', ( #55650, #12350, #23767, #57102 ) ) ;
#2787=DIRECTION ( 'NONE',  ( 3.016910393003147986E-15, 1.000000000000000000, -0.000000000000000000 ) ) ;
#2788=AXIS2_PLACEMENT_3D ( 'NONE', #55122, #5644, #37819 ) ;
#2792=ORIENTED_EDGE ( 'NONE', *, *, #29625, .T. ) ;
#2795=VECTOR ( 'NONE', #15106, 1000.000000000000000 ) ;
#2796=CARTESIAN_POINT ( 'NONE',  ( 6.849523737882817542, -10.50702373788282529, 54.00000000000000711 ) ) ;
#2803=EDGE_CURVE ( 'NONE', #54522, #20164, #29274, .T. ) ;
#2808=VECTOR ( 'NONE', #20875, 1000.000000000000114 ) ;
#2813=ORIENTED_EDGE ( 'NONE', *, *, #57418, .F. ) ;
#2817=DIRECTION ( 'NONE',  ( 4.745709458399858621E-16, 1.000000000000000000, 1.836970198721035604E-16 ) ) ;
#2819=CARTESIAN_POINT ( 'NONE',  ( 8.835729544836338434, -2.544523737882825820, 54.00000000000000711 ) ) ;
#2821=DIRECTION ( 'NONE',  ( -0.000000000000000000, 0.000000000000000000, -1.000000000000000000 ) ) ;
#2828=DIRECTION ( 'NONE',  ( 0.000000000000000000, 3.673940397442059868E-16, -1.000000000000000000 ) ) ;
#2830=ORIENTED_EDGE ( 'NONE', *, *, #47593, .T. ) ;
#2840=DIRECTION ( 'NONE',  ( -1.000000000000000000, 1.952517519553884087E-14, 0.000000000000000000 ) ) ;
#2845=CARTESIAN_POINT ( 'NONE',  ( 5.257023737882801306, 5.242976262117200470, 54.00000000000000711 ) ) ;
#2848=DIRECTION ( 'NONE',  ( 1.836970198721029934E-16, 1.836970198721010706E-16, -1.000000000000000000 ) ) ;
#2854=AXIS2_PLACEMENT_3D ( 'NONE', #30402, #3534, #52322 ) ;
#2856=VECTOR ( 'NONE', #907, 1000.000000000000000 ) ;
#2861=ORIENTED_EDGE ( 'NONE', *, *, #54468, .T. ) ;
#2866=LINE ( 'NONE', #60527, #656 ) ;
#2882=LINE ( 'NONE', #12101, #66209 ) ;
#2887=PLANE ( 'NONE',  #12297 ) ;
#2889=FACE_OUTER_BOUND ( 'NONE', #2781, .T. ) ;
#2903=ORIENTED_EDGE ( 'NONE', *, *, #67141, .F. ) ;
#2907=FACE_OUTER_BOUND ( 'NONE', #45930, .T. ) ;
#2914=ORIENTED_EDGE ( 'NONE', *, *, #36272, .T. ) ;
#2919=AXIS2_PLACEMENT_3D ( 'NONE', #37340, #69509, #10456 ) ;
#2924=VECTOR ( 'NONE', #69150, 1000.000000000000000 ) ;
#2928=ORIENTED_EDGE ( 'NONE', *, *, #39145, .F. ) ;
#2930=ORIENTED_EDGE ( 'NONE', *, *, #13341, .F. ) ;
#2939=ORIENTED_EDGE ( 'NONE', *, *, #5863, .F. ) ;
#2949=ORIENTED_EDGE ( 'NONE', *, *, #50142, .T. ) ;
#2952=ORIENTED_EDGE ( 'NONE', *, *, #27943, .T. ) ;
#2957=CARTESIAN_POINT ( 'NONE',  ( -3.650476262117221093, 10.49297626211717116, 54.00000000000000711 ) ) ;
#2962=ADVANCED_FACE ( 'NONE', ( #34812 ), #24218, .F. ) ;
#2975=ADVANCED_FACE ( 'NONE', ( #51440 ), #29164, .F. ) ;
#2976=ORIENTED_EDGE ( 'NONE', *, *, #65832, .F. ) ;
#2984=DIRECTION ( 'NONE',  ( 1.836970198721029934E-16, 1.836970198721010706E-16, -1.000000000000000000 ) ) ;
#2987=ORIENTED_EDGE ( 'NONE', *, *, #26747, .T. ) ;
#2988=DIRECTION ( 'NONE',  ( 3.304235192336778667E-15, 1.000000000000000000, 0.000000000000000000 ) ) ;
#2998=DIRECTION ( 'NONE',  ( -1.000000000000000000, 0.000000000000000000, 0.000000000000000000 ) ) ;
#3001=DIRECTION ( 'NONE',  ( -1.000000000000000000, 0.000000000000000000, 0.000000000000000000 ) ) ;
#3004=EDGE_CURVE ( 'NONE', #54028, #17979, #56044, .T. ) ;
#3011=VERTEX_POINT ( 'NONE', #7600 ) ;
#3030=CYLINDRICAL_SURFACE ( 'NONE', #4850, 0.1749999999999998224 ) ;
#3034=ORIENTED_EDGE ( 'NONE', *, *, #1447, .F. ) ;
#3036=CIRCLE ( 'NONE', #42561, 0.5249999999999994671 ) ;
#3047=EDGE_CURVE ( 'NONE', #19854, #10245, #47877, .T. ) ;
#3051=EDGE_CURVE ( 'NONE', #27113, #13327, #51793, .T. ) ;
#3053=ORIENTED_EDGE ( 'NONE', *, *, #52892, .T. ) ;
#3056=CARTESIAN_POINT ( 'NONE',  ( -8.916576262117260399, 8.566576262117216345, 26.00000000000000711 ) ) ;
#3057=ORIENTED_EDGE ( 'NONE', *, *, #59190, .T. ) ;
#3065=CARTESIAN_POINT ( 'NONE',  ( 6.665817930929289759, 7.517976262117195496, 54.00000000000000711 ) ) ;
#3071=CARTESIAN_POINT ( 'NONE',  ( -9.722976262117249746, -3.682023737882726522, 54.00000000000000711 ) ) ;
#3082=CARTESIAN_POINT ( 'NONE',  ( 5.257023737882819070, -5.257023737882815517, 26.00000000000000711 ) ) ;
#3105=LINE ( 'NONE', #1440, #21392 ) ;
#3114=EDGE_LOOP ( 'NONE', ( #58283, #34162, #31033, #23673 ) ) ;
#3115=LINE ( 'NONE', #25378, #11402 ) ;
#3116=ORIENTED_EDGE ( 'NONE', *, *, #68278, .T. ) ;
#3123=LINE ( 'NONE', #57553, #11800 ) ;
#3128=AXIS2_PLACEMENT_3D ( 'NONE', #66980, #46464, #56034 ) ;
#3134=EDGE_CURVE ( 'NONE', #29241, #49648, #46477, .T. ) ;
#3136=EDGE_CURVE ( 'NONE', #32081, #47780, #15368, .T. ) ;
#3147=EDGE_LOOP ( 'NONE', ( #19987, #516, #19250, #56082 ) ) ;
#3149=DIRECTION ( 'NONE',  ( -0.000000000000000000, -0.000000000000000000, -1.000000000000000000 ) ) ;
#3150=ORIENTED_EDGE ( 'NONE', *, *, #36264, .T. ) ;
#3152=CARTESIAN_POINT ( 'NONE',  ( 6.849523737882814878, 10.30047626211719702, 26.00000000000000711 ) ) ;
#3153=DIRECTION ( 'NONE',  ( -0.7071067811865446862, 0.7071067811865503483, 0.000000000000000000 ) ) ;
#3154=EDGE_LOOP ( 'NONE', ( #62891, #51251, #14686, #44057 ) ) ;
#3156=PLANE ( 'NONE',  #24630 ) ;
#3165=CARTESIAN_POINT ( 'NONE',  ( 5.793274621760843957, -6.358413763958979281, 54.00000000000000711 ) ) ;
#3170=LINE ( 'NONE', #40982, #10866 ) ;
#3174=EDGE_CURVE ( 'NONE', #32604, #34404, #52863, .T. ) ;
#3176=EDGE_CURVE ( 'NONE', #21488, #15324, #33189, .T. ) ;
#3202=ORIENTED_EDGE ( 'NONE', *, *, #38585, .T. ) ;
#3206=LINE ( 'NONE', #2492, #35776 ) ;
#3208=DIRECTION ( 'NONE',  ( -9.912705577010344285E-15, -1.000000000000000000, 0.000000000000000000 ) ) ;
#3212=LINE ( 'NONE', #19805, #32364 ) ;
#3213=VERTEX_POINT ( 'NONE', #42924 ) ;
#3214=CARTESIAN_POINT ( 'NONE',  ( -7.342976262117273833, -4.961189459950004377, 54.00000000000000711 ) ) ;
#3217=ORIENTED_EDGE ( 'NONE', *, *, #22049, .T. ) ;
#3236=DIRECTION ( 'NONE',  ( -0.000000000000000000, -0.000000000000000000, -1.000000000000000000 ) ) ;
#3239=FACE_OUTER_BOUND ( 'NONE', #59744, .T. ) ;
#3243=CYLINDRICAL_SURFACE ( 'NONE', #5265, 0.1749999999999989342 ) ;
#3262=DIRECTION ( 'NONE',  ( 0.000000000000000000, 1.000000000000000000, 0.000000000000000000 ) ) ;
#3268=CIRCLE ( 'NONE', #40553, 0.1749999999999998224 ) ;
#3274=EDGE_CURVE ( 'NONE', #41781, #62241, #43962, .T. ) ;
#3277=ORIENTED_EDGE ( 'NONE', *, *, #49222, .T. ) ;
#3279=ORIENTED_EDGE ( 'NONE', *, *, #69682, .T. ) ;
#3283=CARTESIAN_POINT ( 'NONE',  ( -9.722976262117226653, -2.544523737882726344, 54.00000000000000711 ) ) ;
#3288=AXIS2_PLACEMENT_3D ( 'NONE', #16995, #60461, #32910 ) ;
#3290=ORIENTED_EDGE ( 'NONE', *, *, #31771, .T. ) ;
#3298=EDGE_CURVE ( 'NONE', #8082, #16593, #42224, .T. ) ;
#3299=EDGE_LOOP ( 'NONE', ( #41233, #6220, #68864, #10764 ) ) ;
#3304=VERTEX_POINT ( 'NONE', #69451 ) ;
#3313=EDGE_CURVE ( 'NONE', #30867, #14406, #5465, .T. ) ;
#3319=ORIENTED_EDGE ( 'NONE', *, *, #51400, .F. ) ;
#3326=ORIENTED_EDGE ( 'NONE', *, *, #63904, .T. ) ;
#3337=CARTESIAN_POINT ( 'NONE',  ( 8.612468434717241550, -1.480523737882815549, 26.00000000000000711 ) ) ;
#3338=VERTEX_POINT ( 'NONE', #11098 ) ;
#3339=FACE_OUTER_BOUND ( 'NONE', #41905, .T. ) ;
#3340=LINE ( 'NONE', #15352, #11412 ) ;
#3345=CARTESIAN_POINT ( 'NONE',  ( 9.562023737882805463, 8.130476262117184660, 54.00000000000000711 ) ) ;
#3361=CARTESIAN_POINT ( 'NONE',  ( 10.31452373788281562, -6.849523737882823760, 54.00000000000000711 ) ) ;
#3362=ORIENTED_EDGE ( 'NONE', *, *, #44019, .F. ) ;
#3365=EDGE_LOOP ( 'NONE', ( #430, #37714, #11740, #16677 ) ) ;
#3373=AXIS2_PLACEMENT_3D ( 'NONE', #57861, #35952, #9429 ) ;
#3389=FACE_OUTER_BOUND ( 'NONE', #19594, .T. ) ;
#3391=VERTEX_POINT ( 'NONE', #67552 ) ;
#3393=VERTEX_POINT ( 'NONE', #13088 ) ;
#3394=ORIENTED_EDGE ( 'NONE', *, *, #64702, .T. ) ;
#3400=EDGE_CURVE ( 'NONE', #53683, #49178, #41009, .T. ) ;
#3401=CARTESIAN_POINT ( 'NONE',  ( -7.517976262117252340, -3.848229544836285321, 54.00000000000000711 ) ) ;
#3407=DIRECTION ( 'NONE',  ( -0.000000000000000000, -0.000000000000000000, -1.000000000000000000 ) ) ;
#3424=DIRECTION ( 'NONE',  ( 1.000000000000000000, -1.088659024508174415E-14, 1.836970198721009966E-16 ) ) ;
#3426=FACE_OUTER_BOUND ( 'NONE', #17614, .T. ) ;
#3435=AXIS2_PLACEMENT_3D ( 'NONE', #14473, #18714, #56545 ) ;
#3437=CARTESIAN_POINT ( 'NONE',  ( 10.50702373788278265, 3.650476262117142934, 54.00000000000000711 ) ) ;
#3440=EDGE_CURVE ( 'NONE', #58150, #29117, #2141, .T. ) ;
#3443=DIRECTION ( 'NONE',  ( -0.7671651518153087546, -0.6414496315691469164, 2.309356642089053889E-17 ) ) ;
#3444=PLANE ( 'NONE',  #58361 ) ;
#3445=LINE ( 'NONE', #46216, #62608 ) ;
#3456=ORIENTED_EDGE ( 'NONE', *, *, #11388, .F. ) ;
#3464=ORIENTED_EDGE ( 'NONE', *, *, #62935, .T. ) ;
#3468=ORIENTED_EDGE ( 'NONE', *, *, #50494, .T. ) ;
#3472=CIRCLE ( 'NONE', #55406, 1.224999999999998757 ) ;
#3484=AXIS2_PLACEMENT_3D ( 'NONE', #16611, #20858, #54435 ) ;
#3510=DIRECTION ( 'NONE',  ( -1.000000000000000000, 5.626525616968433120E-15, 0.000000000000000000 ) ) ;
#3511=CARTESIAN_POINT ( 'NONE',  ( 9.929523737882748335, 0.9414762621171531842, 26.00000000000000711 ) ) ;
#3520=VERTEX_POINT ( 'NONE', #42769 ) ;
#3523=CARTESIAN_POINT ( 'NONE',  ( -9.547976262117254365, 8.130476262117182884, 26.00000000000000711 ) ) ;
#3524=CIRCLE ( 'NONE', #42988, 0.5250000000000003553 ) ;
#3527=DIRECTION ( 'NONE',  ( -3.491481338843133355E-15, -1.000000000000000000, -1.836970198721029934E-16 ) ) ;
#3534=DIRECTION ( 'NONE',  ( 0.000000000000000000, 3.673940397442059868E-16, -1.000000000000000000 ) ) ;
#3544=ORIENTED_EDGE ( 'NONE', *, *, #2138, .T. ) ;
#3554=EDGE_LOOP ( 'NONE', ( #19642, #44567, #61700, #49917 ) ) ;
#3560=DIRECTION ( 'NONE',  ( -1.836970198721029934E-16, -1.836970198721010706E-16, 1.000000000000000000 ) ) ;
#3561=ORIENTED_EDGE ( 'NONE', *, *, #66313, .F. ) ;
#3568=EDGE_LOOP ( 'NONE', ( #64677, #30089, #9976, #16076 ) ) ;
#3578=DIRECTION ( 'NONE',  ( 1.000000000000000000, -1.047444401652940007E-14, 1.836970198721010706E-16 ) ) ;
#3583=ORIENTED_EDGE ( 'NONE', *, *, #49603, .T. ) ;
#3586=ORIENTED_EDGE ( 'NONE', *, *, #6130, .T. ) ;
#3592=ORIENTED_EDGE ( 'NONE', *, *, #9385, .T. ) ;
#3594=LINE ( 'NONE', #46364, #7930 ) ;
#3595=DIRECTION ( 'NONE',  ( 0.000000000000000000, -3.673940397442059868E-16, 1.000000000000000000 ) ) ;
#3611=LINE ( 'NONE', #1259, #55065 ) ;
#3615=ORIENTED_EDGE ( 'NONE', *, *, #46826, .F. ) ;
#3621=DIRECTION ( 'NONE',  ( -0.6414496315691420314, 0.7671651518153128624, 2.587583378555127804E-16 ) ) ;
#3622=EDGE_CURVE ( 'NONE', #15670, #38025, #33193, .T. ) ;
#3627=LINE ( 'NONE', #40748, #20027 ) ;
#3631=CARTESIAN_POINT ( 'NONE',  ( -3.650476262117223314, 10.30047626211716683, 26.00000000000000711 ) ) ;
#3636=ORIENTED_EDGE ( 'NONE', *, *, #39034, .T. ) ;
#3637=AXIS2_PLACEMENT_3D ( 'NONE', #50835, #67105, #45529 ) ;
#3643=AXIS2_PLACEMENT_3D ( 'NONE', #659, #33172, #27875 ) ;
#3645=CARTESIAN_POINT ( 'NONE',  ( -7.605476262117258024, 9.722976262117178692, 26.00000000000000711 ) ) ;
#3662=ORIENTED_EDGE ( 'NONE', *, *, #33384, .T. ) ;
#3665=ORIENTED_EDGE ( 'NONE', *, *, #21227, .T. ) ;
#3669=DIRECTION ( 'NONE',  ( -1.836970198721029934E-16, 1.836970198721036344E-16, -1.000000000000000000 ) ) ;
#3672=CARTESIAN_POINT ( 'NONE',  ( -9.547976262117300550, -8.144523737882753522, 26.00000000000000000 ) ) ;
#3680=AXIS2_PLACEMENT_3D ( 'NONE', #27732, #890, #38685 ) ;
#3681=DIRECTION ( 'NONE',  ( 1.836970198721029934E-16, -1.836970198721036344E-16, 1.000000000000000000 ) ) ;
#3691=VECTOR ( 'NONE', #57312, 1000.000000000000000 ) ;
#3697=ADVANCED_FACE ( 'NONE', ( #688 ), #11955, .F. ) ;
#3714=ADVANCED_FACE ( 'NONE', ( #28573 ), #27546, .F. ) ;
#3715=LINE ( 'NONE', #53559, #19271 ) ;
#3720=EDGE_CURVE ( 'NONE', #29410, #14602, #11612, .T. ) ;
#3722=FACE_OUTER_BOUND ( 'NONE', #15976, .T. ) ;
#3727=ORIENTED_EDGE ( 'NONE', *, *, #15369, .T. ) ;
#3733=ORIENTED_EDGE ( 'NONE', *, *, #55453, .T. ) ;
#3734=DIRECTION ( 'NONE',  ( 0.7671651518152963201, 0.6414496315691619044, 2.356647714346269747E-16 ) ) ;
#3753=DIRECTION ( 'NONE',  ( 0.4999999999999786282, -0.8660254037844510311, 0.000000000000000000 ) ) ;
#3758=FACE_OUTER_BOUND ( 'NONE', #61316, .T. ) ;
#3773=CARTESIAN_POINT ( 'NONE',  ( 9.562023737882805463, 8.130476262117184660, 54.00000000000000711 ) ) ;
#3783=CIRCLE ( 'NONE', #33155, 1.224999999999998757 ) ;
#3788=FACE_OUTER_BOUND ( 'NONE', #14959, .T. ) ;
#3789=LINE ( 'NONE', #36313, #55849 ) ;
#3790=VECTOR ( 'NONE', #48729, 1000.000000000000000 ) ;
#3795=ORIENTED_EDGE ( 'NONE', *, *, #51195, .F. ) ;
#3798=VERTEX_POINT ( 'NONE', #34913 ) ;
#3808=ORIENTED_EDGE ( 'NONE', *, *, #33309, .F. ) ;
#3809=DIRECTION ( 'NONE',  ( 1.000000000000000000, 0.000000000000000000, 0.000000000000000000 ) ) ;
#3810=ORIENTED_EDGE ( 'NONE', *, *, #60185, .T. ) ;
#3816=VERTEX_POINT ( 'NONE', #61807 ) ;
#3819=DIRECTION ( 'NONE',  ( -1.836970198721029934E-16, 1.836970198721036590E-16, -1.000000000000000000 ) ) ;
#3822=ORIENTED_EDGE ( 'NONE', *, *, #33697, .F. ) ;
#3827=DIRECTION ( 'NONE',  ( -6.308085367188448025E-15, -1.000000000000000000, 0.000000000000000000 ) ) ;
#3831=CIRCLE ( 'NONE', #62561, 0.1749999999999998224 ) ;
#3836=ADVANCED_FACE ( 'NONE', ( #25030 ), #55801, .F. ) ;
#3854=FACE_OUTER_BOUND ( 'NONE', #20620, .T. ) ;
#3856=AXIS2_PLACEMENT_3D ( 'NONE', #8936, #4363, #25925 ) ;
#3858=DIRECTION ( 'NONE',  ( 0.5000000000000019984, 0.8660254037844375974, 3.181725716174716554E-16 ) ) ;
#3870=DIRECTION ( 'NONE',  ( 1.836970198721029934E-16, 1.836970198721010706E-16, -1.000000000000000000 ) ) ;
#3871=LINE ( 'NONE', #9172, #18647 ) ;
#3882=VECTOR ( 'NONE', #20490, 1000.000000000000000 ) ;
#3893=CARTESIAN_POINT ( 'NONE',  ( -8.821682069070746479, -2.369523737882742953, 54.00000000000000711 ) ) ;
#3902=VECTOR ( 'NONE', #59045, 1000.000000000000114 ) ;
#3910=DIRECTION ( 'NONE',  ( -0.000000000000000000, 3.673940397442059868E-16, -1.000000000000000000 ) ) ;
#3916=LINE ( 'NONE', #56252, #46988 ) ;
#3920=VERTEX_POINT ( 'NONE', #4519 ) ;
#3934=CARTESIAN_POINT ( 'NONE',  ( 8.580623737882818958, -8.930623737882855906, 54.00000000000000711 ) ) ;
#3937=VERTEX_POINT ( 'NONE', #58951 ) ;
#3940=DIRECTION ( 'NONE',  ( -1.836970198721029934E-16, 1.836970198721036344E-16, -1.000000000000000000 ) ) ;
#3942=CARTESIAN_POINT ( 'NONE',  ( 3.677663764522608680, 6.350872789121272177, 54.00000000000000711 ) ) ;
#3955=DIRECTION ( 'NONE',  ( -0.000000000000000000, -0.000000000000000000, -1.000000000000000000 ) ) ;
#3969=EDGE_CURVE ( 'NONE', #45427, #20102, #661, .T. ) ;
#3971=CARTESIAN_POINT ( 'NONE',  ( 3.677663764522614454, -6.364920264886869461, 26.00000000000000711 ) ) ;
#3975=ADVANCED_FACE ( 'NONE', ( #5219 ), #62855, .F. ) ;
#3981=CARTESIAN_POINT ( 'NONE',  ( 10.50702373788281996, -3.664523737882826815, 54.00000000000000711 ) ) ;
#3988=AXIS2_PLACEMENT_3D ( 'NONE', #46868, #15060, #9403 ) ;
#3999=ORIENTED_EDGE ( 'NONE', *, *, #113, .F. ) ;
#4017=ORIENTED_EDGE ( 'NONE', *, *, #46102, .T. ) ;
#4021=VERTEX_POINT ( 'NONE', #55049 ) ;
#4027=ORIENTED_EDGE ( 'NONE', *, *, #21227, .F. ) ;
#4029=LINE ( 'NONE', #68732, #45374 ) ;
#4032=AXIS2_PLACEMENT_3D ( 'NONE', #35572, #34866, #7999 ) ;
#4049=DIRECTION ( 'NONE',  ( -0.000000000000000000, -0.000000000000000000, -1.000000000000000000 ) ) ;
#4052=VECTOR ( 'NONE', #40336, 1000.000000000000000 ) ;
#4053=DIRECTION ( 'NONE',  ( 1.349135440953254805E-14, 1.000000000000000000, 1.836970198721035604E-16 ) ) ;
#4054=ORIENTED_EDGE ( 'NONE', *, *, #59982, .F. ) ;
#4060=DIRECTION ( 'NONE',  ( -1.000000000000000000, 0.000000000000000000, 0.000000000000000000 ) ) ;
#4061=ORIENTED_EDGE ( 'NONE', *, *, #8787, .T. ) ;
#4063=CARTESIAN_POINT ( 'NONE',  ( -4.706725378239217328, 4.141586236041038482, 54.00000000000000711 ) ) ;
#4064=FACE_OUTER_BOUND ( 'NONE', #10426, .T. ) ;
#4067=EDGE_CURVE ( 'NONE', #34255, #28070, #959, .T. ) ;
#4072=CARTESIAN_POINT ( 'NONE',  ( 6.657023737882818537, -10.31452373788281207, 26.00000000000000000 ) ) ;
#4075=CARTESIAN_POINT ( 'NONE',  ( -9.689726262117330791, -10.05377373788272699, 54.00000000000000711 ) ) ;
#4081=DIRECTION ( 'NONE',  ( -1.000000000000000000, 2.135044278125299371E-15, 0.000000000000000000 ) ) ;
#4084=AXIS2_PLACEMENT_3D ( 'NONE', #63865, #32040, #64221 ) ;
#4086=LINE ( 'NONE', #69475, #8152 ) ;
#4091=ORIENTED_EDGE ( 'NONE', *, *, #8062, .F. ) ;
#4114=CARTESIAN_POINT ( 'NONE',  ( 7.408280051175172076, -3.724485858128701032, 54.00000000000000711 ) ) ;
#4127=LINE ( 'NONE', #63523, #65216 ) ;
#4139=VERTEX_POINT ( 'NONE', #59647 ) ;
#4146=CARTESIAN_POINT ( 'NONE',  ( 6.364920264886889001, 6.822336235477383326, 54.00000000000000711 ) ) ;
#4147=CARTESIAN_POINT ( 'NONE',  ( 8.093267424590459669, 8.697938382363064491, 54.00000000000000711 ) ) ;
#4151=EDGE_LOOP ( 'NONE', ( #36352, #18853, #17435, #38167 ) ) ;
#4173=ORIENTED_EDGE ( 'NONE', *, *, #12908, .F. ) ;
#4175=CARTESIAN_POINT ( 'NONE',  ( 8.930623737882818602, -10.05377373788281581, 26.00000000000000000 ) ) ;
#4176=VERTEX_POINT ( 'NONE', #60677 ) ;
#4178=LINE ( 'NONE', #68161, #40656 ) ;
#4179=CARTESIAN_POINT ( 'NONE',  ( 6.836383711243002814, 6.350872789121261519, 54.00000000000000711 ) ) ;
#4187=ORIENTED_EDGE ( 'NONE', *, *, #26534, .T. ) ;
#4192=AXIS2_PLACEMENT_3D ( 'NONE', #10203, #26469, #15522 ) ;
#4198=AXIS2_PLACEMENT_3D ( 'NONE', #48291, #2779, #42275 ) ;
#4206=CIRCLE ( 'NONE', #39156, 0.1749999999999998224 ) ;
#4209=EDGE_CURVE ( 'NONE', #1245, #64281, #39787, .T. ) ;
#4228=ORIENTED_EDGE ( 'NONE', *, *, #3174, .F. ) ;
#4247=AXIS2_PLACEMENT_3D ( 'NONE', #9068, #14725, #36288 ) ;
#4252=ORIENTED_EDGE ( 'NONE', *, *, #52302, .F. ) ;
#4260=CIRCLE ( 'NONE', #26870, 1.224999999999999423 ) ;
#4262=ADVANCED_FACE ( 'NONE', ( #50063 ), #34482, .F. ) ;
#4267=ORIENTED_EDGE ( 'NONE', *, *, #22951, .F. ) ;
#4270=PLANE ( 'NONE',  #19155 ) ;
#4278=CARTESIAN_POINT ( 'NONE',  ( 7.357023737882806280, 6.651770455163672935, 54.00000000000000711 ) ) ;
#4288=DIRECTION ( 'NONE',  ( 0.000000000000000000, 0.000000000000000000, 1.000000000000000000 ) ) ;
#4289=EDGE_CURVE ( 'NONE', #40726, #9110, #66161, .T. ) ;
#4310=LINE ( 'NONE', #26555, #1788 ) ;
#4313=VECTOR ( 'NONE', #16390, 1000.000000000000000 ) ;
#4331=CARTESIAN_POINT ( 'NONE',  ( 7.186223737882818874, -5.257023737882825287, 54.00000000000000711 ) ) ;
#4337=LINE ( 'NONE', #63015, #43358 ) ;
#4342=EDGE_CURVE ( 'NONE', #2487, #56322, #32261, .T. ) ;
#4344=DIRECTION ( 'NONE',  ( -0.000000000000000000, 3.673940397442059868E-16, -1.000000000000000000 ) ) ;
#4350=CARTESIAN_POINT ( 'NONE',  ( 2.544523737882809833, 8.821682069070735821, 26.00000000000000711 ) ) ;
#4351=ORIENTED_EDGE ( 'NONE', *, *, #68525, .F. ) ;
#4358=DIRECTION ( 'NONE',  ( -1.000000000000000000, 1.079558018506126625E-14, 1.836970198721049656E-16 ) ) ;
#4363=DIRECTION ( 'NONE',  ( -0.6414496315691446959, 0.7671651518153106419, 2.818519042764040589E-16 ) ) ;
#4368=EDGE_CURVE ( 'NONE', #45380, #47595, #64444, .T. ) ;
#4379=DIRECTION ( 'NONE',  ( 8.359604446858500663E-15, 1.000000000000000000, 0.000000000000000000 ) ) ;
#4380=ORIENTED_EDGE ( 'NONE', *, *, #15369, .F. ) ;
#4383=ORIENTED_EDGE ( 'NONE', *, *, #69682, .F. ) ;
#4391=DIRECTION ( 'NONE',  ( 3.540251991789405856E-15, 1.000000000000000000, 0.000000000000000000 ) ) ;
#4394=EDGE_LOOP ( 'NONE', ( #30886, #32218, #19485, #18906 ) ) ;
#4397=LINE ( 'NONE', #25959, #48691 ) ;
#4403=VECTOR ( 'NONE', #56674, 1000.000000000000000 ) ;
#4408=CIRCLE ( 'NONE', #43899, 0.5249999999999994671 ) ;
#4410=VERTEX_POINT ( 'NONE', #55215 ) ;
#4413=CYLINDRICAL_SURFACE ( 'NONE', #35571, 0.1749999999999998224 ) ;
#4416=CARTESIAN_POINT ( 'NONE',  ( -7.342976262117277386, -5.552858015815541393, 26.00000000000000711 ) ) ;
#4417=ORIENTED_EDGE ( 'NONE', *, *, #41119, .T. ) ;
#4425=ORIENTED_EDGE ( 'NONE', *, *, #29502, .F. ) ;
#4430=CARTESIAN_POINT ( 'NONE',  ( -7.447976262117260049, 9.880476262117177555, 25.99999580000000421 ) ) ;
#4437=ORIENTED_EDGE ( 'NONE', *, *, #14219, .F. ) ;
#4445=ORIENTED_EDGE ( 'NONE', *, *, #57166, .F. ) ;
#4447=FACE_OUTER_BOUND ( 'NONE', #40394, .T. ) ;
#4451=VERTEX_POINT ( 'NONE', #60847 ) ;
#4454=CIRCLE ( 'NONE', #43950, 0.1749999999999993783 ) ;
#4457=VERTEX_POINT ( 'NONE', #11379 ) ;
#4458=ORIENTED_EDGE ( 'NONE', *, *, #6978, .T. ) ;
#4459=ORIENTED_EDGE ( 'NONE', *, *, #60331, .T. ) ;
#4469=EDGE_CURVE ( 'NONE', #40228, #12566, #49898, .T. ) ;
#4479=CARTESIAN_POINT ( 'NONE',  ( 9.703773737882785966, -8.580623737882845603, 26.00000000000000000 ) ) ;
#4480=DIRECTION ( 'NONE',  ( 1.214636490590110272E-14, 1.000000000000000000, 1.836970198721032892E-16 ) ) ;
#4500=LINE ( 'NONE', #64247, #9176 ) ;
#4501=CARTESIAN_POINT ( 'NONE',  ( 6.832023737882812142, 9.722976262117196455, 26.00000000000000711 ) ) ;
#4505=EDGE_CURVE ( 'NONE', #42529, #26273, #49278, .T. ) ;
#4514=VERTEX_POINT ( 'NONE', #1808 ) ;
#4516=VECTOR ( 'NONE', #8405, 1000.000000000000000 ) ;
#4519=CARTESIAN_POINT ( 'NONE',  ( 1.480523737882813773, 8.598420958951637161, 54.00000000000000711 ) ) ;
#4535=EDGE_LOOP ( 'NONE', ( #30832, #55391, #69238, #23107 ) ) ;
#4538=AXIS2_PLACEMENT_3D ( 'NONE', #47300, #30337, #58615 ) ;
#4540=ORIENTED_EDGE ( 'NONE', *, *, #43052, .F. ) ;
#4560=PLANE ( 'NONE',  #67257 ) ;
#4571=LINE ( 'NONE', #20815, #49963 ) ;
#4574=FACE_OUTER_BOUND ( 'NONE', #14499, .T. ) ;
#4582=DIRECTION ( 'NONE',  ( 1.671920889371702854E-15, 1.000000000000000000, -0.000000000000000000 ) ) ;
#4584=DIRECTION ( 'NONE',  ( -0.7071067811865401342, 0.7071067811865550112, 0.000000000000000000 ) ) ;
#4586=ORIENTED_EDGE ( 'NONE', *, *, #9742, .F. ) ;
#4592=EDGE_CURVE ( 'NONE', #6741, #68576, #3916, .T. ) ;
#4602=VECTOR ( 'NONE', #1948, 1000.000000000000000 ) ;
#4615=DIRECTION ( 'NONE',  ( -0.000000000000000000, -0.000000000000000000, -1.000000000000000000 ) ) ;
#4620=AXIS2_PLACEMENT_3D ( 'NONE', #20904, #15260, #31532 ) ;
#4621=CARTESIAN_POINT ( 'NONE',  ( -1.466476262117315743, -8.612468434717266419, 54.00000000000000711 ) ) ;
#4624=DIRECTION ( 'NONE',  ( 1.047444401652940007E-14, 1.000000000000000000, 1.836970198721029934E-16 ) ) ;
#4630=EDGE_LOOP ( 'NONE', ( #37370, #41116, #18560, #21222 ) ) ;
#4631=CARTESIAN_POINT ( 'NONE',  ( -10.30047626211724854, -3.664523737882715348, 54.00000000000000711 ) ) ;
#4632=DIRECTION ( 'NONE',  ( -0.000000000000000000, 1.000000000000000000, 3.673940397442059868E-16 ) ) ;
#4634=ORIENTED_EDGE ( 'NONE', *, *, #67184, .F. ) ;
#4636=DIRECTION ( 'NONE',  ( -3.596772705736696467E-15, -1.000000000000000000, 0.000000000000000000 ) ) ;
#4642=EDGE_LOOP ( 'NONE', ( #34547, #10846, #39368, #15040 ) ) ;
#4644=ORIENTED_EDGE ( 'NONE', *, *, #59158, .T. ) ;
#4647=EDGE_CURVE ( 'NONE', #55229, #2503, #3212, .T. ) ;
#4668=ADVANCED_FACE ( 'NONE', ( #41385 ), #8497, .F. ) ;
#4672=FACE_OUTER_BOUND ( 'NONE', #26852, .T. ) ;
#4677=ORIENTED_EDGE ( 'NONE', *, *, #2803, .F. ) ;
#4678=CARTESIAN_POINT ( 'NONE',  ( 5.257023737882801306, 5.242976262117200470, 54.00000000000000711 ) ) ;
#4685=AXIS2_PLACEMENT_3D ( 'NONE', #22389, #43935, #26996 ) ;
#4694=LINE ( 'NONE', #10348, #27765 ) ;
#4703=CLOSED_SHELL ( 'NONE', ( #20308, #65639, #64798, #26382, #9854, #18775, #21464, #38650, #4716, #57354, #54283, #67592, #35845, #61503, #54406, #44138, #27674, #13355, #14310, #34419, #13084, #15592, #46934, #3714, #39287, #11540, #38173, #12032, #41110, #21331, #54486, #19255, #25332, #52895, #30048, #34138, #2962, #60131, #28061, #30259, #53163, #52738, #2720, #30835, #6018, #25811, #53129, #53605, #34182, #35937, #34718, #52715, #58899, #29466, #13092, #16229, #20845, #44403, #41047, #18547, #7696, #38697, #59078, #42656, #17326, #4668, #7008, #38456, #9606, #42053, #61641, #34318, #37496, #4885, #2147, #49045, #22612, #33529, #25573, #18239, #32648, #11650, #57656, #5990, #57754, #22181, #18528, #34974, #27088, #40558, #6020, #58643, #33616, #56199, #20299, #48962, #61149, #14398, #17255, #18056, #45916, #42003, #15549, #10302, #63149, #44759, #16878, #18378, #43352, #21694, #8541, #20803, #24053, #5824, #9061, #21598, #35516, #6532, #43809, #60116, #10289, #40766, #18997, #24847, #57740, #38749, #16246, #57953, #52234, #65532, #54487, #66366, #46087, #4893, #58789, #38045, #48376, #28018, #11634, #66283, #39949, #4262, #1172, #37696, #19824, #13134, #27443, #46343, #58381, #56610, #2975, #20018, #15681, #51896, #58704, #9561, #17767, #56690, #31585, #29212, #14165, #64611, #65052, #32106, #43563, #9934, #36157, #25821, #37627, #51488, #40469, #66826, #67308, #67343, #781, #11818, #14286, #1610, #15682, #37697, #12251, #67143, #25009, #50472, #53107, #43187, #61462, #38732, #3975, #23647, #25237, #11603, #7418, #57512, #66134, #13854, #57813, #38489, #8528, #36599, #46493, #53745, #64787, #11015, #2163, #21199, #25469, #29789, #19410, #14131, #13902, #15032, #13283, #65833, #63423, #30521, #24311, #48612, #68333, #24232, #24553, #19651, #13345, #48030, #44865, #65573, #33474, #48810, #54860, #38747, #21190, #60681, #24188, #15937, #33678, #35125, #23353, #42594, #52321, #10770, #25289, #25703, #15797, #22131, #68354, #14266, #56063, #45413, #16745, #36410, #61603, #15477, #59260, #10341, #44804, #579, #46091, #15187, #69014, #12062, #29018, #54202, #6634, #42339, #24757, #61206, #42094, #41568, #59166, #54365, #69966, #55412, #63452, #68829, #62584, #58377, #65496, #52630, #23520, #63665, #27033, #44617, #18563, #37896, #16795, #43108, #50168, #13740, #19522, #36734, #62030, #39816, #1885, #46789, #46958, #59632, #12521, #9735, #23160, #48327, #22984, #63474, #1109, #53624, #43459, #21657, #21338, #64692, #68870, #26681, #40159, #3697, #59585, #67817, #629, #19003, #48432, #48190, #17460, #67423, #66077, #64302, #43219, #21270, #33232, #39056, #43771, #19221, #69317, #47988, #68793, #62559, #3836, #20198, #35398, #63639, #59649, #63919, #36195, #64771, #11572, #14922, #29286, #39300, #22928, #35011, #44912, #28047, #55261, #20836, #63060, #64772, #28762, #11655, #23836, #54150, #29293, #59739, #39559, #34529, #21224, #39189, #2242, #1154, #20543, #56673, #40318, #13496, #12513, #39781, #54422, #27965 ) ) ;
#4704=CYLINDRICAL_SURFACE ( 'NONE', #20905, 0.5250000000000004663 ) ;
#4707=LINE ( 'NONE', #15668, #19584 ) ;
#4708=ORIENTED_EDGE ( 'NONE', *, *, #62170, .F. ) ;
#4709=ORIENTED_EDGE ( 'NONE', *, *, #43609, .T. ) ;
#4710=ORIENTED_EDGE ( 'NONE', *, *, #42, .T. ) ;
#4716=ADVANCED_FACE ( 'NONE', ( #61902 ), #46684, .F. ) ;
#4731=FACE_OUTER_BOUND ( 'NONE', #65903, .T. ) ;
#4736=EDGE_CURVE ( 'NONE', #37577, #67274, #35559, .T. ) ;
#4743=EDGE_CURVE ( 'NONE', #7648, #10709, #63311, .T. ) ;
#4758=ORIENTED_EDGE ( 'NONE', *, *, #22470, .T. ) ;
#4763=CARTESIAN_POINT ( 'NONE',  ( 9.912023737882815766, -3.857023737882825820, 54.00000000000000711 ) ) ;
#4774=ORIENTED_EDGE ( 'NONE', *, *, #40768, .T. ) ;
#4775=EDGE_CURVE ( 'NONE', #1435, #52904, #52720, .T. ) ;
#4778=DIRECTION ( 'NONE',  ( -0.000000000000000000, 3.673940397442059868E-16, -1.000000000000000000 ) ) ;
#4780=CARTESIAN_POINT ( 'NONE',  ( -9.547976262117254365, 2.355476262117183417, 54.00000000000000711 ) ) ;
#4783=ORIENTED_EDGE ( 'NONE', *, *, #13263, .T. ) ;
#4791=ORIENTED_EDGE ( 'NONE', *, *, #9033, .F. ) ;
#4809=EDGE_CURVE ( 'NONE', #14583, #45832, #8, .T. ) ;
#4810=ORIENTED_EDGE ( 'NONE', *, *, #67802, .T. ) ;
#4812=EDGE_CURVE ( 'NONE', #44524, #27495, #16307, .T. ) ;
#4823=DIRECTION ( 'NONE',  ( -1.000000000000000000, 7.304098846218132892E-15, -0.000000000000000000 ) ) ;
#4826=VECTOR ( 'NONE', #4840, 1000.000000000000000 ) ;
#4835=VERTEX_POINT ( 'NONE', #6679 ) ;
#4839=CARTESIAN_POINT ( 'NONE',  ( 6.836383711243005479, -6.364920264886905876, 54.00000000000000711 ) ) ;
#4840=DIRECTION ( 'NONE',  ( -0.000000000000000000, -0.000000000000000000, -1.000000000000000000 ) ) ;
#4841=ORIENTED_EDGE ( 'NONE', *, *, #4935, .T. ) ;
#4844=CARTESIAN_POINT ( 'NONE',  ( -4.135079735113167843, 6.822336235477362010, 54.00000000000000711 ) ) ;
#4850=AXIS2_PLACEMENT_3D ( 'NONE', #46496, #68070, #57107 ) ;
#4852=CARTESIAN_POINT ( 'NONE',  ( 8.093267424590459669, 8.697938382363064491, 54.00000000000000711 ) ) ;
#4857=VECTOR ( 'NONE', #40201, 1000.000000000000114 ) ;
#4858=AXIS2_PLACEMENT_3D ( 'NONE', #36671, #21111, #20403 ) ;
#4866=EDGE_LOOP ( 'NONE', ( #2767, #54818, #65620, #28844 ) ) ;
#4869=CARTESIAN_POINT ( 'NONE',  ( -1.466476262117324181, -9.404523737882843903, 54.00000000000000711 ) ) ;
#4880=VERTEX_POINT ( 'NONE', #33892 ) ;
#4882=AXIS2_PLACEMENT_3D ( 'NONE', #40466, #62024, #2998 ) ;
#4883=PLANE ( 'NONE',  #51141 ) ;
#4885=ADVANCED_FACE ( 'NONE', ( #17975 ), #11626, .F. ) ;
#4888=ORIENTED_EDGE ( 'NONE', *, *, #59801, .T. ) ;
#4889=ORIENTED_EDGE ( 'NONE', *, *, #27630, .T. ) ;
#4893=ADVANCED_FACE ( 'NONE', ( #49819 ), #55817, .F. ) ;
#4898=CARTESIAN_POINT ( 'NONE',  ( -10.03972626211731445, -8.930623737882747548, 26.00000000000000000 ) ) ;
#4902=EDGE_CURVE ( 'NONE', #2503, #29317, #50208, .T. ) ;
#4903=CARTESIAN_POINT ( 'NONE',  ( 3.157023737882809655, -6.501044194225470640, 26.00000000000000711 ) ) ;
#4910=AXIS2_PLACEMENT_3D ( 'NONE', #1138, #65827, #17381 ) ;
#4911=CARTESIAN_POINT ( 'NONE',  ( 8.711985858128693749, -2.420780051175180692, 54.00000000000000711 ) ) ;
#4924=CARTESIAN_POINT ( 'NONE',  ( -3.663616288757091333, -4.149127210878728711, 54.00000000000000711 ) ) ;
#4925=CARTESIAN_POINT ( 'NONE',  ( -7.342976262117259623, 5.538810540049946773, 54.00000000000000711 ) ) ;
#4928=CARTESIAN_POINT ( 'NONE',  ( -0.9414762621172296786, 9.390476262117148920, 54.00000000000000711 ) ) ;
#4935=EDGE_CURVE ( 'NONE', #66583, #42686, #65057, .T. ) ;
#4951=ORIENTED_EDGE ( 'NONE', *, *, #29385, .T. ) ;
#4955=AXIS2_PLACEMENT_3D ( 'NONE', #30477, #56301, #52052 ) ;
#4963=AXIS2_PLACEMENT_3D ( 'NONE', #57244, #51233, #29307 ) ;
#4966=EDGE_LOOP ( 'NONE', ( #35996, #16475, #56923, #27003 ) ) ;
#4973=CARTESIAN_POINT ( 'NONE',  ( 8.711985858128693749, -8.093267424590470327, 54.00000000000000711 ) ) ;
#4976=ORIENTED_EDGE ( 'NONE', *, *, #50896, .F. ) ;
#4981=ORIENTED_EDGE ( 'NONE', *, *, #49669, .T. ) ;
#4985=EDGE_CURVE ( 'NONE', #68576, #22889, #32872, .T. ) ;
#4991=CARTESIAN_POINT ( 'NONE',  ( 6.849523737882814878, 10.49297626211720136, 26.00000000000000711 ) ) ;
#4994=CARTESIAN_POINT ( 'NONE',  ( -2.530476262117318242, -8.835729544836354421, 54.00000000000000711 ) ) ;
#4997=VERTEX_POINT ( 'NONE', #29988 ) ;
#5001=ORIENTED_EDGE ( 'NONE', *, *, #32110, .F. ) ;
#5004=VECTOR ( 'NONE', #13984, 1000.000000000000000 ) ;
#5007=VECTOR ( 'NONE', #66146, 1000.000000000000000 ) ;
#5008=VECTOR ( 'NONE', #42909, 1000.000000000000000 ) ;
#5010=CARTESIAN_POINT ( 'NONE',  ( 3.677663764522616230, 4.135079735113117216, 26.00000000000000711 ) ) ;
#5012=ORIENTED_EDGE ( 'NONE', *, *, #53945, .F. ) ;
#5015=CARTESIAN_POINT ( 'NONE',  ( 6.836383711243005479, -4.149127210878743810, 54.00000000000000711 ) ) ;
#5019=CARTESIAN_POINT ( 'NONE',  ( -1.620245201994373829, -8.241237374594328813, 54.00000000000000711 ) ) ;
#5021=ORIENTED_EDGE ( 'NONE', *, *, #14964, .F. ) ;
#5023=FACE_OUTER_BOUND ( 'NONE', #56683, .T. ) ;
#5027=CARTESIAN_POINT ( 'NONE',  ( 9.404523737882819034, -0.9555237378828257411, 54.00000000000000711 ) ) ;
#5028=ORIENTED_EDGE ( 'NONE', *, *, #18459, .T. ) ;
#5030=DIRECTION ( 'NONE',  ( 1.000000000000000000, -5.120954910632640039E-15, 0.000000000000000000 ) ) ;
#5032=ORIENTED_EDGE ( 'NONE', *, *, #13681, .T. ) ;
#5037=DIRECTION ( 'NONE',  ( 0.6414496315691617934, 0.7671651518152962090, -0.000000000000000000 ) ) ;
#5059=FACE_OUTER_BOUND ( 'NONE', #19519, .T. ) ;
#5075=VECTOR ( 'NONE', #48095, 1000.000000000000000 ) ;
#5079=EDGE_CURVE ( 'NONE', #4997, #14602, #29272, .T. ) ;
#5086=CARTESIAN_POINT ( 'NONE',  ( -5.242976262117259978, 7.172176262117182510, 54.00000000000000711 ) ) ;
#5112=DIRECTION ( 'NONE',  ( -0.000000000000000000, -0.000000000000000000, 1.000000000000000000 ) ) ;
#5115=DIRECTION ( 'NONE',  ( 1.000000000000000000, 0.000000000000000000, 0.000000000000000000 ) ) ;
#5125=ORIENTED_EDGE ( 'NONE', *, *, #545, .F. ) ;
#5131=EDGE_CURVE ( 'NONE', #11718, #36648, #8406, .T. ) ;
#5147=AXIS2_PLACEMENT_3D ( 'NONE', #25098, #9185, #30754 ) ;
#5163=DIRECTION ( 'NONE',  ( -0.7071067811865401342, 0.7071067811865550112, 1.355854680848613865E-30 ) ) ;
#5164=VECTOR ( 'NONE', #42360, 1000.000000000000000 ) ;
#5168=DIRECTION ( 'NONE',  ( -1.836970198721029934E-16, 1.836970198721036590E-16, -1.000000000000000000 ) ) ;
#5174=VERTEX_POINT ( 'NONE', #42000 ) ;
#5175=VECTOR ( 'NONE', #10642, 1000.000000000000114 ) ;
#5178=CARTESIAN_POINT ( 'NONE',  ( -6.486996718459899114, -2.632023737882779102, 26.00000000000000711 ) ) ;
#5188=DIRECTION ( 'NONE',  ( 0.6414496315691617934, -0.7671651518152962090, 0.000000000000000000 ) ) ;
#5197=LINE ( 'NONE', #69887, #14051 ) ;
#5200=LINE ( 'NONE', #14757, #60996 ) ;
#5208=LINE ( 'NONE', #32073, #40187 ) ;
#5212=CIRCLE ( 'NONE', #15353, 0.1749999999999993783 ) ;
#5216=EDGE_CURVE ( 'NONE', #44788, #27591, #43041, .T. ) ;
#5219=FACE_OUTER_BOUND ( 'NONE', #19050, .T. ) ;
#5220=ORIENTED_EDGE ( 'NONE', *, *, #55453, .F. ) ;
#5222=ORIENTED_EDGE ( 'NONE', *, *, #36754, .F. ) ;
#5228=VECTOR ( 'NONE', #34028, 1000.000000000000000 ) ;
#5231=VECTOR ( 'NONE', #54743, 1000.000000000000000 ) ;
#5232=DIRECTION ( 'NONE',  ( 0.8660254037844363761, -0.5000000000000038858, -1.836970198721044232E-16 ) ) ;
#5243=CARTESIAN_POINT ( 'NONE',  ( 9.703773737882785966, -8.580623737882845603, 26.00000000000000000 ) ) ;
#5254=EDGE_CURVE ( 'NONE', #56335, #48411, #42349, .T. ) ;
#5259=CARTESIAN_POINT ( 'NONE',  ( -3.667976262117227382, 9.897976262117168744, 26.00000000000000711 ) ) ;
#5260=LINE ( 'NONE', #5936, #45963 ) ;
#5265=AXIS2_PLACEMENT_3D ( 'NONE', #7134, #56633, #34010 ) ;
#5267=FACE_OUTER_BOUND ( 'NONE', #44755, .T. ) ;
#5272=ORIENTED_EDGE ( 'NONE', *, *, #23632, .F. ) ;
#5277=ORIENTED_EDGE ( 'NONE', *, *, #35378, .T. ) ;
#5287=VERTEX_POINT ( 'NONE', #66345 ) ;
#5301=DIRECTION ( 'NONE',  ( 0.000000000000000000, -3.673940397442059868E-16, 1.000000000000000000 ) ) ;
#5305=CARTESIAN_POINT ( 'NONE',  ( 3.848229544836323512, -7.357023737882802727, 26.00000000000000000 ) ) ;
#5306=VECTOR ( 'NONE', #7057, 1000.000000000000000 ) ;
#5315=ORIENTED_EDGE ( 'NONE', *, *, #43942, .T. ) ;
#5323=ORIENTED_EDGE ( 'NONE', *, *, #54468, .F. ) ;
#5325=VECTOR ( 'NONE', #35946, 1000.000000000000000 ) ;
#5329=ORIENTED_EDGE ( 'NONE', *, *, #32771, .T. ) ;
#5333=ORIENTED_EDGE ( 'NONE', *, *, #49358, .F. ) ;
#5335=CYLINDRICAL_SURFACE ( 'NONE', #54761, 0.5249999999999999112 ) ;
#5337=LINE ( 'NONE', #68267, #22540 ) ;
#5343=CARTESIAN_POINT ( 'NONE',  ( 5.257023737882795977, 5.242976262117205799, 26.00000000000000711 ) ) ;
#5355=ORIENTED_EDGE ( 'NONE', *, *, #58982, .T. ) ;
#5365=ORIENTED_EDGE ( 'NONE', *, *, #13341, .T. ) ;
#5377=VECTOR ( 'NONE', #45181, 1000.000000000000000 ) ;
#5379=DIRECTION ( 'NONE',  ( 0.7071067811865401342, -0.7071067811865550112, -1.355854680848614216E-30 ) ) ;
#5385=EDGE_CURVE ( 'NONE', #47516, #1435, #54360, .T. ) ;
#5386=ORIENTED_EDGE ( 'NONE', *, *, #29409, .T. ) ;
#5387=DIRECTION ( 'NONE',  ( -0.000000000000000000, 3.673940397442059868E-16, -1.000000000000000000 ) ) ;
#5399=LINE ( 'NONE', #31911, #63404 ) ;
#5401=ORIENTED_EDGE ( 'NONE', *, *, #47197, .F. ) ;
#5413=ORIENTED_EDGE ( 'NONE', *, *, #53447, .T. ) ;
#5414=ORIENTED_EDGE ( 'NONE', *, *, #31507, .F. ) ;
#5417=DIRECTION ( 'NONE',  ( -8.728482790395504563E-15, -1.000000000000000000, 0.000000000000000000 ) ) ;
#5421=CIRCLE ( 'NONE', #9902, 0.5250000000000003553 ) ;
#5438=DIRECTION ( 'NONE',  ( -1.000000000000000000, 0.000000000000000000, 0.000000000000000000 ) ) ;
#5440=ORIENTED_EDGE ( 'NONE', *, *, #12061, .F. ) ;
#5449=LINE ( 'NONE', #69079, #46281 ) ;
#5451=LINE ( 'NONE', #16744, #54115 ) ;
#5453=DIRECTION ( 'NONE',  ( 1.836970198721029934E-16, -1.836970198721036344E-16, 1.000000000000000000 ) ) ;
#5457=DIRECTION ( 'NONE',  ( 0.7071067811865514585, 0.7071067811865435759, -0.000000000000000000 ) ) ;
#5460=CARTESIAN_POINT ( 'NONE',  ( 6.789561617636934443, 7.394232575409549035, 54.00000000000000711 ) ) ;
#5465=LINE ( 'NONE', #53548, #69332 ) ;
#5485=DIRECTION ( 'NONE',  ( -1.836970198721029934E-16, 1.836970198721036344E-16, -1.000000000000000000 ) ) ;
#5491=ORIENTED_EDGE ( 'NONE', *, *, #55035, .T. ) ;
#5493=LINE ( 'NONE', #27045, #32102 ) ;
#5495=CARTESIAN_POINT ( 'NONE',  ( 9.404523737882753309, 0.9414762621171547385, 54.00000000000000711 ) ) ;
#5502=VERTEX_POINT ( 'NONE', #34498 ) ;
#5507=PLANE ( 'NONE',  #44699 ) ;
#5511=AXIS2_PLACEMENT_3D ( 'NONE', #11833, #12185, #39747 ) ;
#5514=ORIENTED_EDGE ( 'NONE', *, *, #19273, .F. ) ;
#5517=CYLINDRICAL_SURFACE ( 'NONE', #48092, 0.1749999999999980738 ) ;
#5519=ORIENTED_EDGE ( 'NONE', *, *, #6978, .F. ) ;
#5520=LINE ( 'NONE', #20381, #27914 ) ;
#5524=EDGE_CURVE ( 'NONE', #23882, #51221, #24253, .T. ) ;
#5525=CARTESIAN_POINT ( 'NONE',  ( 4.149127210878726935, -6.836383711243002814, 54.00000000000000711 ) ) ;
#5528=DIRECTION ( 'NONE',  ( -0.7071067811865527908, -0.7071067811865422437, 0.000000000000000000 ) ) ;
#5529=LINE ( 'NONE', #25714, #23245 ) ;
#5537=CYLINDRICAL_SURFACE ( 'NONE', #7290, 1.224999999999999423 ) ;
#5558=EDGE_LOOP ( 'NONE', ( #13980, #4677, #40424, #49067 ) ) ;
#5563=CARTESIAN_POINT ( 'NONE',  ( -6.822336235477489019, -6.364920264886855250, 54.00000000000000711 ) ) ;
#5565=CIRCLE ( 'NONE', #45054, 0.1749999999999998224 ) ;
#5576=ORIENTED_EDGE ( 'NONE', *, *, #16015, .T. ) ;
#5584=EDGE_LOOP ( 'NONE', ( #58968, #62665, #21953, #68941 ) ) ;
#5588=EDGE_CURVE ( 'NONE', #1729, #64431, #9753, .T. ) ;
#5595=CARTESIAN_POINT ( 'NONE',  ( 9.737023737882816832, -6.832023737882813919, 26.00000000000000000 ) ) ;
#5601=LINE ( 'NONE', #6964, #13650 ) ;
#5607=CIRCLE ( 'NONE', #23649, 0.3499999999999996447 ) ;
#5609=CARTESIAN_POINT ( 'NONE',  ( 9.562023737882801910, 8.130476262117189989, 26.00000000000000711 ) ) ;
#5613=LINE ( 'NONE', #27182, #20863 ) ;
#5614=AXIS2_PLACEMENT_3D ( 'NONE', #13253, #51439, #18916 ) ;
#5619=CARTESIAN_POINT ( 'NONE',  ( 7.186223737882794893, 5.242976262117198694, 26.00000000000000711 ) ) ;
#5622=DIRECTION ( 'NONE',  ( 0.000000000000000000, -3.673940397442059868E-16, 1.000000000000000000 ) ) ;
#5625=DIRECTION ( 'NONE',  ( -0.000000000000000000, -0.000000000000000000, -1.000000000000000000 ) ) ;
#5640=CARTESIAN_POINT ( 'NONE',  ( -2.355476262117229158, 9.547976262117156665, 54.00000000000000711 ) ) ;
#5643=LINE ( 'NONE', #32855, #60398 ) ;
#5644=DIRECTION ( 'NONE',  ( 1.836970198721029934E-16, 1.836970198721010706E-16, -1.000000000000000000 ) ) ;
#5659=ORIENTED_EDGE ( 'NONE', *, *, #37991, .T. ) ;
#5663=DIRECTION ( 'NONE',  ( 0.000000000000000000, -1.000000000000000000, 0.000000000000000000 ) ) ;
#5666=CARTESIAN_POINT ( 'NONE',  ( -6.486996718459913325, -3.157023737882783454, 54.00000000000000711 ) ) ;
#5669=CIRCLE ( 'NONE', #59809, 0.5249999999999990230 ) ;
#5685=EDGE_CURVE ( 'NONE', #36105, #19358, #59920, .T. ) ;
#5687=AXIS2_PLACEMENT_3D ( 'NONE', #13387, #7723, #46261 ) ;
#5688=DIRECTION ( 'NONE',  ( -1.000000000000000000, 0.000000000000000000, 0.000000000000000000 ) ) ;
#5689=CARTESIAN_POINT ( 'NONE',  ( -7.290476262117262962, 9.722976262117180468, 26.00000000000000711 ) ) ;
#5692=ORIENTED_EDGE ( 'NONE', *, *, #41564, .T. ) ;
#5710=ORIENTED_EDGE ( 'NONE', *, *, #50109, .T. ) ;
#5714=VERTEX_POINT ( 'NONE', #33047 ) ;
#5718=VECTOR ( 'NONE', #54758, 1000.000000000000000 ) ;
#5720=DIRECTION ( 'NONE',  ( -4.956352788505168198E-15, -1.000000000000000000, 0.000000000000000000 ) ) ;
#5726=ORIENTED_EDGE ( 'NONE', *, *, #26304, .T. ) ;
#5733=ORIENTED_EDGE ( 'NONE', *, *, #65871, .F. ) ;
#5734=ORIENTED_EDGE ( 'NONE', *, *, #61380, .F. ) ;
#5735=LINE ( 'NONE', #27302, #2407 ) ;
#5747=VERTEX_POINT ( 'NONE', #60255 ) ;
#5748=CARTESIAN_POINT ( 'NONE',  ( -3.142976262117261221, 4.031976262117183296, 54.00000000000000711 ) ) ;
#5750=VERTEX_POINT ( 'NONE', #6181 ) ;
#5762=CARTESIAN_POINT ( 'NONE',  ( 7.969523737882813208, 8.821682069070710952, 54.00000000000000711 ) ) ;
#5763=CARTESIAN_POINT ( 'NONE',  ( -3.663616288757094885, -6.364920264886888113, 54.00000000000000711 ) ) ;
#5765=VECTOR ( 'NONE', #13266, 1000.000000000000000 ) ;
#5766=VECTOR ( 'NONE', #20420, 1000.000000000000000 ) ;
#5767=ORIENTED_EDGE ( 'NONE', *, *, #22268, .F. ) ;
#5768=CARTESIAN_POINT ( 'NONE',  ( -9.722976262117256852, 7.955476262117183062, 54.00000000000000711 ) ) ;
#5773=CARTESIAN_POINT ( 'NONE',  ( -10.49297626211725998, 9.781776262117173104, 26.00000000000000711 ) ) ;
#5776=EDGE_LOOP ( 'NONE', ( #9566, #50589, #67407, #7637, #8249, #31339, #56998, #65191, #2260, #3034, #22347, #689, #49334, #63412, #65098, #28427, #19783, #45336, #58783, #44411, #12300, #22757, #68331, #40785, #25259, #43881, #17651, #50763, #41714, #57478, #63768, #21621, #31028, #5767, #63161, #958, #10464, #31887, #60563, #52535, #26625, #20816, #35464, #17183, #57949, #42703, #31556, #11568, #27091, #1187, #44095, #33885, #16811, #39956, #59652, #49638 ) ) ;
#5783=CARTESIAN_POINT ( 'NONE',  ( 9.912023737882776686, 3.667976262117155883, 26.00000000000000711 ) ) ;
#5788=LINE ( 'NONE', #53533, #69898 ) ;
#5794=DIRECTION ( 'NONE',  ( 1.836970198721029934E-16, 1.836970198721010706E-16, -1.000000000000000000 ) ) ;
#5797=VERTEX_POINT ( 'NONE', #27401 ) ;
#5800=CARTESIAN_POINT ( 'NONE',  ( -9.689726262117325462, -10.05377373788272166, 26.00000000000000000 ) ) ;
#5814=LINE ( 'NONE', #12137, #1256 ) ;
#5824=ADVANCED_FACE ( 'NONE', ( #67311 ), #66265, .F. ) ;
#5827=LINE ( 'NONE', #49637, #16098 ) ;
#5831=ORIENTED_EDGE ( 'NONE', *, *, #60462, .F. ) ;
#5841=ORIENTED_EDGE ( 'NONE', *, *, #35520, .T. ) ;
#5857=DIRECTION ( 'NONE',  ( -1.836970198721029934E-16, -1.836970198721010706E-16, 1.000000000000000000 ) ) ;
#5860=CARTESIAN_POINT ( 'NONE',  ( 8.580623737882849156, 9.689726262117156708, 54.00000000000000711 ) ) ;
#5862=EDGE_CURVE ( 'NONE', #12110, #46962, #51389, .T. ) ;
#5863=EDGE_CURVE ( 'NONE', #3213, #55218, #9087, .T. ) ;
#5867=CYLINDRICAL_SURFACE ( 'NONE', #53397, 0.5249999999999990230 ) ;
#5869=DIRECTION ( 'NONE',  ( 1.836970198721029934E-16, 1.836970198721010706E-16, -1.000000000000000000 ) ) ;
#5876=CARTESIAN_POINT ( 'NONE',  ( 7.357023737882817827, -6.665817930929303969, 54.00000000000000711 ) ) ;
#5884=DIRECTION ( 'NONE',  ( 1.836970198721029934E-16, -1.836970198721036344E-16, 1.000000000000000000 ) ) ;
#5892=ORIENTED_EDGE ( 'NONE', *, *, #4809, .F. ) ;
#5894=CARTESIAN_POINT ( 'NONE',  ( -10.30047626211725742, 3.650476262117184234, 54.00000000000000711 ) ) ;
#5895=LINE ( 'NONE', #27810, #57111 ) ;
#5903=ORIENTED_EDGE ( 'NONE', *, *, #36705, .F. ) ;
#5907=VECTOR ( 'NONE', #48431, 1000.000000000000000 ) ;
#5908=DIRECTION ( 'NONE',  ( -0.6414496315691645689, -0.7671651518152939886, -2.587583378555115478E-16 ) ) ;
#5909=CYLINDRICAL_SURFACE ( 'NONE', #25997, 0.1749999999999993783 ) ;
#5912=EDGE_LOOP ( 'NONE', ( #35029, #8622, #42111, #22088 ) ) ;
#5919=ORIENTED_EDGE ( 'NONE', *, *, #60476, .F. ) ;
#5922=DIRECTION ( 'NONE',  ( -0.7671651518152895477, 0.6414496315691698980, -2.309356642088442522E-17 ) ) ;
#5928=ORIENTED_EDGE ( 'NONE', *, *, #48994, .F. ) ;
#5932=DIRECTION ( 'NONE',  ( 1.000000000000000000, 0.000000000000000000, 0.000000000000000000 ) ) ;
#5935=ORIENTED_EDGE ( 'NONE', *, *, #64147, .T. ) ;
#5936=CARTESIAN_POINT ( 'NONE',  ( 9.737023737882806174, 7.955476262117184838, 54.00000000000000711 ) ) ;
#5942=CARTESIAN_POINT ( 'NONE',  ( 7.357023737882800951, 6.651770455163678264, 26.00000000000000711 ) ) ;
#5949=VERTEX_POINT ( 'NONE', #29127 ) ;
#5950=CARTESIAN_POINT ( 'NONE',  ( -0.9414762621173295987, -9.929523737882849588, 54.00000000000000711 ) ) ;
#5957=AXIS2_PLACEMENT_3D ( 'NONE', #39023, #55633, #2584 ) ;
#5963=VERTEX_POINT ( 'NONE', #23823 ) ;
#5970=CYLINDRICAL_SURFACE ( 'NONE', #33063, 1.224999999999998757 ) ;
#5972=CARTESIAN_POINT ( 'NONE',  ( 1.634292677759874302, 8.227189898828697778, 54.00000000000000711 ) ) ;
#5973=CARTESIAN_POINT ( 'NONE',  ( 4.961189459950040792, 7.342976262117206332, 26.00000000000000711 ) ) ;
#5978=EDGE_CURVE ( 'NONE', #69370, #62681, #34774, .T. ) ;
#5979=ORIENTED_EDGE ( 'NONE', *, *, #36646, .T. ) ;
#5990=ADVANCED_FACE ( 'NONE', ( #58099 ), #36898, .T. ) ;
#6003=DIRECTION ( 'NONE',  ( -1.000000000000000000, -0.000000000000000000, -0.000000000000000000 ) ) ;
#6017=CARTESIAN_POINT ( 'NONE',  ( -9.689726262117227762, 10.03972626211718300, 54.00000000000000711 ) ) ;
#6018=ADVANCED_FACE ( 'NONE', ( #20263 ), #9313, .F. ) ;
#6020=ADVANCED_FACE ( 'NONE', ( #52098 ), #37243, .F. ) ;
#6032=ORIENTED_EDGE ( 'NONE', *, *, #31995, .T. ) ;
#6040=DIRECTION ( 'NONE',  ( -0.000000000000000000, -0.000000000000000000, -1.000000000000000000 ) ) ;
#6043=EDGE_CURVE ( 'NONE', #15881, #52921, #63763, .T. ) ;
#6044=VERTEX_POINT ( 'NONE', #31592 ) ;
#6061=PRESENTATION_STYLE_ASSIGNMENT (( #59455 ) ) ;
#6064=ORIENTED_EDGE ( 'NONE', *, *, #47521, .F. ) ;
#6070=CARTESIAN_POINT ( 'NONE',  ( 6.665817930929283541, 7.342976262117200115, 26.00000000000000711 ) ) ;
#6074=CARTESIAN_POINT ( 'NONE',  ( 3.857023737882779635, -10.31452373788281029, 54.00000000000000711 ) ) ;
#6085=CARTESIAN_POINT ( 'NONE',  ( -3.667976262117227382, 9.897976262117168744, 54.00000000000000711 ) ) ;
#6099=VECTOR ( 'NONE', #14318, 1000.000000000000000 ) ;
#6101=DIRECTION ( 'NONE',  ( 9.912705577010336396E-15, 1.000000000000000000, 0.000000000000000000 ) ) ;
#6105=CARTESIAN_POINT ( 'NONE',  ( -6.350872789121327244, 6.822336235477381550, 54.00000000000000711 ) ) ;
#6117=CIRCLE ( 'NONE', #4963, 0.5249999999999994671 ) ;
#6123=ORIENTED_EDGE ( 'NONE', *, *, #37747, .F. ) ;
#6124=CARTESIAN_POINT ( 'NONE',  ( 2.544523737882818271, 9.722976262117205337, 54.00000000000000711 ) ) ;
#6125=DIRECTION ( 'NONE',  ( -1.000000000000000000, 1.356437060717834182E-15, 0.000000000000000000 ) ) ;
#6130=EDGE_CURVE ( 'NONE', #37690, #4176, #31932, .T. ) ;
#6134=CARTESIAN_POINT ( 'NONE',  ( 7.357023737882817827, -6.665817930929303969, 54.00000000000000711 ) ) ;
#6138=ORIENTED_EDGE ( 'NONE', *, *, #54075, .T. ) ;
#6141=VECTOR ( 'NONE', #10407, 1000.000000000000000 ) ;
#6145=ORIENTED_EDGE ( 'NONE', *, *, #31772, .F. ) ;
#6155=CIRCLE ( 'NONE', #47945, 0.1749999999999998224 ) ;
#6158=DIRECTION ( 'NONE',  ( -1.000000000000000000, 0.000000000000000000, 0.000000000000000000 ) ) ;
#6163=CYLINDRICAL_SURFACE ( 'NONE', #3680, 0.1749999999999998224 ) ;
#6174=DIRECTION ( 'NONE',  ( -3.304235192336773145E-15, -1.000000000000000000, 0.000000000000000000 ) ) ;
#6181=CARTESIAN_POINT ( 'NONE',  ( 8.930623737882848800, 10.03972626211715635, 54.00000000000000711 ) ) ;
#6183=ORIENTED_EDGE ( 'NONE', *, *, #24675, .T. ) ;
#6185=ORIENTED_EDGE ( 'NONE', *, *, #61813, .F. ) ;
#6189=VERTEX_POINT ( 'NONE', #48539 ) ;
#6190=CARTESIAN_POINT ( 'NONE',  ( -8.566576262117260754, 8.916576262117214213, 26.00000000000000711 ) ) ;
#6201=VECTOR ( 'NONE', #38203, 1000.000000000000000 ) ;
#6203=DIRECTION ( 'NONE',  ( -3.491481338843133355E-15, -1.000000000000000000, -1.836970198721029934E-16 ) ) ;
#6204=DIRECTION ( 'NONE',  ( -0.7671651518153006499, 0.6414496315691565753, 0.000000000000000000 ) ) ;
#6220=ORIENTED_EDGE ( 'NONE', *, *, #8069, .F. ) ;
#6221=DIRECTION ( 'NONE',  ( -0.000000000000000000, 3.673940397442059868E-16, -1.000000000000000000 ) ) ;
#6235=CARTESIAN_POINT ( 'NONE',  ( 3.857023737882813386, 9.897976262117209600, 26.00000000000000711 ) ) ;
#6241=AXIS2_PLACEMENT_3D ( 'NONE', #48415, #69977, #28906 ) ;
#6246=EDGE_CURVE ( 'NONE', #51293, #48513, #13592, .T. ) ;
#6253=VECTOR ( 'NONE', #52632, 1000.000000000000000 ) ;
#6265=DIRECTION ( 'NONE',  ( 1.000000000000000000, 2.135044278125301343E-15, -0.000000000000000000 ) ) ;
#6272=EDGE_LOOP ( 'NONE', ( #23945, #27490, #55634, #20712 ) ) ;
#6283=EDGE_LOOP ( 'NONE', ( #59057, #46236, #30325, #67691 ) ) ;
#6285=EDGE_CURVE ( 'NONE', #34294, #35057, #23990, .T. ) ;
#6288=AXIS2_PLACEMENT_3D ( 'NONE', #23607, #67092, #50490 ) ;
#6305=CIRCLE ( 'NONE', #61599, 0.1749999999999998224 ) ;
#6313=DIRECTION ( 'NONE',  ( -1.000000000000000000, 0.000000000000000000, 0.000000000000000000 ) ) ;
#6314=CARTESIAN_POINT ( 'NONE',  ( -5.242976262117280406, -5.257023737882805747, 54.00000000000000711 ) ) ;
#6316=CARTESIAN_POINT ( 'NONE',  ( 3.682023737882818892, 9.897976262117202495, 54.00000000000000711 ) ) ;
#6317=EDGE_CURVE ( 'NONE', #36489, #14072, #24348, .T. ) ;
#6319=PLANE ( 'NONE',  #26008 ) ;
#6322=VERTEX_POINT ( 'NONE', #30359 ) ;
#6323=CARTESIAN_POINT ( 'NONE',  ( -4.135079735113167843, 3.663616288757005623, 26.00000000000000711 ) ) ;
#6346=VERTEX_POINT ( 'NONE', #8421 ) ;
#6351=EDGE_LOOP ( 'NONE', ( #42752, #64723, #59451, #44875 ) ) ;
#6365=LINE ( 'NONE', #4973, #58362 ) ;
#6373=VECTOR ( 'NONE', #57527, 1000.000000000000000 ) ;
#6387=CARTESIAN_POINT ( 'NONE',  ( 9.912023737882815766, -3.857023737882816050, 26.00000000000000711 ) ) ;
#6395=CIRCLE ( 'NONE', #7484, 0.5249999999999990230 ) ;
#6398=CARTESIAN_POINT ( 'NONE',  ( 3.857023737882817827, 10.30047626211720413, 54.00000000000000711 ) ) ;
#6403=VECTOR ( 'NONE', #40361, 1000.000000000000000 ) ;
#6409=ORIENTED_EDGE ( 'NONE', *, *, #44016, .T. ) ;
#6422=DIRECTION ( 'NONE',  ( 0.7071067811865474617, 0.7071067811865474617, 0.000000000000000000 ) ) ;
#6423=EDGE_LOOP ( 'NONE', ( #10747, #15510, #54733, #52394 ) ) ;
#6441=CARTESIAN_POINT ( 'NONE',  ( -3.834182069070765309, 7.342976262117170805, 54.00000000000000711 ) ) ;
#6454=ORIENTED_EDGE ( 'NONE', *, *, #53190, .F. ) ;
#6457=DIRECTION ( 'NONE',  ( 1.000000000000000000, -1.356437060717834379E-15, -1.836970198721032646E-16 ) ) ;
#6465=EDGE_LOOP ( 'NONE', ( #5333, #41674, #8885, #7385 ) ) ;
#6467=LINE ( 'NONE', #49927, #12953 ) ;
#6468=VECTOR ( 'NONE', #4823, 1000.000000000000000 ) ;
#6472=LINE ( 'NONE', #22723, #34602 ) ;
#6475=ORIENTED_EDGE ( 'NONE', *, *, #35780, .T. ) ;
#6480=AXIS2_PLACEMENT_3D ( 'NONE', #24375, #29313, #45575 ) ;
#6486=CARTESIAN_POINT ( 'NONE',  ( 10.31452373788280674, 6.835476262117182067, 54.00000000000000711 ) ) ;
#6489=ORIENTED_EDGE ( 'NONE', *, *, #1650, .F. ) ;
#6491=EDGE_CURVE ( 'NONE', #10855, #16950, #54036, .T. ) ;
#6502=VERTEX_POINT ( 'NONE', #52636 ) ;
#6507=VECTOR ( 'NONE', #59618, 1000.000000000000000 ) ;
#6508=AXIS2_PLACEMENT_3D ( 'NONE', #24638, #56793, #19318 ) ;
#6509=CYLINDRICAL_SURFACE ( 'NONE', #49018, 0.1749999999999989342 ) ;
#6517=DIRECTION ( 'NONE',  ( 1.000000000000000000, -3.491481338843133355E-15, -1.836970198721036344E-16 ) ) ;
#6519=DIRECTION ( 'NONE',  ( -1.671920889371702854E-15, 1.000000000000000000, 3.673940397442059868E-16 ) ) ;
#6529=EDGE_CURVE ( 'NONE', #39629, #51302, #14761, .T. ) ;
#6532=ADVANCED_FACE ( 'NONE', ( #49419 ), #49059, .F. ) ;
#6535=ORIENTED_EDGE ( 'NONE', *, *, #61737, .T. ) ;
#6540=ORIENTED_EDGE ( 'NONE', *, *, #29145, .F. ) ;
#6546=LINE ( 'NONE', #39394, #53244 ) ;
#6548=AXIS2_PLACEMENT_3D ( 'NONE', #54586, #17427, #66223 ) ;
#6567=EDGE_CURVE ( 'NONE', #61001, #1782, #22539, .T. ) ;
#6574=DIRECTION ( 'NONE',  ( -1.000000000000000000, -2.135044278125301343E-15, 0.000000000000000000 ) ) ;
#6584=LINE ( 'NONE', #22830, #45182 ) ;
#6593=ORIENTED_EDGE ( 'NONE', *, *, #56527, .T. ) ;
#6621=CARTESIAN_POINT ( 'NONE',  ( 8.241237374594303944, -1.634292677759877854, 26.00000000000000711 ) ) ;
#6625=CARTESIAN_POINT ( 'NONE',  ( -9.897976262117246904, -3.857023737882716574, 26.00000000000000000 ) ) ;
#6628=DIRECTION ( 'NONE',  ( 1.000000000000000000, -1.047444401652940007E-14, 1.836970198721010706E-16 ) ) ;
#6631=CARTESIAN_POINT ( 'NONE',  ( -3.834182069070765309, 7.342976262117170805, 54.00000000000000711 ) ) ;
#6634=ADVANCED_FACE ( 'NONE', ( #38123 ), #1641, .F. ) ;
#6636=DIRECTION ( 'NONE',  ( 0.000000000000000000, 1.000000000000000000, 0.000000000000000000 ) ) ;
#6647=CARTESIAN_POINT ( 'NONE',  ( 6.832023737882818359, -9.912023737882810437, 26.00000000000000000 ) ) ;
#6651=CARTESIAN_POINT ( 'NONE',  ( 6.849523737882818430, 10.30047626211719169, 54.00000000000000711 ) ) ;
#6657=LINE ( 'NONE', #7335, #36390 ) ;
#6658=ORIENTED_EDGE ( 'NONE', *, *, #46528, .T. ) ;
#6665=ORIENTED_EDGE ( 'NONE', *, *, #60331, .F. ) ;
#6666=VERTEX_POINT ( 'NONE', #27488 ) ;
#6670=PLANE ( 'NONE',  #21393 ) ;
#6679=CARTESIAN_POINT ( 'NONE',  ( -9.390476262117259054, 1.466476262117183627, 26.00000000000000711 ) ) ;
#6685=VECTOR ( 'NONE', #32591, 1000.000000000000000 ) ;
#6693=CYLINDRICAL_SURFACE ( 'NONE', #68545, 0.1749999999999998224 ) ;
#6698=DIRECTION ( 'NONE',  ( 1.836970198721029934E-16, -1.836970198721036344E-16, 1.000000000000000000 ) ) ;
#6708=CIRCLE ( 'NONE', #39461, 0.1749999999999998224 ) ;
#6710=PLANE ( 'NONE',  #15521 ) ;
#6718=DIRECTION ( 'NONE',  ( 0.7071067811865391350, -0.7071067811865560104, 0.000000000000000000 ) ) ;
#6720=DIRECTION ( 'NONE',  ( 0.000000000000000000, -1.000000000000000000, 0.000000000000000000 ) ) ;
#6741=VERTEX_POINT ( 'NONE', #30280 ) ;
#6748=ORIENTED_EDGE ( 'NONE', *, *, #62548, .F. ) ;
#6750=DIRECTION ( 'NONE',  ( 0.7071067811865361374, -0.7071067811865588970, 0.000000000000000000 ) ) ;
#6752=EDGE_LOOP ( 'NONE', ( #63552, #30088, #30966, #66334 ) ) ;
#6754=DIRECTION ( 'NONE',  ( -1.836970198721029934E-16, 1.836970198721036590E-16, -1.000000000000000000 ) ) ;
#6768=AXIS2_PLACEMENT_3D ( 'NONE', #37844, #23908, #34506 ) ;
#6777=CARTESIAN_POINT ( 'NONE',  ( 9.737023737882816832, -3.682023737882826886, 54.00000000000000711 ) ) ;
#6781=ORIENTED_EDGE ( 'NONE', *, *, #12990, .F. ) ;
#6788=LINE ( 'NONE', #22387, #36716 ) ;
#6802=DIRECTION ( 'NONE',  ( 0.000000000000000000, 0.000000000000000000, 1.000000000000000000 ) ) ;
#6806=VECTOR ( 'NONE', #6040, 1000.000000000000000 ) ;
#6819=FACE_OUTER_BOUND ( 'NONE', #12217, .T. ) ;
#6821=ORIENTED_EDGE ( 'NONE', *, *, #26234, .T. ) ;
#6822=CARTESIAN_POINT ( 'NONE',  ( 6.849523737882818430, 10.30047626211719169, 54.00000000000000711 ) ) ;
#6823=EDGE_CURVE ( 'NONE', #39506, #6502, #62427, .T. ) ;
#6834=VERTEX_POINT ( 'NONE', #69850 ) ;
#6836=DIRECTION ( 'NONE',  ( 1.000000000000000000, -1.047444401652940007E-14, 1.836970198721010706E-16 ) ) ;
#6848=CARTESIAN_POINT ( 'NONE',  ( 5.257023737882819070, -3.157023737882815428, 26.00000000000000711 ) ) ;
#6850=ORIENTED_EDGE ( 'NONE', *, *, #6246, .T. ) ;
#6870=VERTEX_POINT ( 'NONE', #14711 ) ;
#6882=DIRECTION ( 'NONE',  ( 1.000000000000000000, 1.570596175624152290E-15, 0.000000000000000000 ) ) ;
#6884=DIRECTION ( 'NONE',  ( 0.000000000000000000, 3.673940397442059868E-16, -1.000000000000000000 ) ) ;
#6887=VECTOR ( 'NONE', #8827, 1000.000000000000000 ) ;
#6890=CARTESIAN_POINT ( 'NONE',  ( -9.915476262117259409, 0.9414762621171833823, 54.00000000000000711 ) ) ;
#6891=VECTOR ( 'NONE', #21721, 1000.000000000000000 ) ;
#6898=FACE_OUTER_BOUND ( 'NONE', #24860, .T. ) ;
#6907=ORIENTED_EDGE ( 'NONE', *, *, #62170, .T. ) ;
#6909=DIRECTION ( 'NONE',  ( -0.7671651518153065341, 0.6414496315691495809, 2.356647714346224881E-16 ) ) ;
#6912=CARTESIAN_POINT ( 'NONE',  ( 6.358413763958958853, 5.779227145995223580, 54.00000000000000711 ) ) ;
#6926=DIRECTION ( 'NONE',  ( 0.000000000000000000, -1.000000000000000000, 0.000000000000000000 ) ) ;
#6930=VERTEX_POINT ( 'NONE', #52914 ) ;
#6935=VERTEX_POINT ( 'NONE', #10451 ) ;
#6938=AXIS2_PLACEMENT_3D ( 'NONE', #1789, #62853, #55544 ) ;
#6944=CARTESIAN_POINT ( 'NONE',  ( 3.682023737882786918, -9.737023737882809726, 54.00000000000000711 ) ) ;
#6949=DIRECTION ( 'NONE',  ( -1.836970198721029934E-16, 1.836970198721036344E-16, -1.000000000000000000 ) ) ;
#6950=VERTEX_POINT ( 'NONE', #44008 ) ;
#6952=CIRCLE ( 'NONE', #17157, 1.224999999999999423 ) ;
#6964=CARTESIAN_POINT ( 'NONE',  ( -10.49297626211729551, -6.849523737882748264, 54.00000000000000711 ) ) ;
#6971=CARTESIAN_POINT ( 'NONE',  ( 6.364920264886884560, 6.822336235477388655, 26.00000000000000711 ) ) ;
#6973=CYLINDRICAL_SURFACE ( 'NONE', #569, 0.1749999999999998224 ) ;
#6975=PRODUCT ( '5537T808_T-Slotted Framing_5537T808', '5537T808_T-Slotted Framing_5537T808', '', ( #40946 ) ) ;
#6978=EDGE_CURVE ( 'NONE', #13295, #29848, #6546, .T. ) ;
#6979=FACE_OUTER_BOUND ( 'NONE', #6423, .T. ) ;
#6981=VERTEX_POINT ( 'NONE', #59931 ) ;
#6983=CARTESIAN_POINT ( 'NONE',  ( -9.689726262117314803, -8.580623737882756785, 54.00000000000000711 ) ) ;
#6995=ORIENTED_EDGE ( 'NONE', *, *, #34646, .F. ) ;
#6996=PLANE ( 'NONE',  #25484 ) ;
#7002=VERTEX_POINT ( 'NONE', #542 ) ;
#7003=ORIENTED_EDGE ( 'NONE', *, *, #26485, .F. ) ;
#7008=ADVANCED_FACE ( 'NONE', ( #60268 ), #49341, .F. ) ;
#7010=LINE ( 'NONE', #65732, #56115 ) ;
#7018=CARTESIAN_POINT ( 'NONE',  ( -3.842976262117224984, 9.897976262117168744, 54.00000000000000711 ) ) ;
#7019=ORIENTED_EDGE ( 'NONE', *, *, #9734, .F. ) ;
#7028=VERTEX_POINT ( 'NONE', #60955 ) ;
#7029=DIRECTION ( 'NONE',  ( -0.7071067811865464625, 0.7071067811865486830, 0.000000000000000000 ) ) ;
#7036=CIRCLE ( 'NONE', #26247, 0.1749999999999998224 ) ;
#7039=CARTESIAN_POINT ( 'NONE',  ( -6.835476262117333057, -10.31452373788278543, 54.00000000000000711 ) ) ;
#7053=DIRECTION ( 'NONE',  ( 0.6414496315691565753, -0.7671651518153006499, -2.818519042764004597E-16 ) ) ;
#7057=DIRECTION ( 'NONE',  ( 1.000000000000000000, -1.130039751537442024E-14, -1.836970198721050642E-16 ) ) ;
#7060=FACE_OUTER_BOUND ( 'NONE', #64004, .T. ) ;
#7067=VERTEX_POINT ( 'NONE', #12176 ) ;
#7069=CARTESIAN_POINT ( 'NONE',  ( -7.955476262117322506, -9.737023737882765317, 26.00000000000000000 ) ) ;
#7079=EDGE_LOOP ( 'NONE', ( #9092, #31609, #40649, #12720 ) ) ;
#7085=DIRECTION ( 'NONE',  ( -0.000000000000000000, -0.000000000000000000, -1.000000000000000000 ) ) ;
#7088=ORIENTED_EDGE ( 'NONE', *, *, #22135, .T. ) ;
#7093=VECTOR ( 'NONE', #15654, 1000.000000000000000 ) ;
#7100=ORIENTED_EDGE ( 'NONE', *, *, #56609, .F. ) ;
#7106=EDGE_CURVE ( 'NONE', #18604, #36864, #40448, .T. ) ;
#7111=DIRECTION ( 'NONE',  ( -1.000000000000000000, 7.665540703601096574E-15, 0.000000000000000000 ) ) ;
#7115=LINE ( 'NONE', #12758, #20751 ) ;
#7117=CIRCLE ( 'NONE', #47770, 0.1749999999999989342 ) ;
#7126=VECTOR ( 'NONE', #34586, 1000.000000000000000 ) ;
#7134=CARTESIAN_POINT ( 'NONE',  ( -3.667976262117330410, -9.912023737882817542, 54.00000000000000711 ) ) ;
#7144=CARTESIAN_POINT ( 'NONE',  ( 10.05377373788281226, 9.689726262117156708, 26.00000000000000711 ) ) ;
#7155=AXIS2_PLACEMENT_3D ( 'NONE', #23156, #60977, #7232 ) ;
#7157=CARTESIAN_POINT ( 'NONE',  ( 5.257023737882819070, -5.257023737882825287, 54.00000000000000711 ) ) ;
#7162=DIRECTION ( 'NONE',  ( 0.000000000000000000, 3.673940397442059868E-16, -1.000000000000000000 ) ) ;
#7172=ORIENTED_EDGE ( 'NONE', *, *, #63043, .T. ) ;
#7176=CARTESIAN_POINT ( 'NONE',  ( 9.562023737882812569, -2.369523737882825998, 54.00000000000000711 ) ) ;
#7182=CARTESIAN_POINT ( 'NONE',  ( 4.046023737882819660, -3.157023737882815873, 26.00000000000000711 ) ) ;
#7187=AXIS2_PLACEMENT_3D ( 'NONE', #19770, #52316, #57264 ) ;
#7190=ORIENTED_EDGE ( 'NONE', *, *, #63477, .F. ) ;
#7193=DIRECTION ( 'NONE',  ( -0.7071067811865550112, -0.7071067811865401342, -2.597868168706466299E-16 ) ) ;
#7194=ORIENTED_EDGE ( 'NONE', *, *, #26304, .F. ) ;
#7196=AXIS2_PLACEMENT_3D ( 'NONE', #34617, #50880, #8808 ) ;
#7202=VECTOR ( 'NONE', #6628, 1000.000000000000000 ) ;
#7205=CIRCLE ( 'NONE', #51123, 0.1749999999999998224 ) ;
#7210=FACE_OUTER_BOUND ( 'NONE', #6351, .T. ) ;
#7216=DIRECTION ( 'NONE',  ( 0.000000000000000000, 0.000000000000000000, 1.000000000000000000 ) ) ;
#7225=ORIENTED_EDGE ( 'NONE', *, *, #65832, .T. ) ;
#7232=DIRECTION ( 'NONE',  ( 1.000000000000000000, 0.000000000000000000, 0.000000000000000000 ) ) ;
#7241=CARTESIAN_POINT ( 'NONE',  ( -10.03972626211732155, -9.703773737882716688, 26.00000000000000000 ) ) ;
#7242=DIRECTION ( 'NONE',  ( 1.836970198721029934E-16, 1.836970198721010706E-16, -1.000000000000000000 ) ) ;
#7246=AXIS2_PLACEMENT_3D ( 'NONE', #65525, #38986, #39668 ) ;
#7262=EDGE_CURVE ( 'NONE', #63019, #21681, #4029, .T. ) ;
#7263=EDGE_LOOP ( 'NONE', ( #24941, #10656, #33634, #63029 ) ) ;
#7265=EDGE_CURVE ( 'NONE', #48513, #45585, #65679, .T. ) ;
#7268=ORIENTED_EDGE ( 'NONE', *, *, #16070, .F. ) ;
#7271=EDGE_CURVE ( 'NONE', #12301, #57153, #30893, .T. ) ;
#7281=VECTOR ( 'NONE', #19343, 1000.000000000000000 ) ;
#7286=CYLINDRICAL_SURFACE ( 'NONE', #16402, 0.1749999999999998224 ) ;
#7290=AXIS2_PLACEMENT_3D ( 'NONE', #69539, #59964, #15794 ) ;
#7292=ORIENTED_EDGE ( 'NONE', *, *, #4067, .T. ) ;
#7308=DIRECTION ( 'NONE',  ( -0.7071067811865475727, -0.7071067811865475727, 0.000000000000000000 ) ) ;
#7332=EDGE_CURVE ( 'NONE', #13327, #56322, #62707, .T. ) ;
#7335=CARTESIAN_POINT ( 'NONE',  ( -7.605476262117258024, 9.722976262117178692, 54.00000000000000711 ) ) ;
#7337=VECTOR ( 'NONE', #6265, 1000.000000000000000 ) ;
#7339=AXIS2_PLACEMENT_3D ( 'NONE', #34673, #62244, #30431 ) ;
#7345=AXIS2_PLACEMENT_3D ( 'NONE', #53840, #36509, #52436 ) ;
#7347=DIRECTION ( 'NONE',  ( 1.836970198721029934E-16, 1.836970198721010706E-16, -1.000000000000000000 ) ) ;
#7354=EDGE_LOOP ( 'NONE', ( #11850, #66864, #39928, #526 ) ) ;
#7355=DIRECTION ( 'NONE',  ( -1.000000000000000000, 1.047444401652940007E-14, -1.836970198721010706E-16 ) ) ;
#7356=CARTESIAN_POINT ( 'NONE',  ( -7.955476262117259445, 9.547976262117179758, 54.00000000000000711 ) ) ;
#7363=DIRECTION ( 'NONE',  ( 9.912705577010344285E-15, 1.000000000000000000, 0.000000000000000000 ) ) ;
#7365=DIRECTION ( 'NONE',  ( -0.7071067811865500152, -0.7071067811865451302, 4.683861624749757595E-31 ) ) ;
#7367=VERTEX_POINT ( 'NONE', #7465 ) ;
#7371=ORIENTED_EDGE ( 'NONE', *, *, #1700, .T. ) ;
#7377=CARTESIAN_POINT ( 'NONE',  ( 7.357023737882817827, -6.665817930929303969, 54.00000000000000711 ) ) ;
#7379=CIRCLE ( 'NONE', #69488, 1.224999999999998757 ) ;
#7385=ORIENTED_EDGE ( 'NONE', *, *, #49909, .T. ) ;
#7387=VECTOR ( 'NONE', #58666, 1000.000000000000000 ) ;
#7392=ORIENTED_EDGE ( 'NONE', *, *, #739, .T. ) ;
#7393=DIRECTION ( 'NONE',  ( 0.000000000000000000, -1.000000000000000000, -3.673940397442059868E-16 ) ) ;
#7399=DIRECTION ( 'NONE',  ( -0.000000000000000000, 3.673940397442059868E-16, -1.000000000000000000 ) ) ;
#7401=CARTESIAN_POINT ( 'NONE',  ( -10.30047626211725742, 6.642976262117184838, 54.00000000000000711 ) ) ;
#7407=CARTESIAN_POINT ( 'NONE',  ( 4.720772854004765762, 6.344366288193357128, 26.00000000000000711 ) ) ;
#7410=ORIENTED_EDGE ( 'NONE', *, *, #42673, .F. ) ;
#7412=CARTESIAN_POINT ( 'NONE',  ( 8.093267424590464998, -8.711985858128699078, 54.00000000000000711 ) ) ;
#7416=ORIENTED_EDGE ( 'NONE', *, *, #1366, .F. ) ;
#7418=ADVANCED_FACE ( 'NONE', ( #39632 ), #55910, .F. ) ;
#7421=ORIENTED_EDGE ( 'NONE', *, *, #45959, .F. ) ;
#7424=FACE_BOUND ( 'NONE', #1427, .T. ) ;
#7442=DIRECTION ( 'NONE',  ( -0.7071067811865588970, -0.7071067811865361374, -2.597868168706466792E-16 ) ) ;
#7444=VECTOR ( 'NONE', #61557, 1000.000000000000000 ) ;
#7446=AXIS2_PLACEMENT_3D ( 'NONE', #42017, #68187, #41663 ) ;
#7447=CARTESIAN_POINT ( 'NONE',  ( -10.50612335864048674, 6.822329165593977507, 26.00000000000000711 ) ) ;
#7459=ORIENTED_EDGE ( 'NONE', *, *, #51195, .T. ) ;
#7465=CARTESIAN_POINT ( 'NONE',  ( 9.929523737882751888, 0.9414762621171479662, 54.00000000000000711 ) ) ;
#7473=ORIENTED_EDGE ( 'NONE', *, *, #16239, .F. ) ;
#7476=VERTEX_POINT ( 'NONE', #30087 ) ;
#7480=VERTEX_POINT ( 'NONE', #46344 ) ;
#7482=CARTESIAN_POINT ( 'NONE',  ( -6.651770455163739548, 7.342976262117183239, 26.00000000000000711 ) ) ;
#7484=AXIS2_PLACEMENT_3D ( 'NONE', #62673, #46068, #36153 ) ;
#7492=ORIENTED_EDGE ( 'NONE', *, *, #33423, .T. ) ;
#7503=CARTESIAN_POINT ( 'NONE',  ( -4.031976262117257903, -3.157023737882818981, 54.00000000000000711 ) ) ;
#7510=CYLINDRICAL_SURFACE ( 'NONE', #68631, 1.929199999999997139 ) ;
#7513=FACE_OUTER_BOUND ( 'NONE', #21774, .T. ) ;
#7539=VECTOR ( 'NONE', #56107, 1000.000000000000000 ) ;
#7541=ORIENTED_EDGE ( 'NONE', *, *, #739, .F. ) ;
#7549=AXIS2_PLACEMENT_3D ( 'NONE', #58637, #20795, #48374 ) ;
#7550=LINE ( 'NONE', #51746, #20695 ) ;
#7552=ORIENTED_EDGE ( 'NONE', *, *, #58852, .T. ) ;
#7561=ORIENTED_EDGE ( 'NONE', *, *, #52806, .T. ) ;
#7565=VECTOR ( 'NONE', #17914, 999.9999999999998863 ) ;
#7567=CARTESIAN_POINT ( 'NONE',  ( -5.242976262117259978, 5.242976262117182706, 54.00000000000000711 ) ) ;
#7568=VERTEX_POINT ( 'NONE', #57658 ) ;
#7575=ORIENTED_EDGE ( 'NONE', *, *, #2429, .F. ) ;
#7587=CARTESIAN_POINT ( 'NONE',  ( -1.466476262117230034, 9.390476262117152473, 54.00000000000000711 ) ) ;
#7589=AXIS2_PLACEMENT_3D ( 'NONE', #37700, #933, #59263 ) ;
#7594=EDGE_CURVE ( 'NONE', #67224, #55172, #5337, .T. ) ;
#7597=EDGE_CURVE ( 'NONE', #48280, #42663, #31588, .T. ) ;
#7598=VERTEX_POINT ( 'NONE', #53768 ) ;
#7600=CARTESIAN_POINT ( 'NONE',  ( 5.793274621760843957, -4.155633711806670405, 54.00000000000000711 ) ) ;
#7624=DIRECTION ( 'NONE',  ( -3.491481338843133355E-15, -1.000000000000000000, 0.000000000000000000 ) ) ;
#7626=VERTEX_POINT ( 'NONE', #37155 ) ;
#7637=ORIENTED_EDGE ( 'NONE', *, *, #58322, .F. ) ;
#7640=DIRECTION ( 'NONE',  ( 0.000000000000000000, -1.000000000000000000, 0.000000000000000000 ) ) ;
#7648=VERTEX_POINT ( 'NONE', #47745 ) ;
#7650=EDGE_CURVE ( 'NONE', #41013, #44516, #58719, .T. ) ;
#7659=CARTESIAN_POINT ( 'NONE',  ( 6.364920264886851697, 3.663616288756991413, 54.00000000000000711 ) ) ;
#7677=ORIENTED_EDGE ( 'NONE', *, *, #50787, .T. ) ;
#7685=EDGE_CURVE ( 'NONE', #46756, #45109, #64709, .T. ) ;
#7690=CARTESIAN_POINT ( 'NONE',  ( 2.369523737882786918, -9.562023737882798358, 54.00000000000000711 ) ) ;
#7692=FACE_OUTER_BOUND ( 'NONE', #63609, .T. ) ;
#7696=ADVANCED_FACE ( 'NONE', ( #59408 ), #54111, .F. ) ;
#7698=CARTESIAN_POINT ( 'NONE',  ( -6.835476262117334834, -10.50702373788278798, 54.00000000000000711 ) ) ;
#7700=ORIENTED_EDGE ( 'NONE', *, *, #37701, .F. ) ;
#7706=LINE ( 'NONE', #66759, #16895 ) ;
#7707=DIRECTION ( 'NONE',  ( 1.000000000000000000, -1.047444401652940007E-14, 1.836970198721010706E-16 ) ) ;
#7709=ORIENTED_EDGE ( 'NONE', *, *, #15273, .T. ) ;
#7722=CARTESIAN_POINT ( 'NONE',  ( 9.737023737882816832, -6.832023737882823688, 54.00000000000000711 ) ) ;
#7723=DIRECTION ( 'NONE',  ( 1.836970198721029934E-16, -1.836970198721036344E-16, 1.000000000000000000 ) ) ;
#7725=VERTEX_POINT ( 'NONE', #48451 ) ;
#7727=CARTESIAN_POINT ( 'NONE',  ( 5.257023737882801306, 5.242976262117200470, 54.00000000000000711 ) ) ;
#7729=LINE ( 'NONE', #66778, #35717 ) ;
#7731=VECTOR ( 'NONE', #35186, 1000.000000000000000 ) ;
#7736=ORIENTED_EDGE ( 'NONE', *, *, #59190, .F. ) ;
#7737=VECTOR ( 'NONE', #24851, 1000.000000000000000 ) ;
#7739=LINE ( 'NONE', #35659, #971 ) ;
#7745=EDGE_CURVE ( 'NONE', #30522, #57627, #48584, .T. ) ;
#7747=VECTOR ( 'NONE', #29844, 1000.000000000000000 ) ;
#7748=DIRECTION ( 'NONE',  ( 2.478176394252608948E-15, 1.000000000000000000, 0.000000000000000000 ) ) ;
#7749=DIRECTION ( 'NONE',  ( 0.000000000000000000, 1.000000000000000000, 0.000000000000000000 ) ) ;
#7764=CARTESIAN_POINT ( 'NONE',  ( 2.544523737882785852, -9.737023737882799068, 54.00000000000000711 ) ) ;
#7766=LINE ( 'NONE', #50900, #21846 ) ;
#7771=EDGE_CURVE ( 'NONE', #1721, #19808, #40163, .T. ) ;
#7782=DIRECTION ( 'NONE',  ( 0.000000000000000000, -3.673940397442059868E-16, 1.000000000000000000 ) ) ;
#7786=DIRECTION ( 'NONE',  ( 9.912705577010435793E-15, 1.000000000000000000, 0.000000000000000000 ) ) ;
#7789=DIRECTION ( 'NONE',  ( 1.952517519553884087E-14, 1.000000000000000000, 1.836970198721046451E-16 ) ) ;
#7792=EDGE_LOOP ( 'NONE', ( #24601, #43342, #35930, #55525 ) ) ;
#7797=ORIENTED_EDGE ( 'NONE', *, *, #38967, .T. ) ;
#7808=ORIENTED_EDGE ( 'NONE', *, *, #64737, .T. ) ;
#7814=LINE ( 'NONE', #50957, #33412 ) ;
#7819=CYLINDRICAL_SURFACE ( 'NONE', #48596, 0.1749999999999998224 ) ;
#7825=VERTEX_POINT ( 'NONE', #19643 ) ;
#7834=DIRECTION ( 'NONE',  ( -1.000000000000000000, 1.047444401652940007E-14, 0.000000000000000000 ) ) ;
#7848=VECTOR ( 'NONE', #25266, 1000.000000000000114 ) ;
#7849=DIRECTION ( 'NONE',  ( -1.000000000000000000, 0.000000000000000000, 0.000000000000000000 ) ) ;
#7850=EDGE_CURVE ( 'NONE', #15565, #59231, #39520, .T. ) ;
#7856=DIRECTION ( 'NONE',  ( 1.000000000000000000, -7.304098846218132892E-15, -2.683482381803073952E-30 ) ) ;
#7867=ORIENTED_EDGE ( 'NONE', *, *, #63414, .T. ) ;
#7889=ORIENTED_EDGE ( 'NONE', *, *, #374, .F. ) ;
#7893=CARTESIAN_POINT ( 'NONE',  ( -9.689726262117227762, 9.689726262117183353, 26.00000000000000711 ) ) ;
#7899=AXIS2_PLACEMENT_3D ( 'NONE', #16928, #55110, #50133 ) ;
#7916=VECTOR ( 'NONE', #27743, 1000.000000000000000 ) ;
#7918=FACE_OUTER_BOUND ( 'NONE', #48283, .T. ) ;
#7921=FACE_OUTER_BOUND ( 'NONE', #3147, .T. ) ;
#7926=CARTESIAN_POINT ( 'NONE',  ( -5.242976262117275077, -5.257023737882800418, 26.00000000000000711 ) ) ;
#7930=VECTOR ( 'NONE', #13488, 1000.000000000000000 ) ;
#7932=VECTOR ( 'NONE', #2095, 1000.000000000000000 ) ;
#7947=DIRECTION ( 'NONE',  ( 1.000000000000000000, -4.121462285523435444E-16, 0.000000000000000000 ) ) ;
#7959=EDGE_LOOP ( 'NONE', ( #7808, #24342, #69344, #12258 ) ) ;
#7981=VECTOR ( 'NONE', #63243, 1000.000000000000000 ) ;
#7982=DIRECTION ( 'NONE',  ( -1.000000000000000000, 0.000000000000000000, 0.000000000000000000 ) ) ;
#7983=ORIENTED_EDGE ( 'NONE', *, *, #21906, .F. ) ;
#7999=DIRECTION ( 'NONE',  ( 1.000000000000000000, 5.013651664672856055E-16, 0.000000000000000000 ) ) ;
#8001=DIRECTION ( 'NONE',  ( 1.000000000000000000, -1.047444401652940007E-14, 1.836970198721010706E-16 ) ) ;
#8004=LINE ( 'NONE', #62443, #15163 ) ;
#8017=DIRECTION ( 'NONE',  ( -1.836970198721029934E-16, 1.836970198721036590E-16, -1.000000000000000000 ) ) ;
#8018=DIRECTION ( 'NONE',  ( -0.000000000000000000, -0.000000000000000000, -1.000000000000000000 ) ) ;
#8020=CARTESIAN_POINT ( 'NONE',  ( -6.858227778582845602, -3.003254798005714488, 54.00000000000000711 ) ) ;
#8035=VERTEX_POINT ( 'NONE', #27406 ) ;
#8041=DIRECTION ( 'NONE',  ( -1.000000000000000000, 0.000000000000000000, 0.000000000000000000 ) ) ;
#8047=ORIENTED_EDGE ( 'NONE', *, *, #19650, .T. ) ;
#8050=FACE_OUTER_BOUND ( 'NONE', #53608, .T. ) ;
#8054=DIRECTION ( 'NONE',  ( -1.000000000000000000, 4.121462285523435444E-16, 1.514200678731842937E-31 ) ) ;
#8059=DIRECTION ( 'NONE',  ( 8.540177112501197482E-15, 1.000000000000000000, -0.000000000000000000 ) ) ;
#8062=EDGE_CURVE ( 'NONE', #11799, #42510, #32724, .T. ) ;
#8064=DIRECTION ( 'NONE',  ( -1.000000000000000000, 0.000000000000000000, 0.000000000000000000 ) ) ;
#8069=EDGE_CURVE ( 'NONE', #67352, #10965, #535, .T. ) ;
#8074=CARTESIAN_POINT ( 'NONE',  ( -6.651770455163739548, 7.342976262117183239, 54.00000000000000711 ) ) ;
#8080=LINE ( 'NONE', #67507, #29440 ) ;
#8082=VERTEX_POINT ( 'NONE', #60619 ) ;
#8084=VECTOR ( 'NONE', #13041, 1000.000000000000000 ) ;
#8086=DIRECTION ( 'NONE',  ( 1.836970198721029934E-16, -1.836970198721036344E-16, 1.000000000000000000 ) ) ;
#8090=DIRECTION ( 'NONE',  ( 0.7071067811865474617, -0.7071067811865474617, 0.000000000000000000 ) ) ;
#8096=DIRECTION ( 'NONE',  ( 1.000000000000000000, -1.254221251785257574E-14, 0.000000000000000000 ) ) ;
#8102=CARTESIAN_POINT ( 'NONE',  ( 6.836383711243005479, -6.364920264886905876, 54.00000000000000711 ) ) ;
#8104=DIRECTION ( 'NONE',  ( 1.836970198721029934E-16, 1.836970198721010706E-16, -1.000000000000000000 ) ) ;
#8108=ORIENTED_EDGE ( 'NONE', *, *, #37525, .T. ) ;
#8111=CARTESIAN_POINT ( 'NONE',  ( 2.420780051175163816, 8.697938382363089360, 26.00000000000000711 ) ) ;
#8114=CYLINDRICAL_SURFACE ( 'NONE', #41372, 0.1749999999999989342 ) ;
#8115=LINE ( 'NONE', #57621, #40614 ) ;
#8120=LINE ( 'NONE', #3893, #30381 ) ;
#8126=CARTESIAN_POINT ( 'NONE',  ( -2.989207322240185594, 6.858227778582772771, 54.00000000000000711 ) ) ;
#8129=ORIENTED_EDGE ( 'NONE', *, *, #35931, .F. ) ;
#8131=AXIS2_PLACEMENT_3D ( 'NONE', #297, #43076, #37780 ) ;
#8134=ORIENTED_EDGE ( 'NONE', *, *, #19268, .T. ) ;
#8135=CARTESIAN_POINT ( 'NONE',  ( 3.677663764522614454, -6.364920264886879231, 54.00000000000000711 ) ) ;
#8148=VERTEX_POINT ( 'NONE', #12850 ) ;
#8152=VECTOR ( 'NONE', #16083, 1000.000000000000000 ) ;
#8158=VECTOR ( 'NONE', #40571, 1000.000000000000000 ) ;
#8177=ORIENTED_EDGE ( 'NONE', *, *, #49625, .T. ) ;
#8180=LINE ( 'NONE', #12103, #17088 ) ;
#8185=DIRECTION ( 'NONE',  ( 0.6414496315691565753, 0.7671651518153006499, 2.818519042764004597E-16 ) ) ;
#8192=CARTESIAN_POINT ( 'NONE',  ( 8.241237374594243548, 1.620245201994235718, 26.00000000000000711 ) ) ;
#8194=VECTOR ( 'NONE', #4624, 1000.000000000000000 ) ;
#8197=ORIENTED_EDGE ( 'NONE', *, *, #10600, .F. ) ;
#8199=ORIENTED_EDGE ( 'NONE', *, *, #9558, .T. ) ;
#8206=CARTESIAN_POINT ( 'NONE',  ( 9.795823737882805915, -10.50702373788282529, 54.00000000000000711 ) ) ;
#8210=AXIS2_PLACEMENT_3D ( 'NONE', #63176, #68840, #57867 ) ;
#8218=VECTOR ( 'NONE', #65004, 1000.000000000000000 ) ;
#8222=ORIENTED_EDGE ( 'NONE', *, *, #18131, .F. ) ;
#8226=CARTESIAN_POINT ( 'NONE',  ( -9.915476262117259409, 0.9414762621171833823, 26.00000000000000711 ) ) ;
#8237=ORIENTED_EDGE ( 'NONE', *, *, #69535, .F. ) ;
#8242=EDGE_LOOP ( 'NONE', ( #13871, #55656, #28396, #15748 ) ) ;
#8249=ORIENTED_EDGE ( 'NONE', *, *, #24748, .F. ) ;
#8253=LINE ( 'NONE', #45735, #35604 ) ;
#8254=ORIENTED_EDGE ( 'NONE', *, *, #20781, .T. ) ;
#8260=FACE_OUTER_BOUND ( 'NONE', #11676, .T. ) ;
#8264=ORIENTED_EDGE ( 'NONE', *, *, #20682, .F. ) ;
#8275=CARTESIAN_POINT ( 'NONE',  ( -3.667976262117328190, -9.737023737882820384, 54.00000000000000711 ) ) ;
#8279=CARTESIAN_POINT ( 'NONE',  ( -10.03972626211731978, -8.930623737882752877, 54.00000000000000711 ) ) ;
#8280=FACE_OUTER_BOUND ( 'NONE', #7263, .T. ) ;
#8281=AXIS2_PLACEMENT_3D ( 'NONE', #43536, #10673, #37554 ) ;
#8307=VECTOR ( 'NONE', #1621, 1000.000000000000000 ) ;
#8309=DIRECTION ( 'NONE',  ( 0.000000000000000000, 0.000000000000000000, 1.000000000000000000 ) ) ;
#8310=PLANE ( 'NONE',  #32298 ) ;
#8314=AXIS2_PLACEMENT_3D ( 'NONE', #46623, #40970, #62903 ) ;
#8315=ORIENTED_EDGE ( 'NONE', *, *, #62935, .F. ) ;
#8318=ORIENTED_EDGE ( 'NONE', *, *, #37002, .T. ) ;
#8322=DIRECTION ( 'NONE',  ( 0.6414496315691446959, 0.7671651518153106419, -0.000000000000000000 ) ) ;
#8326=ORIENTED_EDGE ( 'NONE', *, *, #42243, .T. ) ;
#8335=CARTESIAN_POINT ( 'NONE',  ( 8.835729544836283367, 2.355476262117166986, 26.00000000000000711 ) ) ;
#8338=ORIENTED_EDGE ( 'NONE', *, *, #50494, .F. ) ;
#8349=LINE ( 'NONE', #2698, #7539 ) ;
#8360=PLANE ( 'NONE',  #57947 ) ;
#8362=CARTESIAN_POINT ( 'NONE',  ( -7.342976262117259623, 6.651770455163663165, 26.00000000000000711 ) ) ;
#8370=CIRCLE ( 'NONE', #47917, 1.224999999999999423 ) ;
#8372=ORIENTED_EDGE ( 'NONE', *, *, #49831, .F. ) ;
#8373=DIRECTION ( 'NONE',  ( -0.000000000000000000, -0.000000000000000000, -1.000000000000000000 ) ) ;
#8379=CARTESIAN_POINT ( 'NONE',  ( 4.149127210878741145, 3.663616288756999406, 54.00000000000000711 ) ) ;
#8389=DIRECTION ( 'NONE',  ( -0.000000000000000000, 3.673940397442059868E-16, -1.000000000000000000 ) ) ;
#8395=DIRECTION ( 'NONE',  ( 1.000000000000000000, 0.000000000000000000, 0.000000000000000000 ) ) ;
#8399=LINE ( 'NONE', #14061, #33555 ) ;
#8403=ORIENTED_EDGE ( 'NONE', *, *, #43440, .T. ) ;
#8405=DIRECTION ( 'NONE',  ( 0.7071067811865447972, -0.7071067811865502373, 0.000000000000000000 ) ) ;
#8406=LINE ( 'NONE', #68878, #52553 ) ;
#8421=CARTESIAN_POINT ( 'NONE',  ( -10.49297626211725998, 9.781776262117173104, 54.00000000000000711 ) ) ;
#8430=DIRECTION ( 'NONE',  ( 0.7071067811865510144, 0.7071067811865441310, -8.088905766426390583E-31 ) ) ;
#8433=CARTESIAN_POINT ( 'NONE',  ( -9.781776262117309884, -9.795823737882740190, 26.00000000000000000 ) ) ;
#8442=VECTOR ( 'NONE', #13957, 1000.000000000000000 ) ;
#8448=LINE ( 'NONE', #50197, #48203 ) ;
#8450=DIRECTION ( 'NONE',  ( -0.000000000000000000, 1.000000000000000000, -0.000000000000000000 ) ) ;
#8452=VERTEX_POINT ( 'NONE', #5768 ) ;
#8458=AXIS2_PLACEMENT_3D ( 'NONE', #19990, #41554, #37306 ) ;
#8461=DIRECTION ( 'NONE',  ( -1.836970198721029934E-16, 1.836970198721036590E-16, -1.000000000000000000 ) ) ;
#8464=VECTOR ( 'NONE', #16013, 1000.000000000000000 ) ;
#8474=ORIENTED_EDGE ( 'NONE', *, *, #66512, .T. ) ;
#8490=DIRECTION ( 'NONE',  ( 0.000000000000000000, -3.673940397442059868E-16, 1.000000000000000000 ) ) ;
#8497=PLANE ( 'NONE',  #7339 ) ;
#8505=VECTOR ( 'NONE', #10788, 1000.000000000000000 ) ;
#8528=ADVANCED_FACE ( 'NONE', ( #50267 ), #38293, .F. ) ;
#8535=VERTEX_POINT ( 'NONE', #65168 ) ;
#8536=DIRECTION ( 'NONE',  ( 0.000000000000000000, -0.000000000000000000, 1.000000000000000000 ) ) ;
#8537=CARTESIAN_POINT ( 'NONE',  ( 6.364920264886885448, -6.836383711243011696, 26.00000000000000000 ) ) ;
#8541=ADVANCED_FACE ( 'NONE', ( #33994 ), #66186, .F. ) ;
#8550=EDGE_CURVE ( 'NONE', #64676, #64879, #54902, .T. ) ;
#8553=FACE_OUTER_BOUND ( 'NONE', #39527, .T. ) ;
#8556=VECTOR ( 'NONE', #38960, 1000.000000000000000 ) ;
#8561=ORIENTED_EDGE ( 'NONE', *, *, #26984, .T. ) ;
#8565=DIRECTION ( 'NONE',  ( -1.836970198721029934E-16, 1.836970198721036590E-16, -1.000000000000000000 ) ) ;
#8570=LINE ( 'NONE', #47458, #18196 ) ;
#8571=VERTEX_POINT ( 'NONE', #39314 ) ;
#8579=AXIS2_PLACEMENT_3D ( 'NONE', #33691, #29085, #66563 ) ;
#8580=CARTESIAN_POINT ( 'NONE',  ( 10.31452373788277654, 3.650476262117150483, 26.00000000000000711 ) ) ;
#8587=VERTEX_POINT ( 'NONE', #32974 ) ;
#8589=EDGE_LOOP ( 'NONE', ( #18182, #24753, #28771, #60524 ) ) ;
#8593=DIRECTION ( 'NONE',  ( -0.000000000000000000, 3.673940397442059868E-16, -1.000000000000000000 ) ) ;
#8596=EDGE_LOOP ( 'NONE', ( #50610, #48439, #27548, #68368 ) ) ;
#8598=ORIENTED_EDGE ( 'NONE', *, *, #44019, .T. ) ;
#8605=EDGE_CURVE ( 'NONE', #12591, #51101, #17391, .T. ) ;
#8606=ORIENTED_EDGE ( 'NONE', *, *, #44467, .T. ) ;
#8609=LINE ( 'NONE', #35474, #65012 ) ;
#8612=EDGE_CURVE ( 'NONE', #11541, #2395, #64672, .T. ) ;
#8622=ORIENTED_EDGE ( 'NONE', *, *, #1585, .F. ) ;
#8630=AXIS2_PLACEMENT_3D ( 'NONE', #30366, #40961, #67138 ) ;
#8633=DIRECTION ( 'NONE',  ( 0.000000000000000000, 3.673940397442059868E-16, -1.000000000000000000 ) ) ;
#8641=FACE_OUTER_BOUND ( 'NONE', #61846, .T. ) ;
#8657=ORIENTED_EDGE ( 'NONE', *, *, #50945, .F. ) ;
#8664=DIRECTION ( 'NONE',  ( -0.7071067811865474617, -0.7071067811865474617, 0.000000000000000000 ) ) ;
#8671=AXIS2_PLACEMENT_3D ( 'NONE', #34115, #7242, #50391 ) ;
#8673=DIRECTION ( 'NONE',  ( 1.000000000000000000, 0.000000000000000000, 0.000000000000000000 ) ) ;
#8683=ORIENTED_EDGE ( 'NONE', *, *, #67515, .F. ) ;
#8687=CARTESIAN_POINT ( 'NONE',  ( -9.781776262117313436, -9.795823737882745519, 54.00000000000000711 ) ) ;
#8689=ORIENTED_EDGE ( 'NONE', *, *, #61233, .F. ) ;
#8719=CARTESIAN_POINT ( 'NONE',  ( 1.480523737882788238, -9.404523737882794165, 54.00000000000000711 ) ) ;
#8729=CARTESIAN_POINT ( 'NONE',  ( 2.544523737882812942, 9.722976262117210666, 26.00000000000000711 ) ) ;
#8730=ORIENTED_EDGE ( 'NONE', *, *, #35927, .T. ) ;
#8747=CARTESIAN_POINT ( 'NONE',  ( -6.486996718459931088, 3.142976262117182173, 54.00000000000000711 ) ) ;
#8751=ORIENTED_EDGE ( 'NONE', *, *, #53520, .F. ) ;
#8756=EDGE_CURVE ( 'NONE', #2123, #59802, #18786, .T. ) ;
#8764=DIRECTION ( 'NONE',  ( 1.836970198721029934E-16, 1.836970198721010706E-16, -1.000000000000000000 ) ) ;
#8772=ORIENTED_EDGE ( 'NONE', *, *, #11300, .T. ) ;
#8787=EDGE_CURVE ( 'NONE', #1825, #64092, #25151, .T. ) ;
#8803=EDGE_CURVE ( 'NONE', #17833, #51724, #20649, .T. ) ;
#8808=DIRECTION ( 'NONE',  ( -1.000000000000000000, 0.000000000000000000, 0.000000000000000000 ) ) ;
#8822=DIRECTION ( 'NONE',  ( -0.000000000000000000, 3.673940397442059868E-16, -1.000000000000000000 ) ) ;
#8827=DIRECTION ( 'NONE',  ( 1.000000000000000000, -6.308085367188447236E-15, -2.317552966102676720E-30 ) ) ;
#8828=ORIENTED_EDGE ( 'NONE', *, *, #8062, .T. ) ;
#8832=AXIS2_PLACEMENT_3D ( 'NONE', #6890, #18905, #45769 ) ;
#8835=LINE ( 'NONE', #67889, #33750 ) ;
#8846=ORIENTED_EDGE ( 'NONE', *, *, #40456, .T. ) ;
#8852=PLANE ( 'NONE',  #57231 ) ;
#8853=CARTESIAN_POINT ( 'NONE',  ( -9.547976262117304103, -7.969523737882760805, 54.00000000000000711 ) ) ;
#8857=CARTESIAN_POINT ( 'NONE',  ( -7.517976262117288755, -6.665817930929256008, 26.00000000000000000 ) ) ;
#8859=VERTEX_POINT ( 'NONE', #42102 ) ;
#8860=CARTESIAN_POINT ( 'NONE',  ( -6.835476262117330393, -10.50702373788278265, 26.00000000000000000 ) ) ;
#8861=ORIENTED_EDGE ( 'NONE', *, *, #6285, .F. ) ;
#8868=VERTEX_POINT ( 'NONE', #3934 ) ;
#8871=DIRECTION ( 'NONE',  ( 0.000000000000000000, -3.673940397442059868E-16, 1.000000000000000000 ) ) ;
#8878=VECTOR ( 'NONE', #41077, 1000.000000000000000 ) ;
#8884=EDGE_LOOP ( 'NONE', ( #24503, #58183, #25365, #6593 ) ) ;
#8885=ORIENTED_EDGE ( 'NONE', *, *, #69508, .T. ) ;
#8889=DIRECTION ( 'NONE',  ( 1.000000000000000000, 0.000000000000000000, 0.000000000000000000 ) ) ;
#8897=CARTESIAN_POINT ( 'NONE',  ( -2.406732575409590069, 8.697938382363036069, 26.00000000000000711 ) ) ;
#8898=ORIENTED_EDGE ( 'NONE', *, *, #50003, .T. ) ;
#8900=DIRECTION ( 'NONE',  ( -1.000000000000000000, 0.000000000000000000, 0.000000000000000000 ) ) ;
#8910=VERTEX_POINT ( 'NONE', #27580 ) ;
#8920=DIRECTION ( 'NONE',  ( 1.000000000000000000, 0.000000000000000000, 0.000000000000000000 ) ) ;
#8936=CARTESIAN_POINT ( 'NONE',  ( 4.149127210878726935, -6.836383711243002814, 54.00000000000000711 ) ) ;
#8937=ORIENTED_EDGE ( 'NONE', *, *, #67141, .T. ) ;
#8939=EDGE_LOOP ( 'NONE', ( #32461, #3615, #51696, #65233 ) ) ;
#8941=EDGE_CURVE ( 'NONE', #30522, #58172, #44872, .T. ) ;
#8943=CARTESIAN_POINT ( 'NONE',  ( 5.257023737882819070, -5.257023737882825287, 54.00000000000000711 ) ) ;
#8955=CIRCLE ( 'NONE', #1055, 0.3499999999999996447 ) ;
#8986=VECTOR ( 'NONE', #48005, 1000.000000000000114 ) ;
#9010=CIRCLE ( 'NONE', #10185, 1.224999999999998757 ) ;
#9018=CIRCLE ( 'NONE', #42898, 0.5249999999999994671 ) ;
#9021=ORIENTED_EDGE ( 'NONE', *, *, #69508, .F. ) ;
#9022=ORIENTED_EDGE ( 'NONE', *, *, #44084, .T. ) ;
#9024=VERTEX_POINT ( 'NONE', #22627 ) ;
#9033=EDGE_CURVE ( 'NONE', #33133, #28048, #64724, .T. ) ;
#9035=PLANE ( 'NONE',  #49330 ) ;
#9040=ORIENTED_EDGE ( 'NONE', *, *, #33081, .F. ) ;
#9052=CARTESIAN_POINT ( 'NONE',  ( -1.620245201994301665, 8.227189898828640935, 26.00000000000000711 ) ) ;
#9057=ORIENTED_EDGE ( 'NONE', *, *, #11824, .F. ) ;
#9058=EDGE_CURVE ( 'NONE', #21659, #26808, #61843, .T. ) ;
#9061=ADVANCED_FACE ( 'NONE', ( #46612 ), #40266, .F. ) ;
#9066=AXIS2_PLACEMENT_3D ( 'NONE', #54676, #6909, #38743 ) ;
#9068=CARTESIAN_POINT ( 'NONE',  ( 5.257023737882819070, -5.257023737882825287, 54.00000000000000711 ) ) ;
#9076=CIRCLE ( 'NONE', #14684, 0.1749999999999993783 ) ;
#9082=DIRECTION ( 'NONE',  ( -0.000000000000000000, -0.000000000000000000, -1.000000000000000000 ) ) ;
#9087=CIRCLE ( 'NONE', #52004, 0.3499999999999996447 ) ;
#9090=CARTESIAN_POINT ( 'NONE',  ( 6.836383711243002814, 6.350872789121261519, 54.00000000000000711 ) ) ;
#9091=CARTESIAN_POINT ( 'NONE',  ( -9.915476262117259409, 0.9414762621171833823, 26.00000000000000711 ) ) ;
#9092=ORIENTED_EDGE ( 'NONE', *, *, #4775, .F. ) ;
#9096=DIRECTION ( 'NONE',  ( 0.000000000000000000, 1.000000000000000000, 0.000000000000000000 ) ) ;
#9100=CARTESIAN_POINT ( 'NONE',  ( -7.342976262117273833, -4.961189459950004377, 54.00000000000000711 ) ) ;
#9103=AXIS2_PLACEMENT_3D ( 'NONE', #31246, #41128, #4379 ) ;
#9108=PLANE ( 'NONE',  #6938 ) ;
#9110=VERTEX_POINT ( 'NONE', #2093 ) ;
#9114=EDGE_CURVE ( 'NONE', #40740, #33225, #30166, .T. ) ;
#9123=DIRECTION ( 'NONE',  ( 1.836970198721029934E-16, 1.836970198721010706E-16, -1.000000000000000000 ) ) ;
#9132=EDGE_LOOP ( 'NONE', ( #63084, #58815, #69239, #14345 ) ) ;
#9138=FACE_OUTER_BOUND ( 'NONE', #26548, .T. ) ;
#9142=CARTESIAN_POINT ( 'NONE',  ( -2.355476262117229158, 9.547976262117156665, 54.00000000000000711 ) ) ;
#9145=VECTOR ( 'NONE', #44445, 1000.000000000000000 ) ;
#9146=DIRECTION ( 'NONE',  ( -1.000000000000000000, 0.000000000000000000, 0.000000000000000000 ) ) ;
#9161=ORIENTED_EDGE ( 'NONE', *, *, #28411, .F. ) ;
#9162=CARTESIAN_POINT ( 'NONE',  ( 6.501044194225450212, 3.142976262117187058, 54.00000000000000711 ) ) ;
#9165=CARTESIAN_POINT ( 'NONE',  ( 2.369523737882817116, 9.547976262117204627, 54.00000000000000711 ) ) ;
#9171=LINE ( 'NONE', #52307, #60525 ) ;
#9172=CARTESIAN_POINT ( 'NONE',  ( -6.350872789121327244, 6.822336235477381550, 26.00000000000000711 ) ) ;
#9176=VECTOR ( 'NONE', #26070, 1000.000000000000000 ) ;
#9177=CARTESIAN_POINT ( 'NONE',  ( -9.897976262117259338, 3.842976262117183683, 26.00000000000000711 ) ) ;
#9183=CIRCLE ( 'NONE', #23854, 0.1749999999999998224 ) ;
#9184=VECTOR ( 'NONE', #32770, 1000.000000000000000 ) ;
#9185=DIRECTION ( 'NONE',  ( 1.836970198721029934E-16, 1.836970198721010706E-16, -1.000000000000000000 ) ) ;
#9186=LINE ( 'NONE', #41349, #17388 ) ;
#9192=ORIENTED_EDGE ( 'NONE', *, *, #20583, .F. ) ;
#9196=ORIENTED_EDGE ( 'NONE', *, *, #52227, .T. ) ;
#9198=DIRECTION ( 'NONE',  ( -3.491481338843133355E-15, -1.000000000000000000, 0.000000000000000000 ) ) ;
#9207=EDGE_CURVE ( 'NONE', #7648, #14823, #65214, .T. ) ;
#9210=ORIENTED_EDGE ( 'NONE', *, *, #36412, .F. ) ;
#9214=EDGE_CURVE ( 'NONE', #5750, #19510, #29044, .T. ) ;
#9220=VERTEX_POINT ( 'NONE', #42020 ) ;
#9224=LINE ( 'NONE', #13818, #60390 ) ;
#9225=AXIS2_PLACEMENT_3D ( 'NONE', #15257, #3595, #46026 ) ;
#9228=ORIENTED_EDGE ( 'NONE', *, *, #37499, .F. ) ;
#9231=CARTESIAN_POINT ( 'NONE',  ( 4.046023737882819660, -3.157023737882826087, 54.00000000000000711 ) ) ;
#9233=CIRCLE ( 'NONE', #36327, 0.1749999999999989342 ) ;
#9266=CARTESIAN_POINT ( 'NONE',  ( 9.929523737882751888, 0.9414762621171479662, 54.00000000000000711 ) ) ;
#9268=CIRCLE ( 'NONE', #61171, 0.3499999999999996447 ) ;
#9271=VECTOR ( 'NONE', #36377, 1000.000000000000000 ) ;
#9283=VERTEX_POINT ( 'NONE', #68899 ) ;
#9289=ORIENTED_EDGE ( 'NONE', *, *, #58903, .T. ) ;
#9290=CYLINDRICAL_SURFACE ( 'NONE', #37154, 0.5249999999999990230 ) ;
#9302=VERTEX_POINT ( 'NONE', #25411 ) ;
#9312=VERTEX_POINT ( 'NONE', #47673 ) ;
#9313=PLANE ( 'NONE',  #9103 ) ;
#9316=CARTESIAN_POINT ( 'NONE',  ( -7.955476262117324282, -9.562023737882771712, 54.00000000000000711 ) ) ;
#9326=CARTESIAN_POINT ( 'NONE',  ( 4.149127210878725158, 6.822336235477391320, 54.00000000000000711 ) ) ;
#9329=ORIENTED_EDGE ( 'NONE', *, *, #49906, .T. ) ;
#9330=EDGE_LOOP ( 'NONE', ( #38935, #7194, #6185, #64805 ) ) ;
#9338=DIRECTION ( 'NONE',  ( -1.836970198721029934E-16, 1.836970198721036344E-16, -1.000000000000000000 ) ) ;
#9339=CARTESIAN_POINT ( 'NONE',  ( 8.711985858128693749, -8.093267424590459669, 26.00000000000000000 ) ) ;
#9345=CARTESIAN_POINT ( 'NONE',  ( 3.848229544836323512, -7.357023737882811609, 54.00000000000000711 ) ) ;
#9348=ORIENTED_EDGE ( 'NONE', *, *, #44380, .F. ) ;
#9354=EDGE_LOOP ( 'NONE', ( #52981, #17790, #56277, #21850 ) ) ;
#9360=ORIENTED_EDGE ( 'NONE', *, *, #37564, .F. ) ;
#9368=LINE ( 'NONE', #20326, #49758 ) ;
#9375=ORIENTED_EDGE ( 'NONE', *, *, #43440, .F. ) ;
#9385=EDGE_CURVE ( 'NONE', #29039, #16772, #68637, .T. ) ;
#9398=VERTEX_POINT ( 'NONE', #27496 ) ;
#9403=DIRECTION ( 'NONE',  ( -3.304235192336778667E-15, -1.000000000000000000, 0.000000000000000000 ) ) ;
#9404=VERTEX_POINT ( 'NONE', #10890 ) ;
#9405=LINE ( 'NONE', #37335, #21001 ) ;
#9414=VECTOR ( 'NONE', #21149, 1000.000000000000000 ) ;
#9415=DIRECTION ( 'NONE',  ( 0.6414496315691592399, 0.7671651518152985405, 2.309356642088728176E-17 ) ) ;
#9417=CARTESIAN_POINT ( 'NONE',  ( -2.530476262117229425, 9.547976262117158441, 54.00000000000000711 ) ) ;
#9420=ORIENTED_EDGE ( 'NONE', *, *, #51400, .T. ) ;
#9428=CARTESIAN_POINT ( 'NONE',  ( 6.665817930929297752, -7.357023737882824044, 54.00000000000000711 ) ) ;
#9429=DIRECTION ( 'NONE',  ( -1.901462112903059913E-14, -1.000000000000000000, 0.000000000000000000 ) ) ;
#9433=DIRECTION ( 'NONE',  ( -1.836970198721029934E-16, -1.836970198721010706E-16, 1.000000000000000000 ) ) ;
#9445=CARTESIAN_POINT ( 'NONE',  ( -7.342976262117247188, -3.848229544836283100, 26.00000000000000711 ) ) ;
#9450=DIRECTION ( 'NONE',  ( 1.836970198721029934E-16, -1.836970198721036344E-16, 1.000000000000000000 ) ) ;
#9453=ORIENTED_EDGE ( 'NONE', *, *, #12936, .F. ) ;
#9459=ORIENTED_EDGE ( 'NONE', *, *, #47053, .F. ) ;
#9467=LINE ( 'NONE', #62858, #5766 ) ;
#9468=EDGE_CURVE ( 'NONE', #41511, #69896, #29918, .T. ) ;
#9469=EDGE_LOOP ( 'NONE', ( #48990, #55312, #11434, #52614 ) ) ;
#9480=ORIENTED_EDGE ( 'NONE', *, *, #2593, .F. ) ;
#9484=CARTESIAN_POINT ( 'NONE',  ( 9.404523737882817258, -1.480523737882825985, 54.00000000000000711 ) ) ;
#9487=VECTOR ( 'NONE', #33523, 1000.000000000000000 ) ;
#9493=DIRECTION ( 'NONE',  ( -0.000000000000000000, -0.000000000000000000, -1.000000000000000000 ) ) ;
#9495=EDGE_CURVE ( 'NONE', #28592, #54687, #17913, .T. ) ;
#9498=AXIS2_PLACEMENT_3D ( 'NONE', #31080, #69613, #21509 ) ;
#9499=VECTOR ( 'NONE', #56930, 1000.000000000000000 ) ;
#9517=DIRECTION ( 'NONE',  ( 0.7071067811865550112, 0.7071067811865401342, 0.000000000000000000 ) ) ;
#9527=LINE ( 'NONE', #4924, #61199 ) ;
#9528=EDGE_CURVE ( 'NONE', #46314, #62186, #17953, .T. ) ;
#9537=FACE_OUTER_BOUND ( 'NONE', #13997, .T. ) ;
#9543=CIRCLE ( 'NONE', #52447, 0.1750000000000002387 ) ;
#9555=ORIENTED_EDGE ( 'NONE', *, *, #62482, .F. ) ;
#9558=EDGE_CURVE ( 'NONE', #5287, #10010, #55224, .T. ) ;
#9561=ADVANCED_FACE ( 'NONE', ( #37954 ), #42554, .F. ) ;
#9566=ORIENTED_EDGE ( 'NONE', *, *, #24675, .F. ) ;
#9570=DIRECTION ( 'NONE',  ( -1.836970198721029934E-16, 1.836970198721036590E-16, -1.000000000000000000 ) ) ;
#9579=CARTESIAN_POINT ( 'NONE',  ( -6.651770455163775964, -7.357023737882784964, 26.00000000000000000 ) ) ;
#9582=ORIENTED_EDGE ( 'NONE', *, *, #5685, .F. ) ;
#9592=DIRECTION ( 'NONE',  ( -1.000000000000000000, 0.000000000000000000, 0.000000000000000000 ) ) ;
#9598=CIRCLE ( 'NONE', #46830, 0.1749999999999998224 ) ;
#9606=ADVANCED_FACE ( 'NONE', ( #42899 ), #21687, .T. ) ;
#9611=LINE ( 'NONE', #47428, #51442 ) ;
#9626=CARTESIAN_POINT ( 'NONE',  ( -4.135079735113215804, -6.836383711243002814, 54.00000000000000711 ) ) ;
#9630=ORIENTED_EDGE ( 'NONE', *, *, #22521, .F. ) ;
#9631=CARTESIAN_POINT ( 'NONE',  ( 1.634292677759859869, -8.241237374594282628, 54.00000000000000711 ) ) ;
#9638=VERTEX_POINT ( 'NONE', #64823 ) ;
#9640=LINE ( 'NONE', #41805, #50966 ) ;
#9659=ORIENTED_EDGE ( 'NONE', *, *, #50818, .F. ) ;
#9664=LINE ( 'NONE', #31238, #38906 ) ;
#9684=AXIS2_PLACEMENT_3D ( 'NONE', #37086, #47681, #37773 ) ;
#9720=EDGE_LOOP ( 'NONE', ( #51170, #29471, #65429, #11021 ) ) ;
#9721=LINE ( 'NONE', #62387, #8442 ) ;
#9731=DIRECTION ( 'NONE',  ( -1.000000000000000000, 0.000000000000000000, 0.000000000000000000 ) ) ;
#9734=EDGE_CURVE ( 'NONE', #9638, #45723, #6467, .T. ) ;
#9735=ADVANCED_FACE ( 'NONE', ( #28361 ), #23755, .F. ) ;
#9737=DIRECTION ( 'NONE',  ( -3.491481338843133355E-15, -1.000000000000000000, -1.836970198721029934E-16 ) ) ;
#9739=VECTOR ( 'NONE', #65967, 1000.000000000000000 ) ;
#9742=EDGE_CURVE ( 'NONE', #65973, #34373, #6788, .T. ) ;
#9753=LINE ( 'NONE', #64201, #24 ) ;
#9756=VECTOR ( 'NONE', #348, 1000.000000000000000 ) ;
#9769=DIRECTION ( 'NONE',  ( -0.000000000000000000, -0.000000000000000000, -1.000000000000000000 ) ) ;
#9773=CARTESIAN_POINT ( 'NONE',  ( 6.364920264886885448, -6.836383711243021466, 54.00000000000000711 ) ) ;
#9774=ORIENTED_EDGE ( 'NONE', *, *, #16425, .F. ) ;
#9778=EDGE_CURVE ( 'NONE', #67923, #22000, #39656, .T. ) ;
#9781=ORIENTED_EDGE ( 'NONE', *, *, #28508, .T. ) ;
#9785=EDGE_CURVE ( 'NONE', #62156, #1825, #61213, .T. ) ;
#9791=DIRECTION ( 'NONE',  ( -0.000000000000000000, -0.000000000000000000, -1.000000000000000000 ) ) ;
#9797=EDGE_CURVE ( 'NONE', #14276, #52784, #62640, .T. ) ;
#9800=VECTOR ( 'NONE', #62924, 1000.000000000000000 ) ;
#9820=DIRECTION ( 'NONE',  ( 0.000000000000000000, 0.000000000000000000, 1.000000000000000000 ) ) ;
#9823=CARTESIAN_POINT ( 'NONE',  ( -7.172176262117259782, 5.242976262117182706, 54.00000000000000711 ) ) ;
#9827=ORIENTED_EDGE ( 'NONE', *, *, #28657, .T. ) ;
#9829=VERTEX_POINT ( 'NONE', #22720 ) ;
#9831=DIRECTION ( 'NONE',  ( 0.6414496315691592399, 0.7671651518152985405, 2.309356642088728176E-17 ) ) ;
#9832=CARTESIAN_POINT ( 'NONE',  ( 7.969523737882818537, -8.835729544836345539, 54.00000000000000711 ) ) ;
#9835=DIRECTION ( 'NONE',  ( -0.000000000000000000, -0.000000000000000000, -1.000000000000000000 ) ) ;
#9837=CARTESIAN_POINT ( 'NONE',  ( 4.961189459950046121, 7.342976262117201003, 54.00000000000000711 ) ) ;
#9848=LINE ( 'NONE', #15833, #69233 ) ;
#9849=VERTEX_POINT ( 'NONE', #7482 ) ;
#9850=VECTOR ( 'NONE', #1239, 1000.000000000000000 ) ;
#9854=ADVANCED_FACE ( 'NONE', ( #65848 ), #28030, .F. ) ;
#9885=ORIENTED_EDGE ( 'NONE', *, *, #31572, .F. ) ;
#9901=AXIS2_PLACEMENT_3D ( 'NONE', #20926, #19878, #42501 ) ;
#9902=AXIS2_PLACEMENT_3D ( 'NONE', #55240, #38298, #54561 ) ;
#9921=DIRECTION ( 'NONE',  ( 0.5000000000000004441, -0.8660254037844383745, 0.000000000000000000 ) ) ;
#9928=CARTESIAN_POINT ( 'NONE',  ( 9.562023737882805463, 7.955476262117186614, 54.00000000000000711 ) ) ;
#9929=EDGE_LOOP ( 'NONE', ( #27010, #4634, #16851, #54201 ) ) ;
#9934=ADVANCED_FACE ( 'NONE', ( #3239 ), #47077, .F. ) ;
#9940=DIRECTION ( 'NONE',  ( 0.000000000000000000, 0.000000000000000000, 1.000000000000000000 ) ) ;
#9942=EDGE_CURVE ( 'NONE', #4880, #4176, #3594, .T. ) ;
#9943=ORIENTED_EDGE ( 'NONE', *, *, #59637, .F. ) ;
#9954=LINE ( 'NONE', #3942, #47630 ) ;
#9958=CARTESIAN_POINT ( 'NONE',  ( 7.969523737882818537, -9.737023737882820384, 54.00000000000000711 ) ) ;
#9960=CARTESIAN_POINT ( 'NONE',  ( 2.369523737882786918, -9.562023737882787700, 26.00000000000000000 ) ) ;
#9975=DIRECTION ( 'NONE',  ( -0.6414496315691446959, -0.7671651518153106419, -2.818519042764040589E-16 ) ) ;
#9976=ORIENTED_EDGE ( 'NONE', *, *, #58468, .F. ) ;
#9977=DIRECTION ( 'NONE',  ( 8.612436249475772606E-15, 1.000000000000000000, 0.000000000000000000 ) ) ;
#9982=DIRECTION ( 'NONE',  ( -0.7671651518153105309, -0.6414496315691445849, 0.000000000000000000 ) ) ;
#9987=ORIENTED_EDGE ( 'NONE', *, *, #48821, .T. ) ;
#9995=CYLINDRICAL_SURFACE ( 'NONE', #11450, 1.929199999999998916 ) ;
#10010=VERTEX_POINT ( 'NONE', #9958 ) ;
#10017=DIRECTION ( 'NONE',  ( 1.000000000000000000, 0.000000000000000000, 0.000000000000000000 ) ) ;
#10020=ORIENTED_EDGE ( 'NONE', *, *, #36107, .F. ) ;
#10021=DIRECTION ( 'NONE',  ( 1.047444401652940007E-14, 1.000000000000000000, 1.836970198721029934E-16 ) ) ;
#10034=ORIENTED_EDGE ( 'NONE', *, *, #12668, .F. ) ;
#10035=ORIENTED_EDGE ( 'NONE', *, *, #15845, .F. ) ;
#10036=DIRECTION ( 'NONE',  ( -1.000000000000000000, 0.000000000000000000, 0.000000000000000000 ) ) ;
#10039=FACE_OUTER_BOUND ( 'NONE', #24448, .T. ) ;
#10040=CIRCLE ( 'NONE', #36011, 1.929199999999998028 ) ;
#10041=DIRECTION ( 'NONE',  ( 0.000000000000000000, -1.000000000000000000, -3.673940397442060361E-16 ) ) ;
#10044=CARTESIAN_POINT ( 'NONE',  ( -9.722976262117258628, 3.667976262117184749, 54.00000000000000711 ) ) ;
#10047=ORIENTED_EDGE ( 'NONE', *, *, #19656, .T. ) ;
#10053=CIRCLE ( 'NONE', #1014, 1.929199999999997139 ) ;
#10055=ORIENTED_EDGE ( 'NONE', *, *, #9214, .F. ) ;
#10057=CARTESIAN_POINT ( 'NONE',  ( 5.257023737882795977, 5.242976262117205799, 26.00000000000000711 ) ) ;
#10062=DIRECTION ( 'NONE',  ( -1.836970198721029934E-16, 1.836970198721036344E-16, -1.000000000000000000 ) ) ;
#10063=DIRECTION ( 'NONE',  ( -0.000000000000000000, -0.000000000000000000, -1.000000000000000000 ) ) ;
#10086=EDGE_LOOP ( 'NONE', ( #63830, #61491, #16540, #45743 ) ) ;
#10095=CARTESIAN_POINT ( 'NONE',  ( 5.257023737882819070, -5.257023737882825287, 54.00000000000000711 ) ) ;
#10098=ORIENTED_EDGE ( 'NONE', *, *, #29216, .F. ) ;
#10099=AXIS2_PLACEMENT_3D ( 'NONE', #64834, #16385, #37962 ) ;
#10111=CYLINDRICAL_SURFACE ( 'NONE', #55022, 0.1749999999999998224 ) ;
#10119=CARTESIAN_POINT ( 'NONE',  ( 4.149127210878726935, -6.836383711243002814, 54.00000000000000711 ) ) ;
#10127=CARTESIAN_POINT ( 'NONE',  ( -2.355476262117319308, -8.835729544836356197, 54.00000000000000711 ) ) ;
#10130=FACE_OUTER_BOUND ( 'NONE', #47731, .T. ) ;
#10136=DIRECTION ( 'NONE',  ( 0.7071067811865513475, 0.7071067811865435759, 0.000000000000000000 ) ) ;
#10140=CARTESIAN_POINT ( 'NONE',  ( -6.775514141871385121, 7.394232575409538377, 54.00000000000000711 ) ) ;
#10141=LINE ( 'NONE', #31720, #4826 ) ;
#10150=AXIS2_PLACEMENT_3D ( 'NONE', #42923, #33013, #11097 ) ;
#10151=ORIENTED_EDGE ( 'NONE', *, *, #36935, .T. ) ;
#10152=CARTESIAN_POINT ( 'NONE',  ( -7.955476262117259445, 9.722976262117178692, 54.00000000000000711 ) ) ;
#10154=ORIENTED_EDGE ( 'NONE', *, *, #66172, .F. ) ;
#10160=ORIENTED_EDGE ( 'NONE', *, *, #30172, .T. ) ;
#10161=VERTEX_POINT ( 'NONE', #39571 ) ;
#10173=DIRECTION ( 'NONE',  ( -0.000000000000000000, -0.000000000000000000, -1.000000000000000000 ) ) ;
#10179=ORIENTED_EDGE ( 'NONE', *, *, #53802, .F. ) ;
#10180=AXIS2_PLACEMENT_3D ( 'NONE', #68650, #57329, #34704 ) ;
#10185=AXIS2_PLACEMENT_3D ( 'NONE', #67108, #61095, #13715 ) ;
#10194=ORIENTED_EDGE ( 'NONE', *, *, #12682, .T. ) ;
#10196=CARTESIAN_POINT ( 'NONE',  ( 7.532023737882806103, 6.651770455163672047, 54.00000000000000711 ) ) ;
#10200=VERTEX_POINT ( 'NONE', #22637 ) ;
#10203=CARTESIAN_POINT ( 'NONE',  ( -9.689726262117325462, -9.703773737882725570, 54.00000000000000711 ) ) ;
#10207=ORIENTED_EDGE ( 'NONE', *, *, #37191, .F. ) ;
#10211=DIRECTION ( 'NONE',  ( 1.836970198721029934E-16, 1.836970198721010706E-16, -1.000000000000000000 ) ) ;
#10218=DIRECTION ( 'NONE',  ( -0.7071067811865503483, -0.7071067811865446862, 0.000000000000000000 ) ) ;
#10223=AXIS2_PLACEMENT_3D ( 'NONE', #58469, #58809, #68363 ) ;
#10224=LINE ( 'NONE', #31803, #8878 ) ;
#10231=ORIENTED_EDGE ( 'NONE', *, *, #13677, .F. ) ;
#10242=ORIENTED_EDGE ( 'NONE', *, *, #32117, .T. ) ;
#10245=VERTEX_POINT ( 'NONE', #44188 ) ;
#10246=VECTOR ( 'NONE', #21282, 1000.000000000000000 ) ;
#10252=ORIENTED_EDGE ( 'NONE', *, *, #53513, .F. ) ;
#10254=ORIENTED_EDGE ( 'NONE', *, *, #16191, .F. ) ;
#10274=DIRECTION ( 'NONE',  ( -1.000000000000000000, 0.000000000000000000, 0.000000000000000000 ) ) ;
#10285=CIRCLE ( 'NONE', #18135, 0.5249999999999994671 ) ;
#10286=ORIENTED_EDGE ( 'NONE', *, *, #28527, .T. ) ;
#10289=ADVANCED_FACE ( 'NONE', ( #16653 ), #38557, .F. ) ;
#10302=ADVANCED_FACE ( 'NONE', ( #24011 ), #30728, .F. ) ;
#10311=AXIS2_PLACEMENT_3D ( 'NONE', #61480, #62536, #8090 ) ;
#10314=ORIENTED_EDGE ( 'NONE', *, *, #26422, .F. ) ;
#10321=LINE ( 'NONE', #9626, #61397 ) ;
#10329=LINE ( 'NONE', #31903, #13300 ) ;
#10335=LINE ( 'NONE', #6074, #62262 ) ;
#10340=ORIENTED_EDGE ( 'NONE', *, *, #2056, .F. ) ;
#10341=ADVANCED_FACE ( 'NONE', ( #35304 ), #14470, .F. ) ;
#10348=CARTESIAN_POINT ( 'NONE',  ( -3.663616288757055806, 6.350872789121238426, 54.00000000000000711 ) ) ;
#10352=ORIENTED_EDGE ( 'NONE', *, *, #37891, .F. ) ;
#10353=EDGE_LOOP ( 'NONE', ( #42863, #10231, #38646, #6032 ) ) ;
#10363=VERTEX_POINT ( 'NONE', #29662 ) ;
#10367=ORIENTED_EDGE ( 'NONE', *, *, #29531, .F. ) ;
#10380=VERTEX_POINT ( 'NONE', #35664 ) ;
#10384=DIRECTION ( 'NONE',  ( 0.000000000000000000, 1.000000000000000000, 0.000000000000000000 ) ) ;
#10407=DIRECTION ( 'NONE',  ( -0.7671651518152895477, 0.6414496315691698980, -2.309356642088442522E-17 ) ) ;
#10409=EDGE_LOOP ( 'NONE', ( #55998, #51087, #40356, #68383 ) ) ;
#10415=CARTESIAN_POINT ( 'NONE',  ( 6.358413763958960629, 5.779227145995223580, 54.00000000000000711 ) ) ;
#10426=EDGE_LOOP ( 'NONE', ( #3999, #7416, #55145, #46573 ) ) ;
#10428=DIRECTION ( 'NONE',  ( -0.000000000000000000, 3.673940397442059868E-16, -1.000000000000000000 ) ) ;
#10437=EDGE_CURVE ( 'NONE', #59528, #33844, #47336, .T. ) ;
#10439=ORIENTED_EDGE ( 'NONE', *, *, #4812, .T. ) ;
#10441=ORIENTED_EDGE ( 'NONE', *, *, #29304, .T. ) ;
#10451=CARTESIAN_POINT ( 'NONE',  ( 9.737023737882815055, -7.969523737882814984, 26.00000000000000000 ) ) ;
#10456=DIRECTION ( 'NONE',  ( -1.000000000000000000, 0.000000000000000000, 0.000000000000000000 ) ) ;
#10457=CIRCLE ( 'NONE', #56779, 0.5249999999999990230 ) ;
#10460=EDGE_CURVE ( 'NONE', #13296, #61211, #13976, .T. ) ;
#10464=ORIENTED_EDGE ( 'NONE', *, *, #52986, .F. ) ;
#10475=EDGE_CURVE ( 'NONE', #8148, #18538, #48387, .T. ) ;
#10478=CARTESIAN_POINT ( 'NONE',  ( 2.544523737882792069, -8.835729544836313565, 26.00000000000000000 ) ) ;
#10483=PLANE ( 'NONE',  #54528 ) ;
#10488=DIRECTION ( 'NONE',  ( 1.836970198721029934E-16, 1.836970198721010706E-16, -1.000000000000000000 ) ) ;
#10491=CARTESIAN_POINT ( 'NONE',  ( -6.651770455163781293, -7.357023737882790293, 54.00000000000000711 ) ) ;
#10492=PLANE ( 'NONE',  #57682 ) ;
#10493=ORIENTED_EDGE ( 'NONE', *, *, #26422, .T. ) ;
#10498=VERTEX_POINT ( 'NONE', #26831 ) ;
#10520=LINE ( 'NONE', #59307, #37226 ) ;
#10534=ORIENTED_EDGE ( 'NONE', *, *, #45684, .F. ) ;
#10538=VERTEX_POINT ( 'NONE', #15529 ) ;
#10552=LINE ( 'NONE', #21512, #287 ) ;
#10554=DIRECTION ( 'NONE',  ( 0.7071067811865474617, -0.7071067811865474617, 0.000000000000000000 ) ) ;
#10560=EDGE_CURVE ( 'NONE', #42109, #57811, #17922, .T. ) ;
#10562=DIRECTION ( 'NONE',  ( -0.6414496315691617934, 0.7671651518152962090, 0.000000000000000000 ) ) ;
#10566=EDGE_CURVE ( 'NONE', #55087, #14072, #12608, .T. ) ;
#10576=CARTESIAN_POINT ( 'NONE',  ( -10.49297626211729018, -6.849523737882743823, 26.00000000000000000 ) ) ;
#10577=DIRECTION ( 'NONE',  ( 1.000000000000000000, 0.000000000000000000, 0.000000000000000000 ) ) ;
#10578=CARTESIAN_POINT ( 'NONE',  ( -6.822336235477446387, 4.135079735113101229, 26.00000000000000711 ) ) ;
#10586=DIRECTION ( 'NONE',  ( -1.000000000000000000, 0.000000000000000000, 0.000000000000000000 ) ) ;
#10598=DIRECTION ( 'NONE',  ( -9.912705577010336396E-15, -1.000000000000000000, 0.000000000000000000 ) ) ;
#10599=ORIENTED_EDGE ( 'NONE', *, *, #41014, .T. ) ;
#10600=EDGE_CURVE ( 'NONE', #14190, #15650, #11570, .T. ) ;
#10601=DIRECTION ( 'NONE',  ( -4.956352788505180820E-15, -1.000000000000000000, 0.000000000000000000 ) ) ;
#10606=ORIENTED_EDGE ( 'NONE', *, *, #4289, .T. ) ;
#10612=CIRCLE ( 'NONE', #7155, 0.1749999999999980738 ) ;
#10613=CARTESIAN_POINT ( 'NONE',  ( 9.929523737882817613, -0.9555237378828154160, 26.00000000000000711 ) ) ;
#10615=EDGE_LOOP ( 'NONE', ( #11225, #8264, #59351, #60070 ) ) ;
#10623=EDGE_CURVE ( 'NONE', #61120, #68364, #5601, .T. ) ;
#10639=EDGE_LOOP ( 'NONE', ( #15822, #40608, #5220, #13971 ) ) ;
#10642=DIRECTION ( 'NONE',  ( 0.6414496315691617934, 0.7671651518152962090, -0.000000000000000000 ) ) ;
#10647=AXIS2_PLACEMENT_3D ( 'NONE', #48532, #37585, #59491 ) ;
#10649=EDGE_CURVE ( 'NONE', #24983, #30361, #59689, .T. ) ;
#10656=ORIENTED_EDGE ( 'NONE', *, *, #45022, .F. ) ;
#10657=LINE ( 'NONE', #36126, #36537 ) ;
#10659=ORIENTED_EDGE ( 'NONE', *, *, #11399, .F. ) ;
#10662=EDGE_CURVE ( 'NONE', #48157, #35812, #11917, .T. ) ;
#10670=ORIENTED_EDGE ( 'NONE', *, *, #4469, .T. ) ;
#10672=CARTESIAN_POINT ( 'NONE',  ( 6.836383711243002814, 6.350872789121261519, 54.00000000000000711 ) ) ;
#10673=DIRECTION ( 'NONE',  ( -1.836970198721029934E-16, -1.836970198721010706E-16, 1.000000000000000000 ) ) ;
#10692=ORIENTED_EDGE ( 'NONE', *, *, #15102, .F. ) ;
#10709=VERTEX_POINT ( 'NONE', #5942 ) ;
#10726=DIRECTION ( 'NONE',  ( 0.000000000000000000, 3.673940397442059868E-16, -1.000000000000000000 ) ) ;
#10735=CARTESIAN_POINT ( 'NONE',  ( 8.144523737882810366, 9.547976262117190416, 26.00000000000000711 ) ) ;
#10743=VECTOR ( 'NONE', #38864, 1000.000000000000000 ) ;
#10744=ORIENTED_EDGE ( 'NONE', *, *, #45734, .T. ) ;
#10747=ORIENTED_EDGE ( 'NONE', *, *, #10662, .T. ) ;
#10751=VERTEX_POINT ( 'NONE', #61761 ) ;
#10752=DIRECTION ( 'NONE',  ( -1.836970198721029934E-16, 1.836970198721036590E-16, -1.000000000000000000 ) ) ;
#10759=ORIENTED_EDGE ( 'NONE', *, *, #36646, .F. ) ;
#10763=CARTESIAN_POINT ( 'NONE',  ( 6.836383711242975281, 4.135079735113102117, 54.00000000000000711 ) ) ;
#10764=ORIENTED_EDGE ( 'NONE', *, *, #30831, .T. ) ;
#10770=ADVANCED_FACE ( 'NONE', ( #18619 ), #28875, .F. ) ;
#10780=EDGE_CURVE ( 'NONE', #13545, #38341, #24642, .T. ) ;
#10788=DIRECTION ( 'NONE',  ( -0.000000000000000000, -0.000000000000000000, -1.000000000000000000 ) ) ;
#10796=EDGE_CURVE ( 'NONE', #55278, #37989, #8004, .T. ) ;
#10797=ORIENTED_EDGE ( 'NONE', *, *, #1650, .T. ) ;
#10798=EDGE_CURVE ( 'NONE', #15964, #52649, #24285, .T. ) ;
#10801=EDGE_CURVE ( 'NONE', #39506, #3304, #56451, .T. ) ;
#10808=EDGE_CURVE ( 'NONE', #15214, #54732, #40886, .T. ) ;
#10810=DIRECTION ( 'NONE',  ( -0.000000000000000000, 3.673940397442059868E-16, -1.000000000000000000 ) ) ;
#10811=CARTESIAN_POINT ( 'NONE',  ( -6.486996718459903555, -2.632023737882784431, 54.00000000000000711 ) ) ;
#10812=ORIENTED_EDGE ( 'NONE', *, *, #44084, .F. ) ;
#10818=DIRECTION ( 'NONE',  ( 9.799566706031580591E-15, 1.000000000000000000, 1.836970198721018348E-16 ) ) ;
#10819=DIRECTION ( 'NONE',  ( 1.000000000000000000, -3.491481338843133355E-15, -1.836970198721036344E-16 ) ) ;
#10821=LINE ( 'NONE', #20733, #56981 ) ;
#10828=DIRECTION ( 'NONE',  ( -0.000000000000000000, -0.000000000000000000, -1.000000000000000000 ) ) ;
#10830=ORIENTED_EDGE ( 'NONE', *, *, #36927, .T. ) ;
#10831=CARTESIAN_POINT ( 'NONE',  ( 10.05377373788278739, -8.930623737882855906, 54.00000000000000711 ) ) ;
#10841=VECTOR ( 'NONE', #67441, 1000.000000000000000 ) ;
#10845=FACE_OUTER_BOUND ( 'NONE', #6283, .T. ) ;
#10846=ORIENTED_EDGE ( 'NONE', *, *, #9785, .F. ) ;
#10850=AXIS2_PLACEMENT_3D ( 'NONE', #24689, #28936, #28587 ) ;
#10855=VERTEX_POINT ( 'NONE', #4479 ) ;
#10858=ORIENTED_EDGE ( 'NONE', *, *, #42880, .F. ) ;
#10861=DIRECTION ( 'NONE',  ( 1.000000000000000000, -3.491481338843133355E-15, -1.836970198721036590E-16 ) ) ;
#10864=ORIENTED_EDGE ( 'NONE', *, *, #41442, .T. ) ;
#10866=VECTOR ( 'NONE', #3870, 1000.000000000000000 ) ;
#10887=CARTESIAN_POINT ( 'NONE',  ( 8.093267424590464998, -8.711985858128690197, 26.00000000000000000 ) ) ;
#10890=CARTESIAN_POINT ( 'NONE',  ( -0.9414762621172249046, 9.915476262117151052, 26.00000000000000711 ) ) ;
#10897=DIRECTION ( 'NONE',  ( -0.7071067811865451302, 0.7071067811865500152, 2.597868168706484541E-16 ) ) ;
#10905=DIRECTION ( 'NONE',  ( -1.836970198721029934E-16, -1.836970198721010706E-16, 1.000000000000000000 ) ) ;
#10906=LINE ( 'NONE', #49077, #44918 ) ;
#10910=ORIENTED_EDGE ( 'NONE', *, *, #4902, .T. ) ;
#10911=PLANE ( 'NONE',  #27899 ) ;
#10912=LINE ( 'NONE', #63264, #32743 ) ;
#10918=LINE ( 'NONE', #43426, #22296 ) ;
#10928=CARTESIAN_POINT ( 'NONE',  ( -6.642976262117329611, -10.31452373788278365, 26.00000000000000000 ) ) ;
#10933=ORIENTED_EDGE ( 'NONE', *, *, #41463, .T. ) ;
#10936=AXIS2_PLACEMENT_3D ( 'NONE', #64076, #20912, #8900 ) ;
#10947=VERTEX_POINT ( 'NONE', #31364 ) ;
#10951=VECTOR ( 'NONE', #27243, 1000.000000000000227 ) ;
#10954=CARTESIAN_POINT ( 'NONE',  ( 3.157023737882797665, 4.031976262117209053, 54.00000000000000711 ) ) ;
#10965=VERTEX_POINT ( 'NONE', #68473 ) ;
#10967=VECTOR ( 'NONE', #63599, 1000.000000000000114 ) ;
#10994=CARTESIAN_POINT ( 'NONE',  ( -5.242976262117259978, 5.242976262117182706, 54.00000000000000711 ) ) ;
#10999=EDGE_LOOP ( 'NONE', ( #12335, #17292, #67496, #61988 ) ) ;
#11007=CARTESIAN_POINT ( 'NONE',  ( 3.157023737882819425, -4.046023737882825877, 54.00000000000000711 ) ) ;
#11015=ADVANCED_FACE ( 'NONE', ( #51036 ), #40781, .F. ) ;
#11018=CARTESIAN_POINT ( 'NONE',  ( -4.135079735113203370, -3.677663764522608236, 26.00000000000000711 ) ) ;
#11020=VECTOR ( 'NONE', #15082, 1000.000000000000000 ) ;
#11021=ORIENTED_EDGE ( 'NONE', *, *, #25663, .T. ) ;
#11023=VERTEX_POINT ( 'NONE', #35822 ) ;
#11026=LINE ( 'NONE', #779, #66984 ) ;
#11042=ORIENTED_EDGE ( 'NONE', *, *, #66476, .F. ) ;
#11052=EDGE_CURVE ( 'NONE', #36149, #1729, #7550, .T. ) ;
#11062=EDGE_CURVE ( 'NONE', #42883, #29241, #3783, .T. ) ;
#11063=DIRECTION ( 'NONE',  ( -1.000000000000000000, -3.016910393003147986E-15, -0.000000000000000000 ) ) ;
#11072=VECTOR ( 'NONE', #4053, 1000.000000000000000 ) ;
#11096=ORIENTED_EDGE ( 'NONE', *, *, #3004, .T. ) ;
#11097=DIRECTION ( 'NONE',  ( 1.920292680692490463E-14, 1.000000000000000000, 0.000000000000000000 ) ) ;
#11098=CARTESIAN_POINT ( 'NONE',  ( 2.544523737882818271, 9.722976262117205337, 54.00000000000000711 ) ) ;
#11108=EDGE_CURVE ( 'NONE', #6666, #18538, #48534, .T. ) ;
#11110=ORIENTED_EDGE ( 'NONE', *, *, #49906, .F. ) ;
#11119=PLANE ( 'NONE',  #46560 ) ;
#11128=EDGE_LOOP ( 'NONE', ( #16297, #37636, #28196, #33217 ) ) ;
#11131=ORIENTED_EDGE ( 'NONE', *, *, #43886, .T. ) ;
#11141=EDGE_CURVE ( 'NONE', #22435, #19590, #4707, .T. ) ;
#11146=VERTEX_POINT ( 'NONE', #37238 ) ;
#11151=FACE_BOUND ( 'NONE', #55952, .T. ) ;
#11154=CYLINDRICAL_SURFACE ( 'NONE', #57317, 0.5249999999999985789 ) ;
#11157=CARTESIAN_POINT ( 'NONE',  ( -2.989207322240228226, -6.872275254348431339, 26.00000000000000711 ) ) ;
#11159=FACE_OUTER_BOUND ( 'NONE', #570, .T. ) ;
#11162=LINE ( 'NONE', #64235, #21203 ) ;
#11163=CARTESIAN_POINT ( 'NONE',  ( -5.242976262117280406, -5.257023737882805747, 54.00000000000000711 ) ) ;
#11166=ORIENTED_EDGE ( 'NONE', *, *, #57575, .F. ) ;
#11167=FACE_OUTER_BOUND ( 'NONE', #19957, .T. ) ;
#11169=EDGE_CURVE ( 'NONE', #51101, #86, #21856, .T. ) ;
#11176=CARTESIAN_POINT ( 'NONE',  ( 0.9555237378827827754, -9.929523737882790968, 54.00000000000000711 ) ) ;
#11186=CARTESIAN_POINT ( 'NONE',  ( -9.781776262117318765, -10.50702373788275246, 26.00000000000000000 ) ) ;
#11214=ORIENTED_EDGE ( 'NONE', *, *, #4368, .T. ) ;
#11225=ORIENTED_EDGE ( 'NONE', *, *, #36667, .F. ) ;
#11230=ORIENTED_EDGE ( 'NONE', *, *, #68183, .F. ) ;
#11234=ORIENTED_EDGE ( 'NONE', *, *, #66579, .T. ) ;
#11242=CARTESIAN_POINT ( 'NONE',  ( 8.241237374594247100, 1.620245201994230611, 54.00000000000000711 ) ) ;
#11244=LINE ( 'NONE', #69961, #45833 ) ;
#11250=CARTESIAN_POINT ( 'NONE',  ( 9.912023737882815766, -3.682023737882817116, 26.00000000000000711 ) ) ;
#11251=CARTESIAN_POINT ( 'NONE',  ( -6.835476262117260227, 10.49297626211718359, 54.00000000000000711 ) ) ;
#11254=DIRECTION ( 'NONE',  ( 0.000000000000000000, 1.000000000000000000, 0.000000000000000000 ) ) ;
#11256=LINE ( 'NONE', #32499, #23048 ) ;
#11271=DIRECTION ( 'NONE',  ( -8.359604446858500663E-15, -1.000000000000000000, 0.000000000000000000 ) ) ;
#11280=VECTOR ( 'NONE', #58163, 1000.000000000000000 ) ;
#11281=VERTEX_POINT ( 'NONE', #27660 ) ;
#11287=ORIENTED_EDGE ( 'NONE', *, *, #46598, .T. ) ;
#11289=CARTESIAN_POINT ( 'NONE',  ( 9.795823737882805915, -10.50702373788282529, 54.00000000000000711 ) ) ;
#11293=ORIENTED_EDGE ( 'NONE', *, *, #30706, .F. ) ;
#11300=EDGE_CURVE ( 'NONE', #2701, #9404, #48978, .T. ) ;
#11302=EDGE_CURVE ( 'NONE', #23844, #19581, #65864, .T. ) ;
#11318=CARTESIAN_POINT ( 'NONE',  ( -9.390476262117260831, 0.9414762621171833823, 26.00000000000000711 ) ) ;
#11321=DIRECTION ( 'NONE',  ( 0.000000000000000000, 3.673940397442059868E-16, -1.000000000000000000 ) ) ;
#11325=DIRECTION ( 'NONE',  ( 0.8660254037844401509, 0.4999999999999974465, 0.000000000000000000 ) ) ;
#11346=LINE ( 'NONE', #15274, #10246 ) ;
#11349=CIRCLE ( 'NONE', #29405, 1.224999999999998757 ) ;
#11352=FILL_AREA_STYLE ('',( #64756 ) ) ;
#11354=EDGE_CURVE ( 'NONE', #50609, #66948, #6117, .T. ) ;
#11357=EDGE_CURVE ( 'NONE', #30669, #67341, #61851, .T. ) ;
#11363=VECTOR ( 'NONE', #38897, 1000.000000000000000 ) ;
#11379=CARTESIAN_POINT ( 'NONE',  ( -9.880476262117236175, 7.447976262117216528, 26.00000000000000711 ) ) ;
#11381=DIRECTION ( 'NONE',  ( 0.000000000000000000, -1.000000000000000000, -3.673940397442059868E-16 ) ) ;
#11386=LINE ( 'NONE', #59834, #37760 ) ;
#11388=EDGE_CURVE ( 'NONE', #55692, #31525, #38804, .T. ) ;
#11390=AXIS2_PLACEMENT_3D ( 'NONE', #31172, #69697, #64727 ) ;
#11395=EDGE_CURVE ( 'NONE', #19920, #10538, #61394, .T. ) ;
#11399=EDGE_CURVE ( 'NONE', #53330, #52904, #30726, .T. ) ;
#11402=VECTOR ( 'NONE', #8764, 1000.000000000000000 ) ;
#11407=VECTOR ( 'NONE', #17442, 1000.000000000000000 ) ;
#11411=EDGE_LOOP ( 'NONE', ( #49987, #7410, #34762, #68698 ) ) ;
#11412=VECTOR ( 'NONE', #31285, 1000.000000000000000 ) ;
#11416=LINE ( 'NONE', #23060, #44740 ) ;
#11419=PLANE ( 'NONE',  #10099 ) ;
#11434=ORIENTED_EDGE ( 'NONE', *, *, #33427, .F. ) ;
#11435=PLANE ( 'NONE',  #10150 ) ;
#11438=CARTESIAN_POINT ( 'NONE',  ( 6.501044194225450212, 3.142976262117187058, 54.00000000000000711 ) ) ;
#11439=LINE ( 'NONE', #22417, #68103 ) ;
#11450=AXIS2_PLACEMENT_3D ( 'NONE', #51725, #31224, #14244 ) ;
#11456=VECTOR ( 'NONE', #53539, 1000.000000000000000 ) ;
#11458=FACE_OUTER_BOUND ( 'NONE', #2350, .T. ) ;
#11460=EDGE_LOOP ( 'NONE', ( #65485, #6658, #21823, #47309, #59682, #8828, #46258, #55313, #52450, #13019, #33860, #10286, #3592, #67913, #6821, #35635, #44323 ) ) ;
#11464=CARTESIAN_POINT ( 'NONE',  ( 8.930623737882839919, 8.566576262117191476, 26.00000000000000711 ) ) ;
#11466=EDGE_LOOP ( 'NONE', ( #63419, #8197, #6665, #64532 ) ) ;
#11468=EDGE_CURVE ( 'NONE', #27729, #4139, #17354, .T. ) ;
#11476=AXIS2_PLACEMENT_3D ( 'NONE', #36462, #62992, #47418 ) ;
#11479=CARTESIAN_POINT ( 'NONE',  ( -6.822336235477446387, 4.135079735113102117, 54.00000000000000711 ) ) ;
#11486=CARTESIAN_POINT ( 'NONE',  ( -4.947141984184481700, 7.342976262117180575, 26.00000000000000711 ) ) ;
#11496=DIRECTION ( 'NONE',  ( 0.000000000000000000, 1.000000000000000000, 0.000000000000000000 ) ) ;
#11506=FACE_OUTER_BOUND ( 'NONE', #66263, .T. ) ;
#11511=DIRECTION ( 'NONE',  ( -0.000000000000000000, 3.673940397442059868E-16, -1.000000000000000000 ) ) ;
#11512=DIRECTION ( 'NONE',  ( 0.000000000000000000, 0.000000000000000000, 1.000000000000000000 ) ) ;
#11515=CARTESIAN_POINT ( 'NONE',  ( -6.775514141871423313, -7.408280051175137437, 26.00000000000000000 ) ) ;
#11518=EDGE_CURVE ( 'NONE', #38364, #4410, #31786, .T. ) ;
#11529=ORIENTED_EDGE ( 'NONE', *, *, #12599, .F. ) ;
#11530=AXIS2_PLACEMENT_3D ( 'NONE', #65635, #55381, #65970 ) ;
#11540=ADVANCED_FACE ( 'NONE', ( #3854 ), #63253, .T. ) ;
#11541=VERTEX_POINT ( 'NONE', #20465 ) ;
#11542=EDGE_LOOP ( 'NONE', ( #41289, #40472, #56529, #58880 ) ) ;
#11553=ORIENTED_EDGE ( 'NONE', *, *, #62887, .T. ) ;
#11556=ORIENTED_EDGE ( 'NONE', *, *, #39673, .T. ) ;
#11560=EDGE_CURVE ( 'NONE', #15483, #38190, #20119, .T. ) ;
#11561=VECTOR ( 'NONE', #44024, 1000.000000000000000 ) ;
#11568=ORIENTED_EDGE ( 'NONE', *, *, #24585, .F. ) ;
#11570=LINE ( 'NONE', #65347, #43033 ) ;
#11572=ADVANCED_FACE ( 'NONE', ( #60278 ), #63610, .F. ) ;
#11573=DIRECTION ( 'NONE',  ( 1.000000000000000000, 3.016910393003147986E-15, 1.108394896831706469E-30 ) ) ;
#11589=VECTOR ( 'NONE', #33777, 1000.000000000000000 ) ;
#11591=AXIS2_PLACEMENT_3D ( 'NONE', #25183, #47446, #25894 ) ;
#11592=ORIENTED_EDGE ( 'NONE', *, *, #56146, .F. ) ;
#11596=CARTESIAN_POINT ( 'NONE',  ( -3.834182069070765309, 7.342976262117171693, 54.00000000000000711 ) ) ;
#11597=LINE ( 'NONE', #45160, #11874 ) ;
#11599=DIRECTION ( 'NONE',  ( -0.000000000000000000, 3.673940397442059868E-16, -1.000000000000000000 ) ) ;
#11603=ADVANCED_FACE ( 'NONE', ( #65928 ), #13235, .F. ) ;
#11606=DIRECTION ( 'NONE',  ( 0.7671651518153105309, -0.6414496315691445849, -0.000000000000000000 ) ) ;
#11612=LINE ( 'NONE', #44832, #26539 ) ;
#11615=CIRCLE ( 'NONE', #4882, 0.1749999999999980738 ) ;
#11617=ORIENTED_EDGE ( 'NONE', *, *, #18270, .T. ) ;
#11626=PLANE ( 'NONE',  #38855 ) ;
#11633=LINE ( 'NONE', #44166, #552 ) ;
#11634=ADVANCED_FACE ( 'NONE', ( #18185 ), #39069, .F. ) ;
#11637=ORIENTED_EDGE ( 'NONE', *, *, #30744, .F. ) ;
#11638=ORIENTED_EDGE ( 'NONE', *, *, #45022, .T. ) ;
#11642=VECTOR ( 'NONE', #63405, 1000.000000000000000 ) ;
#11645=VERTEX_POINT ( 'NONE', #23846 ) ;
#11646=DIRECTION ( 'NONE',  ( 9.912705577010336396E-15, 1.000000000000000000, 0.000000000000000000 ) ) ;
#11650=ADVANCED_FACE ( 'NONE', ( #1937 ), #44704, .T. ) ;
#11652=ORIENTED_EDGE ( 'NONE', *, *, #27978, .F. ) ;
#11655=ADVANCED_FACE ( 'NONE', ( #23503 ), #51067, .T. ) ;
#11669=CIRCLE ( 'NONE', #65741, 0.1749999999999998224 ) ;
#11672=EDGE_CURVE ( 'NONE', #9024, #61728, #28448, .T. ) ;
#11676=EDGE_LOOP ( 'NONE', ( #1850, #26566, #30854, #5413 ) ) ;
#11685=EDGE_CURVE ( 'NONE', #41827, #5747, #17850, .T. ) ;
#11701=VECTOR ( 'NONE', #63388, 1000.000000000000000 ) ;
#11707=ORIENTED_EDGE ( 'NONE', *, *, #227, .F. ) ;
#11710=LINE ( 'NONE', #48177, #39903 ) ;
#11718=VERTEX_POINT ( 'NONE', #23145 ) ;
#11720=LINE ( 'NONE', #16710, #27670 ) ;
#11727=AXIS2_PLACEMENT_3D ( 'NONE', #53901, #22060, #16061 ) ;
#11734=ORIENTED_EDGE ( 'NONE', *, *, #64123, .F. ) ;
#11740=ORIENTED_EDGE ( 'NONE', *, *, #29369, .T. ) ;
#11742=AXIS2_PLACEMENT_3D ( 'NONE', #65567, #32696, #48966 ) ;
#11747=DIRECTION ( 'NONE',  ( -1.836970198721029934E-16, 1.836970198721036590E-16, -1.000000000000000000 ) ) ;
#11750=AXIS2_PLACEMENT_3D ( 'NONE', #45571, #36023, #51598 ) ;
#11758=ORIENTED_EDGE ( 'NONE', *, *, #14964, .T. ) ;
#11759=VECTOR ( 'NONE', #50795, 1000.000000000000000 ) ;
#11771=EDGE_CURVE ( 'NONE', #3393, #21681, #24557, .T. ) ;
#11773=DIRECTION ( 'NONE',  ( -0.7671651518153028704, -0.6414496315691537998, -2.587583378555113506E-16 ) ) ;
#11778=DIRECTION ( 'NONE',  ( -0.000000000000000000, -0.000000000000000000, -1.000000000000000000 ) ) ;
#11790=DIRECTION ( 'NONE',  ( -1.000000000000000000, 0.000000000000000000, 0.000000000000000000 ) ) ;
#11792=FACE_OUTER_BOUND ( 'NONE', #42416, .T. ) ;
#11795=VECTOR ( 'NONE', #56920, 1000.000000000000000 ) ;
#11799=VERTEX_POINT ( 'NONE', #67684 ) ;
#11800=VECTOR ( 'NONE', #9123, 1000.000000000000000 ) ;
#11809=ORIENTED_EDGE ( 'NONE', *, *, #49962, .T. ) ;
#11818=ADVANCED_FACE ( 'NONE', ( #46460 ), #25966, .T. ) ;
#11821=ORIENTED_EDGE ( 'NONE', *, *, #37564, .T. ) ;
#11824=EDGE_CURVE ( 'NONE', #59587, #29192, #40811, .T. ) ;
#11829=LINE ( 'NONE', #37426, #52023 ) ;
#11833=CARTESIAN_POINT ( 'NONE',  ( 6.836383711242975281, 4.135079735113102117, 54.00000000000000711 ) ) ;
#11839=CYLINDRICAL_SURFACE ( 'NONE', #59566, 0.1749999999999998224 ) ;
#11850=ORIENTED_EDGE ( 'NONE', *, *, #931, .T. ) ;
#11852=DIRECTION ( 'NONE',  ( -1.047444401652940007E-14, -1.000000000000000000, -1.836970198721029934E-16 ) ) ;
#11870=ORIENTED_EDGE ( 'NONE', *, *, #35587, .F. ) ;
#11874=VECTOR ( 'NONE', #33180, 1000.000000000000000 ) ;
#11876=ORIENTED_EDGE ( 'NONE', *, *, #10780, .T. ) ;
#11903=EDGE_CURVE ( 'NONE', #53683, #49071, #36643, .T. ) ;
#11905=AXIS2_PLACEMENT_3D ( 'NONE', #50559, #66805, #19073 ) ;
#11908=CARTESIAN_POINT ( 'NONE',  ( -8.697938382363135545, 8.079219948824830411, 26.00000000000000711 ) ) ;
#11917=LINE ( 'NONE', #43776, #52072 ) ;
#11931=CARTESIAN_POINT ( 'NONE',  ( 6.364920264886851697, 3.663616288756991413, 54.00000000000000711 ) ) ;
#11934=AXIS2_PLACEMENT_3D ( 'NONE', #67200, #24065, #35723 ) ;
#11940=CYLINDRICAL_SURFACE ( 'NONE', #35680, 0.3499999999999996447 ) ;
#11946=LINE ( 'NONE', #1692, #21852 ) ;
#11953=CARTESIAN_POINT ( 'NONE',  ( 6.358413763958968623, -4.720772854004790631, 54.00000000000000711 ) ) ;
#11955=CYLINDRICAL_SURFACE ( 'NONE', #2788, 0.1749999999999998224 ) ;
#11963=DIRECTION ( 'NONE',  ( -5.163402228214836012E-15, -1.000000000000000000, -1.836970198721026976E-16 ) ) ;
#11964=FACE_OUTER_BOUND ( 'NONE', #13269, .T. ) ;
#11967=ORIENTED_EDGE ( 'NONE', *, *, #13894, .T. ) ;
#11973=ORIENTED_EDGE ( 'NONE', *, *, #37002, .F. ) ;
#11984=ORIENTED_EDGE ( 'NONE', *, *, #7650, .F. ) ;
#11986=AXIS2_PLACEMENT_3D ( 'NONE', #12105, #54917, #26997 ) ;
#11994=AXIS2_PLACEMENT_3D ( 'NONE', #2094, #6698, #43841 ) ;
#11998=EDGE_CURVE ( 'NONE', #23009, #39317, #32998, .T. ) ;
#11999=CIRCLE ( 'NONE', #44753, 1.929199999999998916 ) ;
#12003=CARTESIAN_POINT ( 'NONE',  ( -5.242976262117280406, -5.257023737882805747, 54.00000000000000711 ) ) ;
#12004=ORIENTED_EDGE ( 'NONE', *, *, #61631, .T. ) ;
#12008=DIRECTION ( 'NONE',  ( 8.339399738404099512E-15, 1.000000000000000000, 1.836970198721025990E-16 ) ) ;
#12010=PLANE ( 'NONE',  #31718 ) ;
#12015=DIRECTION ( 'NONE',  ( -0.7071067811865560104, -0.7071067811865391350, -2.597868168706466792E-16 ) ) ;
#12026=CARTESIAN_POINT ( 'NONE',  ( 6.364920264886851697, 3.663616288756991413, 54.00000000000000711 ) ) ;
#12032=ADVANCED_FACE ( 'NONE', ( #33680 ), #17417, .F. ) ;
#12036=ORIENTED_EDGE ( 'NONE', *, *, #3622, .F. ) ;
#12039=ORIENTED_EDGE ( 'NONE', *, *, #33950, .T. ) ;
#12043=VECTOR ( 'NONE', #58744, 1000.000000000000000 ) ;
#12045=AXIS2_PLACEMENT_3D ( 'NONE', #21476, #49049, #60329 ) ;
#12052=ORIENTED_EDGE ( 'NONE', *, *, #17117, .F. ) ;
#12053=LINE ( 'NONE', #51280, #27273 ) ;
#12054=ORIENTED_EDGE ( 'NONE', *, *, #58713, .T. ) ;
#12061=EDGE_CURVE ( 'NONE', #20506, #48716, #14019, .T. ) ;
#12062=ADVANCED_FACE ( 'NONE', ( #39334 ), #2202, .T. ) ;
#12068=ORIENTED_EDGE ( 'NONE', *, *, #19552, .F. ) ;
#12079=VECTOR ( 'NONE', #24910, 1000.000000000000000 ) ;
#12089=CARTESIAN_POINT ( 'NONE',  ( -10.30047626211725742, 6.835476262117182955, 54.00000000000000711 ) ) ;
#12090=ORIENTED_EDGE ( 'NONE', *, *, #1527, .T. ) ;
#12097=EDGE_LOOP ( 'NONE', ( #21215, #41794, #25137, #64434 ) ) ;
#12100=AXIS2_PLACEMENT_3D ( 'NONE', #7926, #62726, #19595 ) ;
#12101=CARTESIAN_POINT ( 'NONE',  ( -9.547976262117217061, -2.369523737882723857, 26.00000000000000711 ) ) ;
#12103=CARTESIAN_POINT ( 'NONE',  ( -3.667976262117228714, 9.722976262117169810, 54.00000000000000711 ) ) ;
#12105=CARTESIAN_POINT ( 'NONE',  ( -5.242976262117259978, 5.242976262117182706, 54.00000000000000711 ) ) ;
#12109=DIRECTION ( 'NONE',  ( 0.000000000000000000, 1.000000000000000000, 3.673940397442059868E-16 ) ) ;
#12110=VERTEX_POINT ( 'NONE', #18104 ) ;
#12114=LINE ( 'NONE', #27357, #61869 ) ;
#12120=CYLINDRICAL_SURFACE ( 'NONE', #8579, 0.1749999999999998224 ) ;
#12137=CARTESIAN_POINT ( 'NONE',  ( -4.135079735113167843, 6.822336235477362010, 54.00000000000000711 ) ) ;
#12145=DIRECTION ( 'NONE',  ( -0.7071067811865411334, 0.7071067811865539010, 0.000000000000000000 ) ) ;
#12151=CARTESIAN_POINT ( 'NONE',  ( 9.562023737882764607, 2.355476262117153663, 54.00000000000000711 ) ) ;
#12164=ORIENTED_EDGE ( 'NONE', *, *, #49669, .F. ) ;
#12176=CARTESIAN_POINT ( 'NONE',  ( -10.30047626211724854, -3.664523737882715348, 54.00000000000000711 ) ) ;
#12178=( GEOMETRIC_REPRESENTATION_CONTEXT ( 3 ) GLOBAL_UNCERTAINTY_ASSIGNED_CONTEXT ( ( #14706 ) ) GLOBAL_UNIT_ASSIGNED_CONTEXT ( ( #68, #49191, #38917 ) ) REPRESENTATION_CONTEXT ( 'NONE', 'WORKASPACE' ) );
#12185=DIRECTION ( 'NONE',  ( -0.7671651518153128624, -0.6414496315691420314, 2.309356642089219057E-17 ) ) ;
#12186=CIRCLE ( 'NONE', #18963, 1.224999999999999423 ) ;
#12187=CARTESIAN_POINT ( 'NONE',  ( 7.357023737882784076, 3.834182069070697807, 54.00000000000000711 ) ) ;
#12190=LINE ( 'NONE', #28795, #17760 ) ;
#12192=LINE ( 'NONE', #18192, #11561 ) ;
#12199=VECTOR ( 'NONE', #5457, 1000.000000000000000 ) ;
#12203=DIRECTION ( 'NONE',  ( -1.000000000000000000, 3.491481338843133355E-15, 1.836970198721036590E-16 ) ) ;
#12204=DIRECTION ( 'NONE',  ( 1.836970198721029934E-16, -1.836970198721036344E-16, 1.000000000000000000 ) ) ;
#12206=LINE ( 'NONE', #33779, #14974 ) ;
#12217=EDGE_LOOP ( 'NONE', ( #13783, #61563, #52378, #5386 ) ) ;
#12220=CARTESIAN_POINT ( 'NONE',  ( -2.406732575409666008, -8.711985858128704407, 26.00000000000000711 ) ) ;
#12233=ORIENTED_EDGE ( 'NONE', *, *, #25026, .F. ) ;
#12236=CARTESIAN_POINT ( 'NONE',  ( 4.149127210878741145, 3.663616288756999406, 54.00000000000000711 ) ) ;
#12246=CARTESIAN_POINT ( 'NONE',  ( 2.632023737882806191, 6.486996718459881350, 54.00000000000000711 ) ) ;
#12249=ORIENTED_EDGE ( 'NONE', *, *, #32366, .T. ) ;
#12251=ADVANCED_FACE ( 'NONE', ( #13505 ), #58040, .F. ) ;
#12253=DIRECTION ( 'NONE',  ( 0.7071067811865474617, 0.7071067811865474617, 0.000000000000000000 ) ) ;
#12258=ORIENTED_EDGE ( 'NONE', *, *, #55080, .T. ) ;
#12260=DIRECTION ( 'NONE',  ( -1.000000000000000000, 1.047444401652940007E-14, -1.836970198721010706E-16 ) ) ;
#12261=LINE ( 'NONE', #56116, #23938 ) ;
#12265=DIRECTION ( 'NONE',  ( 3.304235192336781428E-15, 1.000000000000000000, 0.000000000000000000 ) ) ;
#12267=CARTESIAN_POINT ( 'NONE',  ( 6.849523737882817542, -10.50702373788282529, 54.00000000000000711 ) ) ;
#12270=VECTOR ( 'NONE', #34750, 1000.000000000000000 ) ;
#12281=CARTESIAN_POINT ( 'NONE',  ( -7.955476262117259445, 9.722976262117178692, 26.00000000000000711 ) ) ;
#12283=CARTESIAN_POINT ( 'NONE',  ( 3.677663764522614454, -4.149127210878770455, 54.00000000000000711 ) ) ;
#12285=LINE ( 'NONE', #60387, #5718 ) ;
#12288=AXIS2_PLACEMENT_3D ( 'NONE', #50473, #64241, #37365 ) ;
#12291=ORIENTED_EDGE ( 'NONE', *, *, #40768, .F. ) ;
#12297=AXIS2_PLACEMENT_3D ( 'NONE', #39663, #8185, #6204 ) ;
#12300=ORIENTED_EDGE ( 'NONE', *, *, #63043, .F. ) ;
#12301=VERTEX_POINT ( 'NONE', #27277 ) ;
#12308=DIRECTION ( 'NONE',  ( -0.000000000000000000, -0.000000000000000000, -1.000000000000000000 ) ) ;
#12310=DIRECTION ( 'NONE',  ( -1.261617073437657735E-14, -1.000000000000000000, 0.000000000000000000 ) ) ;
#12314=DIRECTION ( 'NONE',  ( -1.000000000000000000, 8.540177112501197482E-15, 0.000000000000000000 ) ) ;
#12317=VECTOR ( 'NONE', #56341, 1000.000000000000000 ) ;
#12327=FACE_OUTER_BOUND ( 'NONE', #29947, .T. ) ;
#12328=DIRECTION ( 'NONE',  ( 0.000000000000000000, -1.000000000000000000, 0.000000000000000000 ) ) ;
#12331=VECTOR ( 'NONE', #52557, 1000.000000000000000 ) ;
#12335=ORIENTED_EDGE ( 'NONE', *, *, #2494, .T. ) ;
#12339=VERTEX_POINT ( 'NONE', #16667 ) ;
#12345=CARTESIAN_POINT ( 'NONE',  ( 4.155633711806658859, -4.720772854004797736, 26.00000000000000711 ) ) ;
#12350=ORIENTED_EDGE ( 'NONE', *, *, #68823, .F. ) ;
#12364=FACE_BOUND ( 'NONE', #49903, .T. ) ;
#12375=EDGE_CURVE ( 'NONE', #45981, #10245, #59787, .T. ) ;
#12376=ORIENTED_EDGE ( 'NONE', *, *, #29851, .T. ) ;
#12382=VECTOR ( 'NONE', #35331, 1000.000000000000000 ) ;
#12384=DIRECTION ( 'NONE',  ( -1.000000000000000000, 0.000000000000000000, 0.000000000000000000 ) ) ;
#12387=EDGE_LOOP ( 'NONE', ( #39589, #5928, #57701, #33088 ) ) ;
#12391=EDGE_LOOP ( 'NONE', ( #29646, #8861, #12068, #40555 ) ) ;
#12395=CARTESIAN_POINT ( 'NONE',  ( -10.49297626211726175, 3.650476262117184234, 54.00000000000000711 ) ) ;
#12412=DIRECTION ( 'NONE',  ( -0.000000000000000000, 3.673940397442059868E-16, -1.000000000000000000 ) ) ;
#12414=ORIENTED_EDGE ( 'NONE', *, *, #18434, .F. ) ;
#12420=VECTOR ( 'NONE', #50872, 1000.000000000000000 ) ;
#12426=ORIENTED_EDGE ( 'NONE', *, *, #7265, .F. ) ;
#12431=LINE ( 'NONE', #45659, #36269 ) ;
#12457=DIRECTION ( 'NONE',  ( 1.836970198721029934E-16, 1.836970198721010706E-16, -1.000000000000000000 ) ) ;
#12459=EDGE_CURVE ( 'NONE', #42591, #48280, #66120, .T. ) ;
#12466=ORIENTED_EDGE ( 'NONE', *, *, #64829, .T. ) ;
#12467=EDGE_CURVE ( 'NONE', #17187, #18067, #57018, .T. ) ;
#12476=ORIENTED_EDGE ( 'NONE', *, *, #2548, .T. ) ;
#12478=LINE ( 'NONE', #24502, #1312 ) ;
#12481=CIRCLE ( 'NONE', #68982, 0.5249999999999994671 ) ;
#12485=PLANE ( 'NONE',  #33058 ) ;
#12500=ORIENTED_EDGE ( 'NONE', *, *, #24261, .F. ) ;
#12509=VERTEX_POINT ( 'NONE', #22985 ) ;
#12513=ADVANCED_FACE ( 'NONE', ( #22649 ), #1090, .F. ) ;
#12515=CARTESIAN_POINT ( 'NONE',  ( -9.722976262117258628, 6.817976262117182884, 26.00000000000000711 ) ) ;
#12517=DIRECTION ( 'NONE',  ( -3.304235192336778667E-15, -1.000000000000000000, 0.000000000000000000 ) ) ;
#12519=CARTESIAN_POINT ( 'NONE',  ( -4.706725378239216440, 6.344366288193329595, 54.00000000000000711 ) ) ;
#12520=VERTEX_POINT ( 'NONE', #44201 ) ;
#12521=ADVANCED_FACE ( 'NONE', ( #7060 ), #33602, .F. ) ;
#12522=CARTESIAN_POINT ( 'NONE',  ( -5.242976262117259978, 5.242976262117182706, 26.00000000000000711 ) ) ;
#12528=CYLINDRICAL_SURFACE ( 'NONE', #46122, 0.5250000000000004663 ) ;
#12532=VERTEX_POINT ( 'NONE', #12704 ) ;
#12546=CARTESIAN_POINT ( 'NONE',  ( -4.135079735113208699, -3.677663764522613121, 54.00000000000000711 ) ) ;
#12558=ORIENTED_EDGE ( 'NONE', *, *, #57820, .T. ) ;
#12566=VERTEX_POINT ( 'NONE', #29322 ) ;
#12576=ORIENTED_EDGE ( 'NONE', *, *, #49126, .T. ) ;
#12581=AXIS2_PLACEMENT_3D ( 'NONE', #4350, #25910, #69376 ) ;
#12583=ORIENTED_EDGE ( 'NONE', *, *, #3720, .T. ) ;
#12589=DIRECTION ( 'NONE',  ( 1.836970198721029934E-16, 1.836970198721010706E-16, -1.000000000000000000 ) ) ;
#12591=VERTEX_POINT ( 'NONE', #41691 ) ;
#12596=EDGE_CURVE ( 'NONE', #50286, #40232, #56214, .T. ) ;
#12599=EDGE_CURVE ( 'NONE', #36429, #12509, #50892, .T. ) ;
#12605=AXIS2_PLACEMENT_3D ( 'NONE', #31605, #53180, #4391 ) ;
#12608=LINE ( 'NONE', #32809, #7202 ) ;
#12613=ORIENTED_EDGE ( 'NONE', *, *, #62506, .T. ) ;
#12617=CARTESIAN_POINT ( 'NONE',  ( -9.547976262117256141, 2.530476262117183683, 54.00000000000000711 ) ) ;
#12625=DIRECTION ( 'NONE',  ( -1.000000000000000000, -5.013651664672856055E-16, 0.000000000000000000 ) ) ;
#12647=VERTEX_POINT ( 'NONE', #45584 ) ;
#12652=DIRECTION ( 'NONE',  ( -0.000000000000000000, -0.000000000000000000, -1.000000000000000000 ) ) ;
#12663=ORIENTED_EDGE ( 'NONE', *, *, #2803, .T. ) ;
#12666=AXIS2_PLACEMENT_3D ( 'NONE', #15530, #10905, #53697 ) ;
#12668=EDGE_CURVE ( 'NONE', #43731, #21439, #3871, .T. ) ;
#12674=DIRECTION ( 'NONE',  ( -0.000000000000000000, 3.673940397442059868E-16, -1.000000000000000000 ) ) ;
#12682=EDGE_CURVE ( 'NONE', #22714, #38860, #40290, .T. ) ;
#12690=DIRECTION ( 'NONE',  ( -0.6414496315691494699, -0.7671651518153064231, -0.000000000000000000 ) ) ;
#12696=DIRECTION ( 'NONE',  ( -0.000000000000000000, 3.673940397442059868E-16, -1.000000000000000000 ) ) ;
#12697=CARTESIAN_POINT ( 'NONE',  ( 6.364920264886885448, -3.677663764522628664, 54.00000000000000711 ) ) ;
#12701=DIRECTION ( 'NONE',  ( -9.912705577010435793E-15, -1.000000000000000000, 0.000000000000000000 ) ) ;
#12704=CARTESIAN_POINT ( 'NONE',  ( 3.003254798005744242, -6.872275254348413576, 54.00000000000000711 ) ) ;
#12711=DIRECTION ( 'NONE',  ( -1.836970198721029934E-16, 1.836970198721036590E-16, -1.000000000000000000 ) ) ;
#12720=ORIENTED_EDGE ( 'NONE', *, *, #11399, .T. ) ;
#12723=ORIENTED_EDGE ( 'NONE', *, *, #61311, .T. ) ;
#12724=CIRCLE ( 'NONE', #21791, 0.1749999999999998224 ) ;
#12731=FACE_OUTER_BOUND ( 'NONE', #53429, .T. ) ;
#12735=ORIENTED_EDGE ( 'NONE', *, *, #7594, .T. ) ;
#12736=CARTESIAN_POINT ( 'NONE',  ( 5.257023737882819070, -5.257023737882825287, 54.00000000000000711 ) ) ;
#12741=CARTESIAN_POINT ( 'NONE',  ( -10.30047626211725742, 3.842976262117182351, 54.00000000000000711 ) ) ;
#12755=DIRECTION ( 'NONE',  ( -7.665540703601096574E-15, -1.000000000000000000, 0.000000000000000000 ) ) ;
#12758=CARTESIAN_POINT ( 'NONE',  ( 5.257023737882819070, -7.186223737882822427, 54.00000000000000711 ) ) ;
#12762=EDGE_LOOP ( 'NONE', ( #51760, #4351, #66348, #8598 ) ) ;
#12779=FACE_OUTER_BOUND ( 'NONE', #33128, .T. ) ;
#12782=EDGE_CURVE ( 'NONE', #29317, #52054, #52675, .T. ) ;
#12787=PLANE ( 'NONE',  #46847 ) ;
#12789=CARTESIAN_POINT ( 'NONE',  ( 8.580623737882818958, -8.930623737882855906, 54.00000000000000711 ) ) ;
#12800=ORIENTED_EDGE ( 'NONE', *, *, #37009, .F. ) ;
#12803=AXIS2_PLACEMENT_3D ( 'NONE', #5762, #32970, #26982 ) ;
#12806=ORIENTED_EDGE ( 'NONE', *, *, #40324, .F. ) ;
#12816=ORIENTED_EDGE ( 'NONE', *, *, #37945, .F. ) ;
#12820=EDGE_LOOP ( 'NONE', ( #42364, #25435, #18516, #69830 ) ) ;
#12822=LINE ( 'NONE', #34387, #43356 ) ;
#12829=ORIENTED_EDGE ( 'NONE', *, *, #24536, .T. ) ;
#12837=CIRCLE ( 'NONE', #42239, 1.929199999999998028 ) ;
#12845=VECTOR ( 'NONE', #66976, 1000.000000000000000 ) ;
#12850=CARTESIAN_POINT ( 'NONE',  ( -3.710438382363173027, -7.408280051175170300, 26.00000000000000711 ) ) ;
#12852=FACE_OUTER_BOUND ( 'NONE', #67939, .T. ) ;
#12854=DIRECTION ( 'NONE',  ( 1.000000000000000000, 0.000000000000000000, 0.000000000000000000 ) ) ;
#12866=ORIENTED_EDGE ( 'NONE', *, *, #30744, .T. ) ;
#12867=CARTESIAN_POINT ( 'NONE',  ( -6.344366288193421077, -4.720772854004749775, 54.00000000000000711 ) ) ;
#12869=DIRECTION ( 'NONE',  ( -1.221996412923863950E-14, -1.000000000000000000, 0.000000000000000000 ) ) ;
#12878=ORIENTED_EDGE ( 'NONE', *, *, #57271, .T. ) ;
#12881=DIRECTION ( 'NONE',  ( -2.135044278125301343E-15, 1.000000000000000000, 0.000000000000000000 ) ) ;
#12884=AXIS2_PLACEMENT_3D ( 'NONE', #37236, #42869, #64454 ) ;
#12889=CARTESIAN_POINT ( 'NONE',  ( 6.665817930929297752, -7.357023737882814274, 26.00000000000000000 ) ) ;
#12890=CARTESIAN_POINT ( 'NONE',  ( 9.404523737882817258, -1.480523737882826207, 54.00000000000000711 ) ) ;
#12905=CARTESIAN_POINT ( 'NONE',  ( 8.580623737882849156, 9.689726262117156708, 54.00000000000000711 ) ) ;
#12906=DIRECTION ( 'NONE',  ( -1.000000000000000000, 1.047444401652940007E-14, 0.000000000000000000 ) ) ;
#12907=ORIENTED_EDGE ( 'NONE', *, *, #37612, .F. ) ;
#12908=EDGE_CURVE ( 'NONE', #7367, #66946, #33850, .T. ) ;
#12909=CIRCLE ( 'NONE', #28723, 0.3499999999999996447 ) ;
#12912=ORIENTED_EDGE ( 'NONE', *, *, #56527, .F. ) ;
#12916=ORIENTED_EDGE ( 'NONE', *, *, #69396, .T. ) ;
#12917=DIRECTION ( 'NONE',  ( 1.047444401652940007E-14, 1.000000000000000000, 0.000000000000000000 ) ) ;
#12936=EDGE_CURVE ( 'NONE', #52784, #53491, #22225, .T. ) ;
#12941=ORIENTED_EDGE ( 'NONE', *, *, #24946, .T. ) ;
#12943=CIRCLE ( 'NONE', #22016, 0.5249999999999990230 ) ;
#12949=EDGE_CURVE ( 'NONE', #35367, #47586, #33356, .T. ) ;
#12953=VECTOR ( 'NONE', #54566, 1000.000000000000000 ) ;
#12968=LINE ( 'NONE', #29235, #4857 ) ;
#12974=ORIENTED_EDGE ( 'NONE', *, *, #64380, .T. ) ;
#12980=CARTESIAN_POINT ( 'NONE',  ( 1.480523737882808444, 8.598420958951642490, 26.00000000000000711 ) ) ;
#12986=AXIS2_PLACEMENT_3D ( 'NONE', #18875, #22535, #28172 ) ;
#12990=EDGE_CURVE ( 'NONE', #29373, #1632, #44117, .T. ) ;
#12991=CARTESIAN_POINT ( 'NONE',  ( 8.711985858128693749, -2.420780051175180692, 54.00000000000000711 ) ) ;
#12995=CARTESIAN_POINT ( 'NONE',  ( -1.991476262117235274, 8.598420958951582094, 54.00000000000000711 ) ) ;
#12999=EDGE_CURVE ( 'NONE', #46962, #15894, #14028, .T. ) ;
#13008=ORIENTED_EDGE ( 'NONE', *, *, #16738, .T. ) ;
#13013=EDGE_LOOP ( 'NONE', ( #41662, #36388, #16133, #31133 ) ) ;
#13019=ORIENTED_EDGE ( 'NONE', *, *, #50896, .T. ) ;
#13028=ORIENTED_EDGE ( 'NONE', *, *, #38959, .F. ) ;
#13035=EDGE_CURVE ( 'NONE', #40232, #42575, #35586, .T. ) ;
#13041=DIRECTION ( 'NONE',  ( -1.836970198721029934E-16, 1.836970198721036590E-16, -1.000000000000000000 ) ) ;
#13042=EDGE_CURVE ( 'NONE', #46007, #7648, #45498, .T. ) ;
#13043=ORIENTED_EDGE ( 'NONE', *, *, #68569, .F. ) ;
#13051=CARTESIAN_POINT ( 'NONE',  ( -2.530476262117327568, -9.737023737882829266, 54.00000000000000711 ) ) ;
#13064=CIRCLE ( 'NONE', #57144, 0.1749999999999998224 ) ;
#13071=CARTESIAN_POINT ( 'NONE',  ( 8.093267424590454340, 8.697938382363069820, 26.00000000000000711 ) ) ;
#13073=DIRECTION ( 'NONE',  ( 1.000000000000000000, 0.000000000000000000, 0.000000000000000000 ) ) ;
#13083=CIRCLE ( 'NONE', #58288, 0.5249999999999990230 ) ;
#13084=ADVANCED_FACE ( 'NONE', ( #13682 ), #51158, .F. ) ;
#13088=CARTESIAN_POINT ( 'NONE',  ( 9.562023737882812569, -2.369523737882825998, 54.00000000000000711 ) ) ;
#13092=ADVANCED_FACE ( 'NONE', ( #24651 ), #2377, .F. ) ;
#13094=EDGE_LOOP ( 'NONE', ( #32447, #27475, #54753, #7575 ) ) ;
#13110=CARTESIAN_POINT ( 'NONE',  ( -5.242976262117280406, -5.257023737882805747, 54.00000000000000711 ) ) ;
#13111=ORIENTED_EDGE ( 'NONE', *, *, #9785, .T. ) ;
#13112=EDGE_LOOP ( 'NONE', ( #8683, #46906, #59138, #41464 ) ) ;
#13122=ORIENTED_EDGE ( 'NONE', *, *, #62887, .F. ) ;
#13128=FACE_OUTER_BOUND ( 'NONE', #53755, .T. ) ;
#13130=LINE ( 'NONE', #17756, #22741 ) ;
#13134=ADVANCED_FACE ( 'NONE', ( #35954 ), #57516, .F. ) ;
#13137=AXIS2_PLACEMENT_3D ( 'NONE', #18481, #44314, #12145 ) ;
#13138=DIRECTION ( 'NONE',  ( -0.000000000000000000, 3.673940397442059868E-16, -1.000000000000000000 ) ) ;
#13153=DIRECTION ( 'NONE',  ( 1.000000000000000000, 0.000000000000000000, 0.000000000000000000 ) ) ;
#13164=DIRECTION ( 'NONE',  ( -0.000000000000000000, 3.673940397442059868E-16, -1.000000000000000000 ) ) ;
#13170=ORIENTED_EDGE ( 'NONE', *, *, #29374, .T. ) ;
#13172=DIRECTION ( 'NONE',  ( 0.000000000000000000, 1.000000000000000000, 0.000000000000000000 ) ) ;
#13173=LINE ( 'NONE', #45692, #38725 ) ;
#13177=CARTESIAN_POINT ( 'NONE',  ( 7.969523737882818537, -8.835729544836334881, 26.00000000000000000 ) ) ;
#13181=FACE_OUTER_BOUND ( 'NONE', #43863, .T. ) ;
#13203=CARTESIAN_POINT ( 'NONE',  ( -10.30047626211729295, -6.657023737882751924, 54.00000000000000711 ) ) ;
#13204=CIRCLE ( 'NONE', #32462, 0.1749999999999998224 ) ;
#13211=VECTOR ( 'NONE', #27597, 1000.000000000000000 ) ;
#13216=ORIENTED_EDGE ( 'NONE', *, *, #44313, .F. ) ;
#13217=VECTOR ( 'NONE', #30630, 1000.000000000000000 ) ;
#13219=FACE_OUTER_BOUND ( 'NONE', #47735, .T. ) ;
#13220=ORIENTED_EDGE ( 'NONE', *, *, #63826, .F. ) ;
#13226=CARTESIAN_POINT ( 'NONE',  ( 5.257023737882795977, 5.242976262117205799, 26.00000000000000711 ) ) ;
#13235=PLANE ( 'NONE',  #63715 ) ;
#13244=AXIS2_PLACEMENT_3D ( 'NONE', #67137, #19738, #62176 ) ;
#13253=CARTESIAN_POINT ( 'NONE',  ( -7.342976262117273833, -4.961189459950004377, 54.00000000000000711 ) ) ;
#13260=ORIENTED_EDGE ( 'NONE', *, *, #49261, .F. ) ;
#13263=EDGE_CURVE ( 'NONE', #51293, #65543, #52940, .T. ) ;
#13266=DIRECTION ( 'NONE',  ( -0.000000000000000000, -0.000000000000000000, -1.000000000000000000 ) ) ;
#13269=EDGE_LOOP ( 'NONE', ( #27324, #29736, #51483, #51189 ) ) ;
#13271=CARTESIAN_POINT ( 'NONE',  ( 6.657023737882821202, 10.30047626211719347, 54.00000000000000711 ) ) ;
#13275=EDGE_CURVE ( 'NONE', #22435, #5714, #5529, .T. ) ;
#13283=ADVANCED_FACE ( 'NONE', ( #63537 ), #63880, .F. ) ;
#13295=VERTEX_POINT ( 'NONE', #65939 ) ;
#13296=VERTEX_POINT ( 'NONE', #43338 ) ;
#13300=VECTOR ( 'NONE', #48161, 1000.000000000000000 ) ;
#13301=DIRECTION ( 'NONE',  ( 0.8660254037844363761, -0.5000000000000038858, 0.000000000000000000 ) ) ;
#13306=EDGE_LOOP ( 'NONE', ( #6850, #28491, #11973, #66869 ) ) ;
#13310=DIRECTION ( 'NONE',  ( -1.047444401652940007E-14, -1.000000000000000000, -1.836970198721029934E-16 ) ) ;
#13311=PLANE ( 'NONE',  #31326 ) ;
#13313=EDGE_CURVE ( 'NONE', #67681, #56335, #66306, .T. ) ;
#13314=VECTOR ( 'NONE', #68044, 1000.000000000000000 ) ;
#13317=FACE_OUTER_BOUND ( 'NONE', #16548, .T. ) ;
#13326=LINE ( 'NONE', #39162, #19529 ) ;
#13327=VERTEX_POINT ( 'NONE', #49010 ) ;
#13328=DIRECTION ( 'NONE',  ( -1.000000000000000000, 3.491481338843133355E-15, 1.836970198721036590E-16 ) ) ;
#13330=DIRECTION ( 'NONE',  ( -0.000000000000000000, -0.000000000000000000, -1.000000000000000000 ) ) ;
#13341=EDGE_CURVE ( 'NONE', #47150, #12339, #936, .T. ) ;
#13342=ORIENTED_EDGE ( 'NONE', *, *, #43236, .T. ) ;
#13345=ADVANCED_FACE ( 'NONE', ( #23159 ), #33773, .F. ) ;
#13348=CARTESIAN_POINT ( 'NONE',  ( 2.005523737882793256, -8.612468434717222010, 54.00000000000000711 ) ) ;
#13350=ORIENTED_EDGE ( 'NONE', *, *, #55499, .T. ) ;
#13355=ADVANCED_FACE ( 'NONE', ( #6898 ), #60652, .T. ) ;
#13372=PLANE ( 'NONE',  #18871 ) ;
#13373=LINE ( 'NONE', #44843, #53576 ) ;
#13377=CARTESIAN_POINT ( 'NONE',  ( 10.50702373788281996, -3.664523737882816157, 26.00000000000000711 ) ) ;
#13378=ORIENTED_EDGE ( 'NONE', *, *, #23166, .F. ) ;
#13384=CARTESIAN_POINT ( 'NONE',  ( -5.242976262117259978, 5.242976262117182706, 54.00000000000000711 ) ) ;
#13387=CARTESIAN_POINT ( 'NONE',  ( 5.257023737882801306, 5.242976262117200470, 54.00000000000000711 ) ) ;
#13392=ORIENTED_EDGE ( 'NONE', *, *, #29316, .T. ) ;
#13395=LINE ( 'NONE', #3152, #48166 ) ;
#13396=FACE_OUTER_BOUND ( 'NONE', #49950, .T. ) ;
#13403=ORIENTED_EDGE ( 'NONE', *, *, #50396, .T. ) ;
#13408=CIRCLE ( 'NONE', #42747, 0.1749999999999989342 ) ;
#13414=EDGE_CURVE ( 'NONE', #51859, #11281, #23860, .T. ) ;
#13419=CARTESIAN_POINT ( 'NONE',  ( 3.677663764522614454, -6.364920264886879231, 54.00000000000000711 ) ) ;
#13422=DIRECTION ( 'NONE',  ( -0.6414496315691494699, 0.7671651518153064231, 2.818519042764025305E-16 ) ) ;
#13428=ORIENTED_EDGE ( 'NONE', *, *, #33567, .F. ) ;
#13431=VERTEX_POINT ( 'NONE', #63720 ) ;
#13435=LINE ( 'NONE', #67174, #63186 ) ;
#13446=ORIENTED_EDGE ( 'NONE', *, *, #61233, .T. ) ;
#13452=DIRECTION ( 'NONE',  ( -1.000000000000000000, 0.000000000000000000, 0.000000000000000000 ) ) ;
#13460=DIRECTION ( 'NONE',  ( -0.5000000000000004441, 0.8660254037844383745, 0.000000000000000000 ) ) ;
#13462=CARTESIAN_POINT ( 'NONE',  ( 6.657023737882813208, 9.897976262117198942, 26.00000000000000711 ) ) ;
#13463=ORIENTED_EDGE ( 'NONE', *, *, #42538, .F. ) ;
#13480=EDGE_CURVE ( 'NONE', #58172, #25429, #22157, .T. ) ;
#13484=CARTESIAN_POINT ( 'NONE',  ( 8.580623737882842050, 8.916576262117192897, 26.00000000000000711 ) ) ;
#13488=DIRECTION ( 'NONE',  ( -8.802523127157697409E-15, -1.000000000000000000, -1.836970198721026976E-16 ) ) ;
#13490=CARTESIAN_POINT ( 'NONE',  ( 3.677663764522614454, -4.149127210878761574, 26.00000000000000711 ) ) ;
#13496=ADVANCED_FACE ( 'NONE', ( #29160 ), #50726, .T. ) ;
#13498=DIRECTION ( 'NONE',  ( -0.000000000000000000, -0.000000000000000000, -1.000000000000000000 ) ) ;
#13499=ORIENTED_EDGE ( 'NONE', *, *, #35834, .F. ) ;
#13501=VECTOR ( 'NONE', #22160, 1000.000000000000000 ) ;
#13502=AXIS2_PLACEMENT_3D ( 'NONE', #15219, #37138, #53401 ) ;
#13503=CARTESIAN_POINT ( 'NONE',  ( 6.872275254348426010, -3.003254798005762449, 54.00000000000000711 ) ) ;
#13505=FACE_OUTER_BOUND ( 'NONE', #4394, .T. ) ;
#13511=CARTESIAN_POINT ( 'NONE',  ( 8.930623737882818602, -10.05377373788282469, 54.00000000000000711 ) ) ;
#13517=PLANE ( 'NONE',  #42460 ) ;
#13539=AXIS2_PLACEMENT_3D ( 'NONE', #30615, #67408, #41575 ) ;
#13544=DIRECTION ( 'NONE',  ( 1.836970198721029934E-16, 1.836970198721010706E-16, -1.000000000000000000 ) ) ;
#13545=VERTEX_POINT ( 'NONE', #27286 ) ;
#13578=CARTESIAN_POINT ( 'NONE',  ( 7.408280051175133885, 3.710438382363056675, 26.00000000000000711 ) ) ;
#13580=ORIENTED_EDGE ( 'NONE', *, *, #25892, .T. ) ;
#13585=CARTESIAN_POINT ( 'NONE',  ( -8.598420958951642490, -2.005523737882745738, 54.00000000000000711 ) ) ;
#13592=CIRCLE ( 'NONE', #5687, 1.224999999999998757 ) ;
#13597=ORIENTED_EDGE ( 'NONE', *, *, #33608, .T. ) ;
#13604=LINE ( 'NONE', #44720, #27062 ) ;
#13630=ORIENTED_EDGE ( 'NONE', *, *, #58427, .F. ) ;
#13632=CARTESIAN_POINT ( 'NONE',  ( -10.30047626211725742, 6.835476262117182955, 54.00000000000000711 ) ) ;
#13640=ORIENTED_EDGE ( 'NONE', *, *, #51422, .F. ) ;
#13645=VECTOR ( 'NONE', #40269, 1000.000000000000000 ) ;
#13648=DIRECTION ( 'NONE',  ( 1.836970198721029934E-16, 1.836970198721010706E-16, -1.000000000000000000 ) ) ;
#13650=VECTOR ( 'NONE', #12260, 1000.000000000000000 ) ;
#13651=AXIS2_PLACEMENT_3D ( 'NONE', #30455, #40362, #2523 ) ;
#13676=CARTESIAN_POINT ( 'NONE',  ( -8.130476262117259267, 9.547976262117177981, 54.00000000000000711 ) ) ;
#13677=EDGE_CURVE ( 'NONE', #19158, #45832, #23683, .T. ) ;
#13679=DIRECTION ( 'NONE',  ( -1.000000000000000000, 7.304098846218132892E-15, -0.000000000000000000 ) ) ;
#13681=EDGE_CURVE ( 'NONE', #51881, #48238, #28995, .T. ) ;
#13682=FACE_OUTER_BOUND ( 'NONE', #9330, .T. ) ;
#13684=DIRECTION ( 'NONE',  ( -0.000000000000000000, -0.000000000000000000, -1.000000000000000000 ) ) ;
#13688=CARTESIAN_POINT ( 'NONE',  ( 10.50702373788280752, 6.835476262117182067, 54.00000000000000711 ) ) ;
#13691=LINE ( 'NONE', #19341, #32322 ) ;
#13697=VERTEX_POINT ( 'NONE', #50216 ) ;
#13705=CARTESIAN_POINT ( 'NONE',  ( 0.9555237378827827754, -9.929523737882790968, 54.00000000000000711 ) ) ;
#13713=ORIENTED_EDGE ( 'NONE', *, *, #32369, .T. ) ;
#13715=DIRECTION ( 'NONE',  ( -1.062075597536821678E-14, -1.000000000000000000, 0.000000000000000000 ) ) ;
#13716=LINE ( 'NONE', #2752, #68652 ) ;
#13718=CARTESIAN_POINT ( 'NONE',  ( 5.257023737882819070, -5.257023737882825287, 54.00000000000000711 ) ) ;
#13720=DIRECTION ( 'NONE',  ( -0.000000000000000000, 3.673940397442059868E-16, -1.000000000000000000 ) ) ;
#13732=DIRECTION ( 'NONE',  ( -0.000000000000000000, -0.000000000000000000, -1.000000000000000000 ) ) ;
#13738=CARTESIAN_POINT ( 'NONE',  ( 9.703773737882785966, -9.703773737882823269, 54.00000000000000711 ) ) ;
#13740=ADVANCED_FACE ( 'NONE', ( #1775 ), #34641, .F. ) ;
#13748=DIRECTION ( 'NONE',  ( -1.000000000000000000, -1.570596175624152290E-15, 0.000000000000000000 ) ) ;
#13753=ORIENTED_EDGE ( 'NONE', *, *, #55882, .F. ) ;
#13754=DIRECTION ( 'NONE',  ( -1.836970198721029934E-16, 1.836970198721036590E-16, -1.000000000000000000 ) ) ;
#13759=DIRECTION ( 'NONE',  ( -1.254221251785257574E-14, -1.000000000000000000, -1.836970198721013171E-16 ) ) ;
#13762=ORIENTED_EDGE ( 'NONE', *, *, #16872, .T. ) ;
#13766=CARTESIAN_POINT ( 'NONE',  ( 4.046023737882819660, -3.157023737882826087, 54.00000000000000711 ) ) ;
#13783=ORIENTED_EDGE ( 'NONE', *, *, #38873, .T. ) ;
#13784=CARTESIAN_POINT ( 'NONE',  ( 10.05377373788281581, 8.916576262117182239, 54.00000000000000711 ) ) ;
#13795=AXIS2_PLACEMENT_3D ( 'NONE', #58311, #10211, #20812 ) ;
#13804=ORIENTED_EDGE ( 'NONE', *, *, #9742, .T. ) ;
#13807=LINE ( 'NONE', #12741, #4052 ) ;
#13808=CARTESIAN_POINT ( 'NONE',  ( -7.394232575409614761, 6.775514141871308738, 54.00000000000000711 ) ) ;
#13818=CARTESIAN_POINT ( 'NONE',  ( 8.093267424590464998, -8.711985858128699078, 54.00000000000000711 ) ) ;
#13820=AXIS2_PLACEMENT_3D ( 'NONE', #68777, #41897, #36589 ) ;
#13845=DIRECTION ( 'NONE',  ( -0.000000000000000000, -0.000000000000000000, -1.000000000000000000 ) ) ;
#13853=DIRECTION ( 'NONE',  ( -0.000000000000000000, 3.673940397442059868E-16, -1.000000000000000000 ) ) ;
#13854=ADVANCED_FACE ( 'NONE', ( #41348 ), #8114, .F. ) ;
#13871=ORIENTED_EDGE ( 'NONE', *, *, #40562, .T. ) ;
#13873=DIRECTION ( 'NONE',  ( -1.836970198721029934E-16, 1.836970198721036590E-16, -1.000000000000000000 ) ) ;
#13884=ORIENTED_EDGE ( 'NONE', *, *, #30128, .T. ) ;
#13892=DIRECTION ( 'NONE',  ( -1.000000000000000000, 0.000000000000000000, 0.000000000000000000 ) ) ;
#13894=EDGE_CURVE ( 'NONE', #22546, #65963, #20140, .T. ) ;
#13902=ADVANCED_FACE ( 'NONE', ( #9537 ), #24394, .F. ) ;
#13913=FACE_OUTER_BOUND ( 'NONE', #52449, .T. ) ;
#13932=DIRECTION ( 'NONE',  ( 9.050731179009442381E-15, 1.000000000000000000, 3.673940397442060361E-16 ) ) ;
#13934=AXIS2_PLACEMENT_3D ( 'NONE', #45849, #2372, #23934 ) ;
#13940=ORIENTED_EDGE ( 'NONE', *, *, #30275, .T. ) ;
#13941=EDGE_CURVE ( 'NONE', #4410, #67915, #53701, .T. ) ;
#13943=CARTESIAN_POINT ( 'NONE',  ( -6.344366288193410419, 5.779227145995219139, 54.00000000000000711 ) ) ;
#13944=CARTESIAN_POINT ( 'NONE',  ( 3.682023737882818448, 9.722976262117203561, 54.00000000000000711 ) ) ;
#13946=ORIENTED_EDGE ( 'NONE', *, *, #58145, .F. ) ;
#13957=DIRECTION ( 'NONE',  ( 1.836970198721029934E-16, 1.836970198721010706E-16, -1.000000000000000000 ) ) ;
#13965=EDGE_CURVE ( 'NONE', #46962, #22289, #31088, .T. ) ;
#13967=AXIS2_PLACEMENT_3D ( 'NONE', #57118, #30954, #69131 ) ;
#13968=DIRECTION ( 'NONE',  ( -0.000000000000000000, -0.000000000000000000, -1.000000000000000000 ) ) ;
#13971=ORIENTED_EDGE ( 'NONE', *, *, #51215, .T. ) ;
#13974=AXIS2_PLACEMENT_3D ( 'NONE', #66292, #34435, #39748 ) ;
#13976=CIRCLE ( 'NONE', #9498, 1.929199999999998028 ) ;
#13979=AXIS2_PLACEMENT_3D ( 'NONE', #30447, #9940, #52367 ) ;
#13980=ORIENTED_EDGE ( 'NONE', *, *, #43454, .F. ) ;
#13984=DIRECTION ( 'NONE',  ( -0.000000000000000000, 1.000000000000000000, -0.000000000000000000 ) ) ;
#13990=DIRECTION ( 'NONE',  ( -0.000000000000000000, -0.000000000000000000, -1.000000000000000000 ) ) ;
#13997=EDGE_LOOP ( 'NONE', ( #7172, #26441, #429, #45791 ) ) ;
#13999=CARTESIAN_POINT ( 'NONE',  ( 10.50702373788281818, -9.795823737882813020, 54.00000000000000711 ) ) ;
#14018=DIRECTION ( 'NONE',  ( -0.000000000000000000, -0.000000000000000000, -1.000000000000000000 ) ) ;
#14019=CIRCLE ( 'NONE', #2763, 0.1749999999999989342 ) ;
#14022=VECTOR ( 'NONE', #34669, 1000.000000000000000 ) ;
#14028=LINE ( 'NONE', #29233, #60444 ) ;
#14032=LINE ( 'NONE', #30309, #36359 ) ;
#14041=CARTESIAN_POINT ( 'NONE',  ( 5.552858015815571591, 7.342976262117199227, 54.00000000000000711 ) ) ;
#14051=VECTOR ( 'NONE', #53297, 1000.000000000000000 ) ;
#14056=DIRECTION ( 'NONE',  ( -0.6414496315691521344, -0.7671651518153044247, -2.309356642088966375E-17 ) ) ;
#14059=EDGE_CURVE ( 'NONE', #13697, #47387, #42381, .T. ) ;
#14061=CARTESIAN_POINT ( 'NONE',  ( -3.650476262117333892, -10.31452373788281740, 54.00000000000000711 ) ) ;
#14065=EDGE_CURVE ( 'NONE', #62186, #51473, #63635, .T. ) ;
#14071=AXIS2_PLACEMENT_3D ( 'NONE', #12995, #34569, #8041 ) ;
#14072=VERTEX_POINT ( 'NONE', #10928 ) ;
#14075=EDGE_LOOP ( 'NONE', ( #37192, #58893, #56346, #33075 ) ) ;
#14092=ORIENTED_EDGE ( 'NONE', *, *, #58692, .F. ) ;
#14112=DIRECTION ( 'NONE',  ( -3.491481338843133355E-15, -1.000000000000000000, -1.836970198721029934E-16 ) ) ;
#14114=DIRECTION ( 'NONE',  ( -0.7071067811865474617, -0.7071067811865474617, -2.597868168706479611E-16 ) ) ;
#14118=LINE ( 'NONE', #42044, #39186 ) ;
#14119=AXIS2_PLACEMENT_3D ( 'NONE', #64360, #53753, #15919 ) ;
#14127=ORIENTED_EDGE ( 'NONE', *, *, #25097, .F. ) ;
#14131=ADVANCED_FACE ( 'NONE', ( #16588 ), #319, .F. ) ;
#14132=LINE ( 'NONE', #24396, #1114 ) ;
#14139=VERTEX_POINT ( 'NONE', #12281 ) ;
#14150=FACE_OUTER_BOUND ( 'NONE', #36246, .T. ) ;
#14155=CYLINDRICAL_SURFACE ( 'NONE', #11934, 0.1749999999999998224 ) ;
#14162=ORIENTED_EDGE ( 'NONE', *, *, #5131, .T. ) ;
#14164=AXIS2_PLACEMENT_3D ( 'NONE', #6314, #27882, #49457 ) ;
#14165=ADVANCED_FACE ( 'NONE', ( #38825 ), #34197, .F. ) ;
#14166=CARTESIAN_POINT ( 'NONE',  ( 7.186223737882818874, -5.257023737882825287, 54.00000000000000711 ) ) ;
#14173=ORIENTED_EDGE ( 'NONE', *, *, #47526, .F. ) ;
#14175=CIRCLE ( 'NONE', #34441, 1.224999999999999423 ) ;
#14182=VECTOR ( 'NONE', #38785, 1000.000000000000114 ) ;
#14184=CARTESIAN_POINT ( 'NONE',  ( 4.961189459950040792, 7.342976262117206332, 26.00000000000000711 ) ) ;
#14190=VERTEX_POINT ( 'NONE', #6651 ) ;
#14208=EDGE_CURVE ( 'NONE', #37440, #21386, #11597, .T. ) ;
#14219=EDGE_CURVE ( 'NONE', #1371, #330, #597, .T. ) ;
#14221=AXIS2_PLACEMENT_3D ( 'NONE', #3773, #26396, #64577 ) ;
#14242=ORIENTED_EDGE ( 'NONE', *, *, #30535, .T. ) ;
#14244=DIRECTION ( 'NONE',  ( 0.000000000000000000, 1.000000000000000000, 0.000000000000000000 ) ) ;
#14247=ORIENTED_EDGE ( 'NONE', *, *, #545, .T. ) ;
#14266=ADVANCED_FACE ( 'NONE', ( #68502 ), #3444, .F. ) ;
#14276=VERTEX_POINT ( 'NONE', #41619 ) ;
#14280=ORIENTED_EDGE ( 'NONE', *, *, #46153, .T. ) ;
#14283=AXIS2_PLACEMENT_3D ( 'NONE', #34341, #28362, #2528 ) ;
#14286=ADVANCED_FACE ( 'NONE', ( #40563 ), #25011, .F. ) ;
#14293=DIRECTION ( 'NONE',  ( -3.304235192336781428E-15, -1.000000000000000000, 0.000000000000000000 ) ) ;
#14296=DIRECTION ( 'NONE',  ( -1.047444401652940007E-14, -1.000000000000000000, -1.836970198721029934E-16 ) ) ;
#14297=CARTESIAN_POINT ( 'NONE',  ( 9.703773737882814387, 8.566576262117184370, 54.00000000000000711 ) ) ;
#14305=ORIENTED_EDGE ( 'NONE', *, *, #59327, .F. ) ;
#14310=ADVANCED_FACE ( 'NONE', ( #3788 ), #25361, .F. ) ;
#14318=DIRECTION ( 'NONE',  ( 1.836970198721029934E-16, 1.836970198721010706E-16, -1.000000000000000000 ) ) ;
#14322=DIRECTION ( 'NONE',  ( 0.8660254037844363761, -0.5000000000000038858, -1.836970198721044232E-16 ) ) ;
#14328=VECTOR ( 'NONE', #55507, 1000.000000000000000 ) ;
#14329=VECTOR ( 'NONE', #68904, 1000.000000000000000 ) ;
#14336=AXIS2_PLACEMENT_3D ( 'NONE', #7727, #18333, #66082 ) ;
#14345=ORIENTED_EDGE ( 'NONE', *, *, #64781, .T. ) ;
#14349=CARTESIAN_POINT ( 'NONE',  ( 9.562023737882764607, 2.355476262117153663, 54.00000000000000711 ) ) ;
#14360=ORIENTED_EDGE ( 'NONE', *, *, #17660, .T. ) ;
#14371=AXIS2_PLACEMENT_3D ( 'NONE', #24648, #14736, #40896 ) ;
#14380=ORIENTED_EDGE ( 'NONE', *, *, #19426, .T. ) ;
#14398=ADVANCED_FACE ( 'NONE', ( #20401 ), #41969, .T. ) ;
#14406=VERTEX_POINT ( 'NONE', #4501 ) ;
#14408=CARTESIAN_POINT ( 'NONE',  ( 5.257023737882801306, 5.242976262117200470, 54.00000000000000711 ) ) ;
#14409=DIRECTION ( 'NONE',  ( -0.8660254037844363761, 0.5000000000000038858, -0.000000000000000000 ) ) ;
#14412=CARTESIAN_POINT ( 'NONE',  ( 5.257023737882801306, 5.242976262117200470, 54.00000000000000711 ) ) ;
#14420=ORIENTED_EDGE ( 'NONE', *, *, #53513, .T. ) ;
#14429=CIRCLE ( 'NONE', #9901, 0.3499999999999996447 ) ;
#14430=VECTOR ( 'NONE', #66535, 1000.000000000000000 ) ;
#14444=ORIENTED_EDGE ( 'NONE', *, *, #5254, .T. ) ;
#14448=EDGE_CURVE ( 'NONE', #29117, #44931, #69543, .T. ) ;
#14457=DIRECTION ( 'NONE',  ( -0.000000000000000000, -0.000000000000000000, -1.000000000000000000 ) ) ;
#14458=ORIENTED_EDGE ( 'NONE', *, *, #56249, .F. ) ;
#14463=CARTESIAN_POINT ( 'NONE',  ( 8.711985858128693749, -2.420780051175170478, 26.00000000000000711 ) ) ;
#14470=PLANE ( 'NONE',  #10311 ) ;
#14473=CARTESIAN_POINT ( 'NONE',  ( -3.142976262117251451, 6.486996718459839606, 54.00000000000000711 ) ) ;
#14476=FACE_OUTER_BOUND ( 'NONE', #23008, .T. ) ;
#14482=EDGE_LOOP ( 'NONE', ( #65484, #12233, #62603, #38975 ) ) ;
#14484=EDGE_CURVE ( 'NONE', #58198, #1953, #59344, .T. ) ;
#14499=EDGE_LOOP ( 'NONE', ( #47694, #49786, #49107, #4644 ) ) ;
#14505=ORIENTED_EDGE ( 'NONE', *, *, #16011, .T. ) ;
#14511=DIRECTION ( 'NONE',  ( 1.000000000000000000, 2.135044278125301343E-15, -0.000000000000000000 ) ) ;
#14516=DIRECTION ( 'NONE',  ( 0.8660254037844383745, 0.5000000000000004441, -0.000000000000000000 ) ) ;
#14517=ORIENTED_EDGE ( 'NONE', *, *, #20290, .T. ) ;
#14519=EDGE_LOOP ( 'NONE', ( #60985, #43817, #58441, #60067 ) ) ;
#14530=PLANE ( 'NONE',  #35657 ) ;
#14537=VECTOR ( 'NONE', #44627, 1000.000000000000000 ) ;
#14548=CARTESIAN_POINT ( 'NONE',  ( 7.969523737882818537, -9.737023737882820384, 54.00000000000000711 ) ) ;
#14550=CARTESIAN_POINT ( 'NONE',  ( -2.530476262117233865, 8.821682069070682530, 54.00000000000000711 ) ) ;
#14556=EDGE_CURVE ( 'NONE', #829, #15613, #55367, .T. ) ;
#14568=EDGE_CURVE ( 'NONE', #18679, #22860, #60306, .T. ) ;
#14570=AXIS2_PLACEMENT_3D ( 'NONE', #37916, #28670, #23375 ) ;
#14572=ORIENTED_EDGE ( 'NONE', *, *, #27902, .T. ) ;
#14583=VERTEX_POINT ( 'NONE', #65956 ) ;
#14585=DIRECTION ( 'NONE',  ( 0.000000000000000000, -3.673940397442059868E-16, 1.000000000000000000 ) ) ;
#14598=ORIENTED_EDGE ( 'NONE', *, *, #57260, .F. ) ;
#14600=ORIENTED_EDGE ( 'NONE', *, *, #20759, .T. ) ;
#14602=VERTEX_POINT ( 'NONE', #11515 ) ;
#14603=CARTESIAN_POINT ( 'NONE',  ( -6.651770455163739548, 7.342976262117183239, 54.00000000000000711 ) ) ;
#14604=LINE ( 'NONE', #35818, #27607 ) ;
#14621=VECTOR ( 'NONE', #69554, 1000.000000000000000 ) ;
#14622=ORIENTED_EDGE ( 'NONE', *, *, #60722, .F. ) ;
#14624=DIRECTION ( 'NONE',  ( -0.000000000000000000, -0.000000000000000000, -1.000000000000000000 ) ) ;
#14670=VECTOR ( 'NONE', #13968, 1000.000000000000000 ) ;
#14679=AXIS2_PLACEMENT_3D ( 'NONE', #69624, #10218, #59348 ) ;
#14684=AXIS2_PLACEMENT_3D ( 'NONE', #48065, #53382, #10577 ) ;
#14686=ORIENTED_EDGE ( 'NONE', *, *, #28893, .T. ) ;
#14704=ORIENTED_EDGE ( 'NONE', *, *, #27795, .F. ) ;
#14706=UNCERTAINTY_MEASURE_WITH_UNIT (LENGTH_MEASURE( 1.000000000000000082E-05 ), #68, 'distance_accuracy_value', 'NONE');
#14710=DIRECTION ( 'NONE',  ( 0.7071067811865514585, 0.7071067811865435759, -0.000000000000000000 ) ) ;
#14711=CARTESIAN_POINT ( 'NONE',  ( 6.789561617636943325, -7.408280051175168524, 26.00000000000000000 ) ) ;
#14712=VECTOR ( 'NONE', #13732, 1000.000000000000000 ) ;
#14724=PLANE ( 'NONE',  #59392 ) ;
#14725=DIRECTION ( 'NONE',  ( -0.000000000000000000, 3.673940397442059868E-16, -1.000000000000000000 ) ) ;
#14728=CARTESIAN_POINT ( 'NONE',  ( 5.552858015815566262, 7.342976262117203667, 26.00000000000000711 ) ) ;
#14733=CIRCLE ( 'NONE', #7899, 0.1749999999999980738 ) ;
#14736=DIRECTION ( 'NONE',  ( 1.836970198721029934E-16, 1.836970198721010706E-16, -1.000000000000000000 ) ) ;
#14738=AXIS2_PLACEMENT_3D ( 'NONE', #6777, #44261, #49580 ) ;
#14746=FACE_OUTER_BOUND ( 'NONE', #17681, .T. ) ;
#14749=ORIENTED_EDGE ( 'NONE', *, *, #45261, .F. ) ;
#14757=CARTESIAN_POINT ( 'NONE',  ( -6.822336235477484578, -6.364920264886849921, 26.00000000000000711 ) ) ;
#14761=CIRCLE ( 'NONE', #55437, 0.5250000000000003553 ) ;
#14765=DIRECTION ( 'NONE',  ( -1.836970198721029934E-16, 1.836970198721036590E-16, -1.000000000000000000 ) ) ;
#14767=DIRECTION ( 'NONE',  ( -1.836970198721029934E-16, 1.836970198721036590E-16, -1.000000000000000000 ) ) ;
#14769=EDGE_LOOP ( 'NONE', ( #63130, #57081, #63630, #30762 ) ) ;
#14770=DIRECTION ( 'NONE',  ( -0.000000000000000000, -0.000000000000000000, -1.000000000000000000 ) ) ;
#14771=AXIS2_PLACEMENT_3D ( 'NONE', #45929, #67140, #62179 ) ;
#14777=VECTOR ( 'NONE', #38218, 1000.000000000000000 ) ;
#14791=VECTOR ( 'NONE', #68771, 1000.000000000000114 ) ;
#14797=VERTEX_POINT ( 'NONE', #36228 ) ;
#14800=EDGE_CURVE ( 'NONE', #52916, #55613, #20662, .T. ) ;
#14805=DIRECTION ( 'NONE',  ( -1.000000000000000000, 0.000000000000000000, 0.000000000000000000 ) ) ;
#14816=CARTESIAN_POINT ( 'NONE',  ( -8.598420958951683346, 1.991476262117183316, 54.00000000000000711 ) ) ;
#14819=CARTESIAN_POINT ( 'NONE',  ( -10.49297626211726175, 6.835476262117182955, 54.00000000000000711 ) ) ;
#14820=DIRECTION ( 'NONE',  ( -8.612436249475772606E-15, -1.000000000000000000, -1.836970198721020566E-16 ) ) ;
#14823=VERTEX_POINT ( 'NONE', #69461 ) ;
#14825=DIRECTION ( 'NONE',  ( 1.047444401652940007E-14, 1.000000000000000000, 1.836970198721029934E-16 ) ) ;
#14837=VERTEX_POINT ( 'NONE', #63461 ) ;
#14843=AXIS2_PLACEMENT_3D ( 'NONE', #13177, #60918, #2574 ) ;
#14848=LINE ( 'NONE', #25812, #2209 ) ;
#14853=LINE ( 'NONE', #6323, #67978 ) ;
#14855=VERTEX_POINT ( 'NONE', #31991 ) ;
#14860=ORIENTED_EDGE ( 'NONE', *, *, #37957, .F. ) ;
#14866=CARTESIAN_POINT ( 'NONE',  ( -9.781776262117247711, 9.781776262117171328, 54.00000000000000711 ) ) ;
#14872=CARTESIAN_POINT ( 'NONE',  ( -3.842976262117329345, -9.912023737882817542, 54.00000000000000711 ) ) ;
#14874=ORIENTED_EDGE ( 'NONE', *, *, #39823, .F. ) ;
#14881=CIRCLE ( 'NONE', #26191, 0.1749999999999980738 ) ;
#14892=ORIENTED_EDGE ( 'NONE', *, *, #18270, .F. ) ;
#14897=CYLINDRICAL_SURFACE ( 'NONE', #47026, 1.224999999999999423 ) ;
#14922=ADVANCED_FACE ( 'NONE', ( #22421 ), #38674, .F. ) ;
#14928=DIRECTION ( 'NONE',  ( 0.6414496315691645689, 0.7671651518152939886, 0.000000000000000000 ) ) ;
#14929=FACE_OUTER_BOUND ( 'NONE', #35207, .T. ) ;
#14930=VECTOR ( 'NONE', #25076, 1000.000000000000000 ) ;
#14947=ORIENTED_EDGE ( 'NONE', *, *, #55895, .T. ) ;
#14951=PLANE ( 'NONE',  #60203 ) ;
#14955=CARTESIAN_POINT ( 'NONE',  ( -6.817976262117261044, 9.897976262117179402, 26.00000000000000711 ) ) ;
#14959=EDGE_LOOP ( 'NONE', ( #64811, #52833, #56719, #59942 ) ) ;
#14961=CARTESIAN_POINT ( 'NONE',  ( 8.835729544836331328, 7.955476262117188391, 54.00000000000000711 ) ) ;
#14964=EDGE_CURVE ( 'NONE', #51473, #67681, #503, .T. ) ;
#14971=EDGE_CURVE ( 'NONE', #355, #45686, #55286, .T. ) ;
#14974=VECTOR ( 'NONE', #37712, 1000.000000000000000 ) ;
#14989=EDGE_LOOP ( 'NONE', ( #10314, #21586, #21390, #17515 ) ) ;
#15000=CARTESIAN_POINT ( 'NONE',  ( -1.466476262117230034, 9.390476262117152473, 54.00000000000000711 ) ) ;
#15001=AXIS2_PLACEMENT_3D ( 'NONE', #56468, #25000, #61778 ) ;
#15008=AXIS2_PLACEMENT_3D ( 'NONE', #5343, #47407, #16277 ) ;
#15010=ORIENTED_EDGE ( 'NONE', *, *, #58692, .T. ) ;
#15019=LINE ( 'NONE', #10415, #53165 ) ;
#15024=LINE ( 'NONE', #41182, #46369 ) ;
#15029=LINE ( 'NONE', #36586, #11280 ) ;
#15030=DIRECTION ( 'NONE',  ( -2.135044278125299371E-15, -1.000000000000000000, 0.000000000000000000 ) ) ;
#15032=ADVANCED_FACE ( 'NONE', ( #31524 ), #53435, .F. ) ;
#15037=ORIENTED_EDGE ( 'NONE', *, *, #42969, .F. ) ;
#15039=EDGE_CURVE ( 'NONE', #44524, #64431, #4310, .T. ) ;
#15040=ORIENTED_EDGE ( 'NONE', *, *, #42673, .T. ) ;
#15044=VECTOR ( 'NONE', #29025, 1000.000000000000114 ) ;
#15060=DIRECTION ( 'NONE',  ( 1.836970198721029934E-16, -1.836970198721036344E-16, 1.000000000000000000 ) ) ;
#15066=ORIENTED_EDGE ( 'NONE', *, *, #51215, .F. ) ;
#15067=ORIENTED_EDGE ( 'NONE', *, *, #54161, .F. ) ;
#15082=DIRECTION ( 'NONE',  ( 1.000000000000000000, 0.000000000000000000, 0.000000000000000000 ) ) ;
#15084=DIRECTION ( 'NONE',  ( 1.000000000000000000, -1.678252938371784572E-14, 1.836970198720999119E-16 ) ) ;
#15099=CARTESIAN_POINT ( 'NONE',  ( -2.530476262117229425, 9.547976262117158441, 54.00000000000000711 ) ) ;
#15102=EDGE_CURVE ( 'NONE', #11645, #43624, #63337, .T. ) ;
#15106=DIRECTION ( 'NONE',  ( -0.000000000000000000, -0.000000000000000000, -1.000000000000000000 ) ) ;
#15148=CARTESIAN_POINT ( 'NONE',  ( -6.835476262117260227, 10.49297626211718359, 54.00000000000000711 ) ) ;
#15152=ORIENTED_EDGE ( 'NONE', *, *, #61100, .T. ) ;
#15160=AXIS2_PLACEMENT_3D ( 'NONE', #8853, #36072, #30425 ) ;
#15163=VECTOR ( 'NONE', #34525, 1000.000000000000000 ) ;
#15168=ORIENTED_EDGE ( 'NONE', *, *, #31386, .T. ) ;
#15173=CYLINDRICAL_SURFACE ( 'NONE', #13795, 1.929199999999998028 ) ;
#15181=EDGE_CURVE ( 'NONE', #47019, #42883, #16651, .T. ) ;
#15186=CARTESIAN_POINT ( 'NONE',  ( 3.848229544836324845, 7.342976262117209885, 26.00000000000000711 ) ) ;
#15187=ADVANCED_FACE ( 'NONE', ( #44523 ), #49164, .T. ) ;
#15190=PLANE ( 'NONE',  #36584 ) ;
#15196=CYLINDRICAL_SURFACE ( 'NONE', #47885, 0.5249999999999994671 ) ;
#15200=VECTOR ( 'NONE', #52221, 1000.000000000000000 ) ;
#15201=VECTOR ( 'NONE', #47055, 1000.000000000000000 ) ;
#15214=VERTEX_POINT ( 'NONE', #65428 ) ;
#15217=VERTEX_POINT ( 'NONE', #38221 ) ;
#15219=CARTESIAN_POINT ( 'NONE',  ( 6.849523737882817542, -10.31452373788282095, 54.00000000000000711 ) ) ;
#15228=CARTESIAN_POINT ( 'NONE',  ( -3.663616288757094885, -6.364920264886888113, 54.00000000000000711 ) ) ;
#15233=EDGE_CURVE ( 'NONE', #7480, #9302, #15437, .T. ) ;
#15238=DIRECTION ( 'NONE',  ( 0.000000000000000000, -3.673940397442059868E-16, 1.000000000000000000 ) ) ;
#15256=VECTOR ( 'NONE', #7347, 1000.000000000000000 ) ;
#15257=CARTESIAN_POINT ( 'NONE',  ( 8.612468434717241550, -2.005523737882825674, 54.00000000000000711 ) ) ;
#15260=DIRECTION ( 'NONE',  ( 1.000000000000000000, 0.000000000000000000, 0.000000000000000000 ) ) ;
#15273=EDGE_CURVE ( 'NONE', #36105, #12301, #38887, .T. ) ;
#15274=CARTESIAN_POINT ( 'NONE',  ( -3.650476262117333892, -10.31452373788281740, 54.00000000000000711 ) ) ;
#15275=EDGE_CURVE ( 'NONE', #38702, #41857, #16551, .T. ) ;
#15278=PLANE ( 'NONE',  #26896 ) ;
#15287=DIRECTION ( 'NONE',  ( 1.836970198721029934E-16, 1.836970198721010706E-16, -1.000000000000000000 ) ) ;
#15293=CARTESIAN_POINT ( 'NONE',  ( 9.929523737882748335, 0.9414762621171531842, 26.00000000000000711 ) ) ;
#15305=CARTESIAN_POINT ( 'NONE',  ( 1.634292677759859869, -8.241237374594271969, 26.00000000000000000 ) ) ;
#15306=ORIENTED_EDGE ( 'NONE', *, *, #18200, .F. ) ;
#15316=ORIENTED_EDGE ( 'NONE', *, *, #33580, .T. ) ;
#15324=VERTEX_POINT ( 'NONE', #18015 ) ;
#15332=VECTOR ( 'NONE', #24637, 1000.000000000000000 ) ;
#15334=ORIENTED_EDGE ( 'NONE', *, *, #42880, .T. ) ;
#15337=DIRECTION ( 'NONE',  ( -1.836970198721029934E-16, 1.836970198721036344E-16, -1.000000000000000000 ) ) ;
#15338=VECTOR ( 'NONE', #25368, 1000.000000000000000 ) ;
#15352=CARTESIAN_POINT ( 'NONE',  ( 9.737023737882804397, 6.817976262117185549, 54.00000000000000711 ) ) ;
#15353=AXIS2_PLACEMENT_3D ( 'NONE', #16467, #55671, #38046 ) ;
#15360=EDGE_CURVE ( 'NONE', #3338, #6044, #8448, .T. ) ;
#15368=LINE ( 'NONE', #31294, #32088 ) ;
#15369=EDGE_CURVE ( 'NONE', #10245, #61001, #42541, .T. ) ;
#15390=DIRECTION ( 'NONE',  ( -0.000000000000000000, 3.673940397442059868E-16, -1.000000000000000000 ) ) ;
#15396=LINE ( 'NONE', #36603, #44433 ) ;
#15404=CIRCLE ( 'NONE', #63964, 0.1749999999999998224 ) ;
#15405=VECTOR ( 'NONE', #25572, 1000.000000000000000 ) ;
#15406=AXIS2_PLACEMENT_3D ( 'NONE', #21908, #48789, #10601 ) ;
#15421=EDGE_LOOP ( 'NONE', ( #60687, #54626, #69198, #2256 ) ) ;
#15423=EDGE_CURVE ( 'NONE', #57811, #58579, #40287, .T. ) ;
#15424=LINE ( 'NONE', #37683, #25550 ) ;
#15427=ORIENTED_EDGE ( 'NONE', *, *, #7771, .T. ) ;
#15436=CARTESIAN_POINT ( 'NONE',  ( -10.30047626211724854, -3.664523737882715348, 54.00000000000000711 ) ) ;
#15437=CIRCLE ( 'NONE', #67367, 1.929199999999998028 ) ;
#15439=DIRECTION ( 'NONE',  ( 1.047444401652940007E-14, 1.000000000000000000, 1.836970198721029934E-16 ) ) ;
#15442=LINE ( 'NONE', #37023, #60 ) ;
#15444=CARTESIAN_POINT ( 'NONE',  ( 1.634292677759859869, -8.241237374594282628, 54.00000000000000711 ) ) ;
#15450=VERTEX_POINT ( 'NONE', #28629 ) ;
#15457=DIRECTION ( 'NONE',  ( -4.956352788505168198E-15, -1.000000000000000000, 0.000000000000000000 ) ) ;
#15464=LINE ( 'NONE', #21798, #22001 ) ;
#15471=ORIENTED_EDGE ( 'NONE', *, *, #12596, .T. ) ;
#15477=ADVANCED_FACE ( 'NONE', ( #14476 ), #30735, .F. ) ;
#15483=VERTEX_POINT ( 'NONE', #47344 ) ;
#15487=EDGE_CURVE ( 'NONE', #69903, #48157, #20473, .T. ) ;
#15495=ORIENTED_EDGE ( 'NONE', *, *, #15903, .F. ) ;
#15510=ORIENTED_EDGE ( 'NONE', *, *, #18524, .F. ) ;
#15513=VECTOR ( 'NONE', #1, 1000.000000000000000 ) ;
#15521=AXIS2_PLACEMENT_3D ( 'NONE', #43505, #48831, #11325 ) ;
#15522=DIRECTION ( 'NONE',  ( -1.000000000000000000, 0.000000000000000000, 0.000000000000000000 ) ) ;
#15529=CARTESIAN_POINT ( 'NONE',  ( 6.358413763958968623, -4.720772854004779973, 26.00000000000000711 ) ) ;
#15530=CARTESIAN_POINT ( 'NONE',  ( -5.242976262117280406, -5.257023737882805747, 54.00000000000000711 ) ) ;
#15532=LINE ( 'NONE', #4911, #43724 ) ;
#15549=ADVANCED_FACE ( 'NONE', ( #69265 ), #25085, .F. ) ;
#15552=CARTESIAN_POINT ( 'NONE',  ( -9.722976262117221324, -2.544523737882721015, 26.00000000000000711 ) ) ;
#15560=LINE ( 'NONE', #37120, #27154 ) ;
#15561=EDGE_CURVE ( 'NONE', #19581, #44397, #43421, .T. ) ;
#15565=VERTEX_POINT ( 'NONE', #37786 ) ;
#15570=DIRECTION ( 'NONE',  ( 0.7071067811865441310, -0.7071067811865510144, -2.597868168706485034E-16 ) ) ;
#15589=CARTESIAN_POINT ( 'NONE',  ( 5.257023737882798642, 6.467976262117203667, 26.00000000000000711 ) ) ;
#15591=EDGE_LOOP ( 'NONE', ( #67673, #12806, #20218, #29618 ) ) ;
#15592=ADVANCED_FACE ( 'NONE', ( #22561 ), #26837, .F. ) ;
#15593=LINE ( 'NONE', #65066, #6201 ) ;
#15608=DIRECTION ( 'NONE',  ( 1.836970198721029934E-16, 1.836970198721010706E-16, -1.000000000000000000 ) ) ;
#15613=VERTEX_POINT ( 'NONE', #5950 ) ;
#15616=DIRECTION ( 'NONE',  ( -1.000000000000000000, 3.903627567395476653E-15, 1.836970198721037083E-16 ) ) ;
#15619=EDGE_CURVE ( 'NONE', #19590, #24664, #22221, .T. ) ;
#15621=CARTESIAN_POINT ( 'NONE',  ( 9.562023737882812569, -8.144523737882813919, 26.00000000000000000 ) ) ;
#15634=DIRECTION ( 'NONE',  ( 2.309061475090597584E-14, 1.000000000000000000, 1.836970198721053107E-16 ) ) ;
#15650=VERTEX_POINT ( 'NONE', #44115 ) ;
#15652=DIRECTION ( 'NONE',  ( 0.000000000000000000, 1.000000000000000000, 0.000000000000000000 ) ) ;
#15654=DIRECTION ( 'NONE',  ( -1.000000000000000000, 1.185108578570163402E-14, 1.836970198721051628E-16 ) ) ;
#15662=ORIENTED_EDGE ( 'NONE', *, *, #22049, .F. ) ;
#15668=CARTESIAN_POINT ( 'NONE',  ( 10.50702373788278265, 3.650476262117142934, 54.00000000000000711 ) ) ;
#15670=VERTEX_POINT ( 'NONE', #48740 ) ;
#15675=EDGE_CURVE ( 'NONE', #36429, #59980, #817, .T. ) ;
#15681=ADVANCED_FACE ( 'NONE', ( #64649 ), #10911, .F. ) ;
#15682=ADVANCED_FACE ( 'NONE', ( #40545 ), #44451, .F. ) ;
#15684=ORIENTED_EDGE ( 'NONE', *, *, #65886, .F. ) ;
#15692=CARTESIAN_POINT ( 'NONE',  ( 6.849523737882818430, 10.49297626211719603, 54.00000000000000711 ) ) ;
#15693=CARTESIAN_POINT ( 'NONE',  ( 9.795823737882805915, -9.795823737882811244, 54.00000000000000711 ) ) ;
#15698=ORIENTED_EDGE ( 'NONE', *, *, #33375, .F. ) ;
#15707=CARTESIAN_POINT ( 'NONE',  ( -1.620245201994301665, 8.227189898828640935, 54.00000000000000711 ) ) ;
#15708=ORIENTED_EDGE ( 'NONE', *, *, #8069, .T. ) ;
#15709=DIRECTION ( 'NONE',  ( 1.836970198721029934E-16, 1.836970198721010706E-16, -1.000000000000000000 ) ) ;
#15722=ORIENTED_EDGE ( 'NONE', *, *, #32760, .T. ) ;
#15723=DIRECTION ( 'NONE',  ( -0.000000000000000000, -0.000000000000000000, -1.000000000000000000 ) ) ;
#15727=PLANE ( 'NONE',  #56868 ) ;
#15734=DIRECTION ( 'NONE',  ( 8.359604446858500663E-15, 1.000000000000000000, 3.673940397442059868E-16 ) ) ;
#15743=CIRCLE ( 'NONE', #62052, 0.7112000000000124889 ) ;
#15745=CARTESIAN_POINT ( 'NONE',  ( 9.795823737882807691, 10.49297626211718537, 54.00000000000000711 ) ) ;
#15748=ORIENTED_EDGE ( 'NONE', *, *, #47671, .T. ) ;
#15752=ORIENTED_EDGE ( 'NONE', *, *, #48964, .T. ) ;
#15759=VECTOR ( 'NONE', #61330, 1000.000000000000000 ) ;
#15764=EDGE_LOOP ( 'NONE', ( #38969, #23029, #64634, #62267 ) ) ;
#15768=ORIENTED_EDGE ( 'NONE', *, *, #22748, .T. ) ;
#15773=CARTESIAN_POINT ( 'NONE',  ( 3.682023737882818448, 9.722976262117203561, 54.00000000000000711 ) ) ;
#15774=ORIENTED_EDGE ( 'NONE', *, *, #40550, .T. ) ;
#15779=DIRECTION ( 'NONE',  ( -1.836970198721029934E-16, 1.836970198721036590E-16, -1.000000000000000000 ) ) ;
#15781=DIRECTION ( 'NONE',  ( -2.135044278125299371E-15, -1.000000000000000000, -3.673940397442060361E-16 ) ) ;
#15790=AXIS2_PLACEMENT_3D ( 'NONE', #48044, #14825, #26481 ) ;
#15791=CARTESIAN_POINT ( 'NONE',  ( -6.822336235477446387, -4.149127210878696737, 54.00000000000000711 ) ) ;
#15794=DIRECTION ( 'NONE',  ( -1.000000000000000000, 0.000000000000000000, 0.000000000000000000 ) ) ;
#15795=CARTESIAN_POINT ( 'NONE',  ( -8.079219948824906794, 8.697938382363059162, 54.00000000000000711 ) ) ;
#15797=ADVANCED_FACE ( 'NONE', ( #2029 ), #39164, .F. ) ;
#15802=VERTEX_POINT ( 'NONE', #45146 ) ;
#15806=CARTESIAN_POINT ( 'NONE',  ( 6.836383711242975281, 4.135079735113102117, 54.00000000000000711 ) ) ;
#15821=DIRECTION ( 'NONE',  ( 1.062075597536821205E-14, 1.000000000000000000, 0.000000000000000000 ) ) ;
#15822=ORIENTED_EDGE ( 'NONE', *, *, #58473, .T. ) ;
#15833=CARTESIAN_POINT ( 'NONE',  ( -9.722976262117258628, 7.605476262117193187, 54.00000000000000711 ) ) ;
#15836=CARTESIAN_POINT ( 'NONE',  ( 6.657023737882818537, -10.31452373788281207, 26.00000000000000000 ) ) ;
#15845=EDGE_CURVE ( 'NONE', #56572, #16440, #20731, .T. ) ;
#15853=CARTESIAN_POINT ( 'NONE',  ( -3.663616288757055806, 4.135079735113128763, 54.00000000000000711 ) ) ;
#15866=LINE ( 'NONE', #69617, #53347 ) ;
#15873=CARTESIAN_POINT ( 'NONE',  ( -3.663616288757055806, 4.135079735113128763, 54.00000000000000711 ) ) ;
#15881=VERTEX_POINT ( 'NONE', #25347 ) ;
#15894=VERTEX_POINT ( 'NONE', #67771 ) ;
#15895=LINE ( 'NONE', #21213, #20532 ) ;
#15897=ORIENTED_EDGE ( 'NONE', *, *, #56336, .F. ) ;
#15898=VECTOR ( 'NONE', #39078, 1000.000000000000000 ) ;
#15900=EDGE_CURVE ( 'NONE', #18742, #65963, #46197, .T. ) ;
#15903=EDGE_CURVE ( 'NONE', #45362, #3520, #44830, .T. ) ;
#15905=ORIENTED_EDGE ( 'NONE', *, *, #48320, .T. ) ;
#15919=DIRECTION ( 'NONE',  ( 9.912705577010336396E-15, 1.000000000000000000, 0.000000000000000000 ) ) ;
#15920=ORIENTED_EDGE ( 'NONE', *, *, #15233, .F. ) ;
#15921=DIRECTION ( 'NONE',  ( -1.836970198721029934E-16, 1.836970198721036344E-16, -1.000000000000000000 ) ) ;
#15926=SHAPE_REPRESENTATION ( '5537T808_T-Slotted Framing_5537T808', ( #45918 ), #44782 ) ;
#15928=AXIS2_PLACEMENT_3D ( 'NONE', #12246, #39133, #39471 ) ;
#15937=ADVANCED_FACE ( 'NONE', ( #3426 ), #46546, .F. ) ;
#15938=DIRECTION ( 'NONE',  ( -1.000000000000000000, -2.135044278125299371E-15, 0.000000000000000000 ) ) ;
#15946=VERTEX_POINT ( 'NONE', #8362 ) ;
#15959=VERTEX_POINT ( 'NONE', #47265 ) ;
#15964=VERTEX_POINT ( 'NONE', #41954 ) ;
#15966=DIRECTION ( 'NONE',  ( -7.665540703601096574E-15, -1.000000000000000000, -3.673940397442059868E-16 ) ) ;
#15976=EDGE_LOOP ( 'NONE', ( #11110, #67863, #24176, #58626 ) ) ;
#15981=ORIENTED_EDGE ( 'NONE', *, *, #40333, .F. ) ;
#15985=LINE ( 'NONE', #30848, #42246 ) ;
#15988=ORIENTED_EDGE ( 'NONE', *, *, #44467, .F. ) ;
#15989=ORIENTED_EDGE ( 'NONE', *, *, #25163, .F. ) ;
#15992=ORIENTED_EDGE ( 'NONE', *, *, #4647, .T. ) ;
#15996=CARTESIAN_POINT ( 'NONE',  ( 3.682023737882786918, -9.737023737882811503, 54.00000000000000711 ) ) ;
#16005=DIRECTION ( 'NONE',  ( -1.000000000000000000, 0.000000000000000000, 0.000000000000000000 ) ) ;
#16010=EDGE_CURVE ( 'NONE', #30669, #50794, #37022, .T. ) ;
#16011=EDGE_CURVE ( 'NONE', #55364, #66440, #47960, .T. ) ;
#16013=DIRECTION ( 'NONE',  ( 1.261617073437657735E-14, 1.000000000000000000, 3.673940397442059868E-16 ) ) ;
#16014=CARTESIAN_POINT ( 'NONE',  ( 2.369523737882815784, 8.821682069070730492, 54.00000000000000711 ) ) ;
#16015=EDGE_CURVE ( 'NONE', #19298, #6935, #11162, .T. ) ;
#16025=CARTESIAN_POINT ( 'NONE',  ( -2.355476262117234931, 8.821682069070680754, 54.00000000000000711 ) ) ;
#16033=VECTOR ( 'NONE', #46695, 1000.000000000000000 ) ;
#16037=ORIENTED_EDGE ( 'NONE', *, *, #63829, .T. ) ;
#16041=DIRECTION ( 'NONE',  ( 0.000000000000000000, -1.000000000000000000, 0.000000000000000000 ) ) ;
#16053=AXIS2_PLACEMENT_3D ( 'NONE', #43804, #39779, #66665 ) ;
#16061=DIRECTION ( 'NONE',  ( -1.000000000000000000, 0.000000000000000000, 0.000000000000000000 ) ) ;
#16064=CIRCLE ( 'NONE', #55572, 0.1749999999999989342 ) ;
#16069=EDGE_CURVE ( 'NONE', #64431, #3937, #31354, .T. ) ;
#16070=EDGE_CURVE ( 'NONE', #5714, #22259, #65280, .T. ) ;
#16076=ORIENTED_EDGE ( 'NONE', *, *, #63826, .T. ) ;
#16083=DIRECTION ( 'NONE',  ( -1.836970198721029934E-16, 1.836970198721036590E-16, -1.000000000000000000 ) ) ;
#16090=DIRECTION ( 'NONE',  ( -1.000000000000000000, 0.000000000000000000, 0.000000000000000000 ) ) ;
#16093=ORIENTED_EDGE ( 'NONE', *, *, #64123, .T. ) ;
#16096=ORIENTED_EDGE ( 'NONE', *, *, #11357, .F. ) ;
#16098=VECTOR ( 'NONE', #39027, 1000.000000000000000 ) ;
#16104=ORIENTED_EDGE ( 'NONE', *, *, #15487, .T. ) ;
#16112=VECTOR ( 'NONE', #39424, 1000.000000000000000 ) ;
#16113=CIRCLE ( 'NONE', #29663, 0.7112000000000124889 ) ;
#16117=CARTESIAN_POINT ( 'NONE',  ( -6.486996718459931088, 2.617976262117183150, 26.00000000000000711 ) ) ;
#16118=VECTOR ( 'NONE', #31860, 1000.000000000000000 ) ;
#16126=DIRECTION ( 'NONE',  ( 0.000000000000000000, 1.000000000000000000, 0.000000000000000000 ) ) ;
#16133=ORIENTED_EDGE ( 'NONE', *, *, #22488, .T. ) ;
#16149=EDGE_CURVE ( 'NONE', #35812, #8571, #3611, .T. ) ;
#16151=VECTOR ( 'NONE', #67642, 1000.000000000000000 ) ;
#16152=EDGE_LOOP ( 'NONE', ( #14444, #34409, #67035, #60254 ) ) ;
#16156=VERTEX_POINT ( 'NONE', #49688 ) ;
#16157=CARTESIAN_POINT ( 'NONE',  ( -9.781776262117324094, -10.50702373788275779, 54.00000000000000711 ) ) ;
#16158=VECTOR ( 'NONE', #34651, 1000.000000000000000 ) ;
#16179=ORIENTED_EDGE ( 'NONE', *, *, #18461, .F. ) ;
#16185=DIRECTION ( 'NONE',  ( 0.000000000000000000, 0.000000000000000000, -1.000000000000000000 ) ) ;
#16191=EDGE_CURVE ( 'NONE', #17051, #56170, #51708, .T. ) ;
#16192=DIRECTION ( 'NONE',  ( 1.000000000000000000, 0.000000000000000000, 0.000000000000000000 ) ) ;
#16206=DIRECTION ( 'NONE',  ( 1.000000000000000000, -1.115702204244422993E-14, -1.836970198721050395E-16 ) ) ;
#16211=DIRECTION ( 'NONE',  ( 1.000000000000000000, 0.000000000000000000, 0.000000000000000000 ) ) ;
#16219=CARTESIAN_POINT ( 'NONE',  ( 6.832023737882818359, -9.737023737882822161, 54.00000000000000711 ) ) ;
#16220=FACE_OUTER_BOUND ( 'NONE', #8242, .T. ) ;
#16225=CARTESIAN_POINT ( 'NONE',  ( -10.49297626211724754, -3.664523737882706023, 26.00000000000000000 ) ) ;
#16229=ADVANCED_FACE ( 'NONE', ( #67964 ), #35068, .F. ) ;
#16234=DIRECTION ( 'NONE',  ( -0.000000000000000000, -0.000000000000000000, -1.000000000000000000 ) ) ;
#16239=EDGE_CURVE ( 'NONE', #6189, #18842, #10657, .T. ) ;
#16244=ORIENTED_EDGE ( 'NONE', *, *, #61407, .F. ) ;
#16246=ADVANCED_FACE ( 'NONE', ( #42131 ), #31542, .F. ) ;
#16251=VECTOR ( 'NONE', #30748, 1000.000000000000000 ) ;
#16255=DIRECTION ( 'NONE',  ( -0.000000000000000000, 3.673940397442059868E-16, -1.000000000000000000 ) ) ;
#16256=DIRECTION ( 'NONE',  ( 0.7671651518152939886, -0.6414496315691644579, -2.587583378555133721E-16 ) ) ;
#16259=VECTOR ( 'NONE', #19405, 1000.000000000000000 ) ;
#16260=ORIENTED_EDGE ( 'NONE', *, *, #3136, .T. ) ;
#16269=VERTEX_POINT ( 'NONE', #5010 ) ;
#16277=DIRECTION ( 'NONE',  ( 3.596772705736696467E-15, 1.000000000000000000, 0.000000000000000000 ) ) ;
#16282=CARTESIAN_POINT ( 'NONE',  ( -9.897976262117259338, 6.642976262117183950, 54.00000000000000711 ) ) ;
#16289=EDGE_CURVE ( 'NONE', #22077, #61234, #63009, .T. ) ;
#16297=ORIENTED_EDGE ( 'NONE', *, *, #31252, .T. ) ;
#16303=VECTOR ( 'NONE', #57447, 1000.000000000000000 ) ;
#16307=CIRCLE ( 'NONE', #67117, 0.1749999999999989342 ) ;
#16317=VECTOR ( 'NONE', #33549, 1000.000000000000000 ) ;
#16321=CYLINDRICAL_SURFACE ( 'NONE', #65373, 0.1749999999999989342 ) ;
#16351=AXIS2_PLACEMENT_3D ( 'NONE', #18018, #39924, #18358 ) ;
#16370=CIRCLE ( 'NONE', #17514, 0.1749999999999989342 ) ;
#16374=ORIENTED_EDGE ( 'NONE', *, *, #2570, .T. ) ;
#16380=DIRECTION ( 'NONE',  ( -1.836970198721029934E-16, -1.836970198721010706E-16, 1.000000000000000000 ) ) ;
#16381=DIRECTION ( 'NONE',  ( 1.000000000000000000, 0.000000000000000000, 0.000000000000000000 ) ) ;
#16382=DIRECTION ( 'NONE',  ( -0.000000000000000000, -0.000000000000000000, -1.000000000000000000 ) ) ;
#16385=DIRECTION ( 'NONE',  ( -1.000000000000000000, 8.339399738404099512E-15, -1.836970198721014650E-16 ) ) ;
#16390=DIRECTION ( 'NONE',  ( -2.135044278125299371E-15, 1.000000000000000000, -0.000000000000000000 ) ) ;
#16399=CARTESIAN_POINT ( 'NONE',  ( -6.817976262117261044, 9.722976262117182245, 54.00000000000000711 ) ) ;
#16402=AXIS2_PLACEMENT_3D ( 'NONE', #61738, #56431, #7982 ) ;
#16405=ORIENTED_EDGE ( 'NONE', *, *, #31971, .F. ) ;
#16412=DIRECTION ( 'NONE',  ( -1.000000000000000000, 8.540177112501197482E-15, 3.137610169492823463E-30 ) ) ;
#16424=EDGE_LOOP ( 'NONE', ( #19138, #33965, #37929, #20076 ) ) ;
#16425=EDGE_CURVE ( 'NONE', #45166, #6666, #22326, .T. ) ;
#16432=CARTESIAN_POINT ( 'NONE',  ( 9.703773737882817940, 10.03972626211715280, 54.00000000000000711 ) ) ;
#16433=LINE ( 'NONE', #54615, #56716 ) ;
#16434=ORIENTED_EDGE ( 'NONE', *, *, #28797, .T. ) ;
#16440=VERTEX_POINT ( 'NONE', #21627 ) ;
#16448=ORIENTED_EDGE ( 'NONE', *, *, #13941, .T. ) ;
#16465=VECTOR ( 'NONE', #60845, 1000.000000000000000 ) ;
#16467=CARTESIAN_POINT ( 'NONE',  ( -7.517976262117247899, -3.848229544836279992, 26.00000000000000711 ) ) ;
#16471=FACE_BOUND ( 'NONE', #48150, .T. ) ;
#16475=ORIENTED_EDGE ( 'NONE', *, *, #11771, .F. ) ;
#16481=FACE_OUTER_BOUND ( 'NONE', #13306, .T. ) ;
#16484=CARTESIAN_POINT ( 'NONE',  ( 8.241237374594247100, 1.620245201994230611, 54.00000000000000711 ) ) ;
#16497=CARTESIAN_POINT ( 'NONE',  ( 3.157023737882805214, 6.486996718459879574, 54.00000000000000711 ) ) ;
#16502=VERTEX_POINT ( 'NONE', #22991 ) ;
#16512=AXIS2_PLACEMENT_3D ( 'NONE', #56506, #29627, #23625 ) ;
#16513=CYLINDRICAL_SURFACE ( 'NONE', #11530, 0.7112000000000124889 ) ;
#16515=VECTOR ( 'NONE', #49664, 1000.000000000000000 ) ;
#16520=VERTEX_POINT ( 'NONE', #50570 ) ;
#16537=EDGE_CURVE ( 'NONE', #50609, #37532, #28991, .T. ) ;
#16540=ORIENTED_EDGE ( 'NONE', *, *, #53113, .F. ) ;
#16546=EDGE_CURVE ( 'NONE', #23407, #47795, #66473, .T. ) ;
#16548=EDGE_LOOP ( 'NONE', ( #5491, #38442, #57729, #36394 ) ) ;
#16551=CIRCLE ( 'NONE', #66252, 1.224999999999999423 ) ;
#16555=ORIENTED_EDGE ( 'NONE', *, *, #5131, .F. ) ;
#16565=CIRCLE ( 'NONE', #12045, 0.3499999999999996447 ) ;
#16567=CARTESIAN_POINT ( 'NONE',  ( 9.737023737882804397, 6.817976262117185549, 54.00000000000000711 ) ) ;
#16570=CARTESIAN_POINT ( 'NONE',  ( -1.466476262117230034, 9.390476262117152473, 54.00000000000000711 ) ) ;
#16574=DIRECTION ( 'NONE',  ( 1.836970198721029934E-16, 1.836970198721010706E-16, -1.000000000000000000 ) ) ;
#16579=LINE ( 'NONE', #11931, #52922 ) ;
#16583=LINE ( 'NONE', #665, #9487 ) ;
#16588=FACE_OUTER_BOUND ( 'NONE', #40572, .T. ) ;
#16593=VERTEX_POINT ( 'NONE', #40991 ) ;
#16597=CARTESIAN_POINT ( 'NONE',  ( 8.711985858128693749, -8.093267424590470327, 54.00000000000000711 ) ) ;
#16598=AXIS2_PLACEMENT_3D ( 'NONE', #55178, #1421, #6720 ) ;
#16599=VERTEX_POINT ( 'NONE', #61501 ) ;
#16603=VECTOR ( 'NONE', #10897, 1000.000000000000114 ) ;
#16604=EDGE_CURVE ( 'NONE', #7028, #57266, #7766, .T. ) ;
#16605=CARTESIAN_POINT ( 'NONE',  ( 3.857023737882783188, -9.912023737882810437, 54.00000000000000711 ) ) ;
#16606=VECTOR ( 'NONE', #27179, 1000.000000000000000 ) ;
#16611=CARTESIAN_POINT ( 'NONE',  ( 8.930623737882818602, -9.703773737882825046, 54.00000000000000711 ) ) ;
#16613=ORIENTED_EDGE ( 'NONE', *, *, #19080, .T. ) ;
#16621=DIRECTION ( 'NONE',  ( -0.000000000000000000, 3.673940397442059868E-16, -1.000000000000000000 ) ) ;
#16626=ORIENTED_EDGE ( 'NONE', *, *, #42574, .F. ) ;
#16628=DIRECTION ( 'NONE',  ( 1.836970198721029934E-16, 1.836970198721010706E-16, -1.000000000000000000 ) ) ;
#16629=EDGE_LOOP ( 'NONE', ( #17173, #44263, #9659, #58119 ) ) ;
#16637=DIRECTION ( 'NONE',  ( 0.000000000000000000, -3.673940397442059868E-16, 1.000000000000000000 ) ) ;
#16651=LINE ( 'NONE', #27590, #14328 ) ;
#16653=FACE_OUTER_BOUND ( 'NONE', #37410, .T. ) ;
#16658=VECTOR ( 'NONE', #10818, 1000.000000000000000 ) ;
#16660=CARTESIAN_POINT ( 'NONE',  ( 6.358413763958955300, 5.779227145995228021, 26.00000000000000711 ) ) ;
#16663=CARTESIAN_POINT ( 'NONE',  ( -5.779227145995285753, 6.344366288193340253, 26.00000000000000711 ) ) ;
#16666=VECTOR ( 'NONE', #38040, 1000.000000000000000 ) ;
#16667=CARTESIAN_POINT ( 'NONE',  ( 7.357023737882817827, -5.552858015815587578, 54.00000000000000711 ) ) ;
#16671=CARTESIAN_POINT ( 'NONE',  ( 4.149127210878726935, -3.677663764522648204, 54.00000000000000711 ) ) ;
#16677=ORIENTED_EDGE ( 'NONE', *, *, #21981, .T. ) ;
#16685=ORIENTED_EDGE ( 'NONE', *, *, #15561, .T. ) ;
#16689=EDGE_CURVE ( 'NONE', #39691, #50336, #19084, .T. ) ;
#16702=LINE ( 'NONE', #38269, #68204 ) ;
#16704=VERTEX_POINT ( 'NONE', #15552 ) ;
#16710=CARTESIAN_POINT ( 'NONE',  ( -8.227189898828745740, 1.620245201994245043, 54.00000000000000711 ) ) ;
#16715=ORIENTED_EDGE ( 'NONE', *, *, #24261, .T. ) ;
#16720=AXIS2_PLACEMENT_3D ( 'NONE', #40385, #61942, #23430 ) ;
#16722=LINE ( 'NONE', #5763, #63901 ) ;
#16723=ORIENTED_EDGE ( 'NONE', *, *, #52385, .T. ) ;
#16727=ORIENTED_EDGE ( 'NONE', *, *, #52894, .T. ) ;
#16735=ORIENTED_EDGE ( 'NONE', *, *, #5079, .F. ) ;
#16738=EDGE_CURVE ( 'NONE', #32965, #49465, #48058, .T. ) ;
#16740=DIRECTION ( 'NONE',  ( -0.6414496315691617934, -0.7671651518152962090, -2.818519042763987834E-16 ) ) ;
#16744=CARTESIAN_POINT ( 'NONE',  ( 8.711985858128644011, 2.406732575409517239, 54.00000000000000711 ) ) ;
#16745=ADVANCED_FACE ( 'NONE', ( #47006 ), #21195, .T. ) ;
#16751=DIRECTION ( 'NONE',  ( 1.836970198721029934E-16, 1.836970198721010706E-16, -1.000000000000000000 ) ) ;
#16772=VERTEX_POINT ( 'NONE', #20829 ) ;
#16781=ORIENTED_EDGE ( 'NONE', *, *, #57492, .T. ) ;
#16795=ADVANCED_FACE ( 'NONE', ( #63631 ), #15190, .F. ) ;
#16804=CARTESIAN_POINT ( 'NONE',  ( 3.857023737882783188, -9.912023737882801555, 26.00000000000000000 ) ) ;
#16811=ORIENTED_EDGE ( 'NONE', *, *, #19955, .F. ) ;
#16823=DIRECTION ( 'NONE',  ( -1.000000000000000000, 0.000000000000000000, 0.000000000000000000 ) ) ;
#16827=CARTESIAN_POINT ( 'NONE',  ( 10.31452373788281562, -3.664523737882826815, 54.00000000000000711 ) ) ;
#16838=CARTESIAN_POINT ( 'NONE',  ( -7.342976262117253405, -3.848229544836288429, 54.00000000000000711 ) ) ;
#16842=DIRECTION ( 'NONE',  ( -1.000000000000000000, 1.828336019306068695E-14, -1.836970198720996407E-16 ) ) ;
#16847=EDGE_CURVE ( 'NONE', #10498, #7825, #16583, .T. ) ;
#16851=ORIENTED_EDGE ( 'NONE', *, *, #53715, .F. ) ;
#16855=EDGE_CURVE ( 'NONE', #68245, #43115, #65941, .T. ) ;
#16862=FACE_OUTER_BOUND ( 'NONE', #66184, .T. ) ;
#16872=EDGE_CURVE ( 'NONE', #67635, #26989, #11256, .T. ) ;
#16878=ADVANCED_FACE ( 'NONE', ( #32832 ), #54412, .F. ) ;
#16879=ORIENTED_EDGE ( 'NONE', *, *, #36628, .F. ) ;
#16883=EDGE_CURVE ( 'NONE', #8452, #62514, #3831, .T. ) ;
#16895=VECTOR ( 'NONE', #56500, 1000.000000000000114 ) ;
#16901=ORIENTED_EDGE ( 'NONE', *, *, #16537, .F. ) ;
#16908=CARTESIAN_POINT ( 'NONE',  ( -3.142976262117262998, -4.046023737882823212, 26.00000000000000711 ) ) ;
#16912=LINE ( 'NONE', #64317, #53786 ) ;
#16916=CARTESIAN_POINT ( 'NONE',  ( -9.722976262117297708, -7.969523737882751924, 26.00000000000000000 ) ) ;
#16918=VECTOR ( 'NONE', #62154, 1000.000000000000000 ) ;
#16922=PLANE ( 'NONE',  #48550 ) ;
#16923=EDGE_LOOP ( 'NONE', ( #35781, #61833, #38844, #47672 ) ) ;
#16924=CARTESIAN_POINT ( 'NONE',  ( -7.342976262117259623, 4.947141984184421304, 54.00000000000000711 ) ) ;
#16928=CARTESIAN_POINT ( 'NONE',  ( -9.897976262117257562, 3.667976262117184749, 54.00000000000000711 ) ) ;
#16937=CARTESIAN_POINT ( 'NONE',  ( -6.651770455163775964, -7.357023737882784964, 26.00000000000000000 ) ) ;
#16939=EDGE_CURVE ( 'NONE', #9220, #47996, #61068, .T. ) ;
#16941=DIRECTION ( 'NONE',  ( -0.000000000000000000, -0.000000000000000000, -1.000000000000000000 ) ) ;
#16949=AXIS2_PLACEMENT_3D ( 'NONE', #50839, #55809, #50507 ) ;
#16950=VERTEX_POINT ( 'NONE', #23255 ) ;
#16954=PLANE ( 'NONE',  #17410 ) ;
#16959=CYLINDRICAL_SURFACE ( 'NONE', #49074, 1.224999999999999423 ) ;
#16965=ORIENTED_EDGE ( 'NONE', *, *, #52848, .T. ) ;
#16969=CARTESIAN_POINT ( 'NONE',  ( 5.793274621760814647, 4.141586236041038482, 54.00000000000000711 ) ) ;
#16973=CARTESIAN_POINT ( 'NONE',  ( -8.130476262117310782, -8.835729544836288696, 26.00000000000000000 ) ) ;
#16982=CARTESIAN_POINT ( 'NONE',  ( 3.848229544836322180, -7.532023737882811432, 54.00000000000000711 ) ) ;
#16995=CARTESIAN_POINT ( 'NONE',  ( -6.817976262117325881, -9.737023737882786634, 54.00000000000000711 ) ) ;
#16999=CARTESIAN_POINT ( 'NONE',  ( -9.880476262117236175, 7.447976262117216528, 54.00000000000000711 ) ) ;
#17007=LINE ( 'NONE', #6398, #29452 ) ;
#17016=ORIENTED_EDGE ( 'NONE', *, *, #39673, .F. ) ;
#17021=AXIS2_PLACEMENT_3D ( 'NONE', #55851, #44890, #18012 ) ;
#17026=EDGE_CURVE ( 'NONE', #10751, #7480, #34548, .T. ) ;
#17030=ORIENTED_EDGE ( 'NONE', *, *, #35927, .F. ) ;
#17034=EDGE_CURVE ( 'NONE', #29317, #64891, #61782, .T. ) ;
#17041=CARTESIAN_POINT ( 'NONE',  ( -6.642976262117260333, 10.30047626211718104, 54.00000000000000711 ) ) ;
#17044=VERTEX_POINT ( 'NONE', #13688 ) ;
#17049=CARTESIAN_POINT ( 'NONE',  ( 10.05377373788281581, 8.916576262117182239, 54.00000000000000711 ) ) ;
#17051=VERTEX_POINT ( 'NONE', #2726 ) ;
#17052=VECTOR ( 'NONE', #64752, 1000.000000000000000 ) ;
#17054=DIRECTION ( 'NONE',  ( -0.000000000000000000, -0.000000000000000000, -1.000000000000000000 ) ) ;
#17070=DIRECTION ( 'NONE',  ( -1.836970198721029934E-16, 1.836970198721036590E-16, -1.000000000000000000 ) ) ;
#17077=DIRECTION ( 'NONE',  ( 0.7671651518153029814, 0.6414496315691537998, 0.000000000000000000 ) ) ;
#17079=DIRECTION ( 'NONE',  ( 0.000000000000000000, 0.000000000000000000, -1.000000000000000000 ) ) ;
#17088=VECTOR ( 'NONE', #66541, 1000.000000000000000 ) ;
#17091=VERTEX_POINT ( 'NONE', #25357 ) ;
#17096=DIRECTION ( 'NONE',  ( 1.000000000000000000, 0.000000000000000000, 0.000000000000000000 ) ) ;
#17099=DIRECTION ( 'NONE',  ( 1.000000000000000000, 0.000000000000000000, 0.000000000000000000 ) ) ;
#17108=FACE_OUTER_BOUND ( 'NONE', #54032, .T. ) ;
#17111=DIRECTION ( 'NONE',  ( 1.115702204244423151E-14, 1.000000000000000000, 1.836970198721016129E-16 ) ) ;
#17116=DIRECTION ( 'NONE',  ( -0.000000000000000000, 3.673940397442059868E-16, -1.000000000000000000 ) ) ;
#17117=EDGE_CURVE ( 'NONE', #51101, #21439, #35960, .T. ) ;
#17119=VERTEX_POINT ( 'NONE', #68845 ) ;
#17121=EDGE_LOOP ( 'NONE', ( #13597, #39695, #34, #15168 ) ) ;
#17123=EDGE_CURVE ( 'NONE', #44788, #14276, #20745, .T. ) ;
#17133=VERTEX_POINT ( 'NONE', #9090 ) ;
#17135=ORIENTED_EDGE ( 'NONE', *, *, #65360, .F. ) ;
#17138=VECTOR ( 'NONE', #15616, 1000.000000000000000 ) ;
#17141=DIRECTION ( 'NONE',  ( -1.000000000000000000, 1.047444401652940007E-14, -1.836970198721010706E-16 ) ) ;
#17149=LINE ( 'NONE', #11486, #68448 ) ;
#17157=AXIS2_PLACEMENT_3D ( 'NONE', #43869, #27960, #38572 ) ;
#17161=EDGE_CURVE ( 'NONE', #14602, #24174, #6155, .T. ) ;
#17165=CARTESIAN_POINT ( 'NONE',  ( 3.664523737882820598, 10.49297626211720491, 54.00000000000000711 ) ) ;
#17170=CARTESIAN_POINT ( 'NONE',  ( -10.30047626211725742, 6.642976262117184838, 26.00000000000000711 ) ) ;
#17173=ORIENTED_EDGE ( 'NONE', *, *, #52298, .T. ) ;
#17174=DIRECTION ( 'NONE',  ( 0.8660254037844435926, 0.4999999999999913958, 2.509347957447859069E-16 ) ) ;
#17181=VECTOR ( 'NONE', #18348, 1000.000000000000000 ) ;
#17183=ORIENTED_EDGE ( 'NONE', *, *, #11300, .F. ) ;
#17187=VERTEX_POINT ( 'NONE', #33446 ) ;
#17196=EDGE_CURVE ( 'NONE', #21626, #22860, #27099, .T. ) ;
#17202=VECTOR ( 'NONE', #57535, 1000.000000000000000 ) ;
#17215=LINE ( 'NONE', #22538, #14182 ) ;
#17230=EDGE_CURVE ( 'NONE', #40228, #28168, #43395, .T. ) ;
#17235=CARTESIAN_POINT ( 'NONE',  ( -3.667976262117228714, 9.722976262117169810, 26.00000000000000711 ) ) ;
#17244=FACE_OUTER_BOUND ( 'NONE', #39970, .T. ) ;
#17251=CYLINDRICAL_SURFACE ( 'NONE', #39724, 0.5250000000000011324 ) ;
#17255=ADVANCED_FACE ( 'NONE', ( #64246 ), #5537, .F. ) ;
#17257=FACE_OUTER_BOUND ( 'NONE', #30713, .T. ) ;
#17259=EDGE_CURVE ( 'NONE', #523, #69426, #48325, .T. ) ;
#17261=DIRECTION ( 'NONE',  ( -1.000000000000000000, 0.000000000000000000, 0.000000000000000000 ) ) ;
#17264=LINE ( 'NONE', #5972, #31664 ) ;
#17268=ORIENTED_EDGE ( 'NONE', *, *, #23613, .F. ) ;
#17269=DIRECTION ( 'NONE',  ( 0.7671651518153006499, -0.6414496315691565753, 0.000000000000000000 ) ) ;
#17271=CARTESIAN_POINT ( 'NONE',  ( 6.665817930929297752, -7.532023737882823866, 54.00000000000000711 ) ) ;
#17272=VECTOR ( 'NONE', #14322, 999.9999999999998863 ) ;
#17275=ORIENTED_EDGE ( 'NONE', *, *, #46390, .T. ) ;
#17285=PLANE ( 'NONE',  #44504 ) ;
#17288=PLANE ( 'NONE',  #1658 ) ;
#17289=DIRECTION ( 'NONE',  ( -1.000000000000000000, -0.000000000000000000, -0.000000000000000000 ) ) ;
#17292=ORIENTED_EDGE ( 'NONE', *, *, #61110, .F. ) ;
#17304=EDGE_LOOP ( 'NONE', ( #23643, #45948, #25243, #12907 ) ) ;
#17314=CARTESIAN_POINT ( 'NONE',  ( 10.50702373788280219, 6.835476262117187396, 26.00000000000000711 ) ) ;
#17326=ADVANCED_FACE ( 'NONE', ( #28814 ), #61336, .F. ) ;
#17328=VERTEX_POINT ( 'NONE', #23871 ) ;
#17346=AXIS2_PLACEMENT_3D ( 'NONE', #9266, #58422, #9977 ) ;
#17352=CARTESIAN_POINT ( 'NONE',  ( 8.930623737882839919, 8.566576262117191476, 26.00000000000000711 ) ) ;
#17354=CIRCLE ( 'NONE', #11750, 0.5249999999999994671 ) ;
#17356=LINE ( 'NONE', #38930, #5007 ) ;
#17367=FACE_OUTER_BOUND ( 'NONE', #20138, .T. ) ;
#17373=DIRECTION ( 'NONE',  ( 1.836970198721029934E-16, -1.836970198721036344E-16, 1.000000000000000000 ) ) ;
#17378=ORIENTED_EDGE ( 'NONE', *, *, #69396, .F. ) ;
#17381=DIRECTION ( 'NONE',  ( -3.304235192336781428E-15, -1.000000000000000000, 0.000000000000000000 ) ) ;
#17388=VECTOR ( 'NONE', #36400, 1000.000000000000000 ) ;
#17391=LINE ( 'NONE', #6105, #324 ) ;
#17399=VERTEX_POINT ( 'NONE', #39091 ) ;
#17401=CARTESIAN_POINT ( 'NONE',  ( -2.617976262117293285, -6.501044194225502615, 54.00000000000000711 ) ) ;
#17402=CARTESIAN_POINT ( 'NONE',  ( -7.342976262117259623, 5.538810540049946773, 54.00000000000000711 ) ) ;
#17410=AXIS2_PLACEMENT_3D ( 'NONE', #21231, #64354, #64022 ) ;
#17415=DIRECTION ( 'NONE',  ( 1.356437060717834182E-15, 1.000000000000000000, 1.836970198721034125E-16 ) ) ;
#17416=ORIENTED_EDGE ( 'NONE', *, *, #5216, .T. ) ;
#17417=CYLINDRICAL_SURFACE ( 'NONE', #7246, 0.5249999999999994671 ) ;
#17424=DIRECTION ( 'NONE',  ( 3.491481338843133355E-15, 1.000000000000000000, 1.836970198721029934E-16 ) ) ;
#17427=DIRECTION ( 'NONE',  ( -0.000000000000000000, -0.000000000000000000, -1.000000000000000000 ) ) ;
#17435=ORIENTED_EDGE ( 'NONE', *, *, #65569, .T. ) ;
#17439=FACE_OUTER_BOUND ( 'NONE', #64683, .T. ) ;
#17442=DIRECTION ( 'NONE',  ( -0.000000000000000000, -0.000000000000000000, 1.000000000000000000 ) ) ;
#17449=PLANE ( 'NONE',  #13137 ) ;
#17451=ORIENTED_EDGE ( 'NONE', *, *, #40277, .T. ) ;
#17453=EDGE_CURVE ( 'NONE', #56866, #18784, #25986, .T. ) ;
#17459=ORIENTED_EDGE ( 'NONE', *, *, #2570, .F. ) ;
#17460=ADVANCED_FACE ( 'NONE', ( #42229 ), #41177, .F. ) ;
#17464=LINE ( 'NONE', #33726, #46727 ) ;
#17467=VECTOR ( 'NONE', #5528, 1000.000000000000000 ) ;
#17476=ORIENTED_EDGE ( 'NONE', *, *, #14208, .T. ) ;
#17495=CARTESIAN_POINT ( 'NONE',  ( 7.357023737882817827, -4.961189459950063885, 54.00000000000000711 ) ) ;
#17503=AXIS2_PLACEMENT_3D ( 'NONE', #16432, #9737, #42604 ) ;
#17505=CARTESIAN_POINT ( 'NONE',  ( -8.697938382363185283, -8.093267424590415260, 54.00000000000000711 ) ) ;
#17510=CARTESIAN_POINT ( 'NONE',  ( -4.141586236041100655, 4.706725378239165813, 54.00000000000000711 ) ) ;
#17511=CARTESIAN_POINT ( 'NONE',  ( -8.821682069070780230, 2.530476262117183683, 54.00000000000000711 ) ) ;
#17513=CARTESIAN_POINT ( 'NONE',  ( -10.30047626211725742, 6.835476262117182955, 26.00000000000000711 ) ) ;
#17514=AXIS2_PLACEMENT_3D ( 'NONE', #10478, #64237, #64576 ) ;
#17515=ORIENTED_EDGE ( 'NONE', *, *, #22951, .T. ) ;
#17527=ORIENTED_EDGE ( 'NONE', *, *, #42, .F. ) ;
#17534=EDGE_CURVE ( 'NONE', #56499, #34373, #9721, .T. ) ;
#17540=LINE ( 'NONE', #32442, #63663 ) ;
#17541=FACE_OUTER_BOUND ( 'NONE', #54040, .T. ) ;
#17544=VECTOR ( 'NONE', #1341, 1000.000000000000000 ) ;
#17551=VECTOR ( 'NONE', #69750, 1000.000000000000000 ) ;
#17556=VECTOR ( 'NONE', #12589, 1000.000000000000000 ) ;
#17560=CARTESIAN_POINT ( 'NONE',  ( -6.350872789121373430, -6.836383711242974393, 26.00000000000000711 ) ) ;
#17561=ORIENTED_EDGE ( 'NONE', *, *, #52383, .T. ) ;
#17565=CIRCLE ( 'NONE', #69518, 0.1749999999999998224 ) ;
#17566=ORIENTED_EDGE ( 'NONE', *, *, #2429, .T. ) ;
#17576=ORIENTED_EDGE ( 'NONE', *, *, #11354, .T. ) ;
#17580=AXIS2_PLACEMENT_3D ( 'NONE', #44738, #61347, #39105 ) ;
#17607=VECTOR ( 'NONE', #37679, 999.9999999999998863 ) ;
#17613=VECTOR ( 'NONE', #28383, 1000.000000000000000 ) ;
#17614=EDGE_LOOP ( 'NONE', ( #22362, #52332, #36894, #5355 ) ) ;
#17615=LINE ( 'NONE', #43449, #27745 ) ;
#17619=CARTESIAN_POINT ( 'NONE',  ( -7.342976262117282715, -5.552858015815545834, 54.00000000000000711 ) ) ;
#17627=ORIENTED_EDGE ( 'NONE', *, *, #49625, .F. ) ;
#17630=CARTESIAN_POINT ( 'NONE',  ( -9.689726262117227762, 8.566576262117216345, 54.00000000000000711 ) ) ;
#17634=DIRECTION ( 'NONE',  ( 1.000000000000000000, -9.050731179009442381E-15, 0.000000000000000000 ) ) ;
#17635=DIRECTION ( 'NONE',  ( -1.836970198721029934E-16, 1.836970198721036590E-16, -1.000000000000000000 ) ) ;
#17643=EDGE_CURVE ( 'NONE', #268, #23882, #18637, .T. ) ;
#17648=DIRECTION ( 'NONE',  ( -0.7071067811865486830, -0.7071067811865464625, 0.000000000000000000 ) ) ;
#17651=ORIENTED_EDGE ( 'NONE', *, *, #62506, .F. ) ;
#17655=CIRCLE ( 'NONE', #16512, 0.1749999999999998224 ) ;
#17657=LINE ( 'NONE', #55493, #21047 ) ;
#17660=EDGE_CURVE ( 'NONE', #56266, #37419, #31641, .T. ) ;
#17676=DIRECTION ( 'NONE',  ( 0.000000000000000000, 1.000000000000000000, 0.000000000000000000 ) ) ;
#17679=CARTESIAN_POINT ( 'NONE',  ( -0.9414762621173187185, -9.404523737882845680, 26.00000000000000711 ) ) ;
#17681=EDGE_LOOP ( 'NONE', ( #20775, #59882, #24668, #2456 ) ) ;
#17696=ORIENTED_EDGE ( 'NONE', *, *, #16239, .T. ) ;
#17698=DIRECTION ( 'NONE',  ( -1.000000000000000000, 0.000000000000000000, 0.000000000000000000 ) ) ;
#17704=AXIS2_PLACEMENT_3D ( 'NONE', #364, #16637, #26540 ) ;
#17705=CARTESIAN_POINT ( 'NONE',  ( -5.242976262117259978, 7.172176262117182510, 54.00000000000000711 ) ) ;
#17711=CIRCLE ( 'NONE', #41433, 0.1749999999999998224 ) ;
#17717=EDGE_LOOP ( 'NONE', ( #12576, #62345, #56512, #8730 ) ) ;
#17723=DIRECTION ( 'NONE',  ( 0.000000000000000000, 1.000000000000000000, 0.000000000000000000 ) ) ;
#17725=CARTESIAN_POINT ( 'NONE',  ( 5.257023737882801306, 6.467976262117199227, 54.00000000000000711 ) ) ;
#17730=ORIENTED_EDGE ( 'NONE', *, *, #41863, .F. ) ;
#17732=CYLINDRICAL_SURFACE ( 'NONE', #26244, 1.224999999999999423 ) ;
#17737=DIRECTION ( 'NONE',  ( 0.7071067811865474617, -0.7071067811865474617, -2.597868168706479611E-16 ) ) ;
#17746=EDGE_CURVE ( 'NONE', #22764, #36489, #60576, .T. ) ;
#17756=CARTESIAN_POINT ( 'NONE',  ( -3.663616288757090445, -4.149127210878730487, 54.00000000000000711 ) ) ;
#17760=VECTOR ( 'NONE', #27428, 1000.000000000000000 ) ;
#17761=LINE ( 'NONE', #13071, #40196 ) ;
#17766=CARTESIAN_POINT ( 'NONE',  ( -10.30047626211725742, 3.650476262117184234, 54.00000000000000711 ) ) ;
#17767=ADVANCED_FACE ( 'NONE', ( #23448 ), #60915, .F. ) ;
#17782=LINE ( 'NONE', #858, #21005 ) ;
#17783=FACE_OUTER_BOUND ( 'NONE', #14482, .T. ) ;
#17787=ORIENTED_EDGE ( 'NONE', *, *, #20059, .T. ) ;
#17790=ORIENTED_EDGE ( 'NONE', *, *, #28756, .F. ) ;
#17805=LINE ( 'NONE', #1206, #52696 ) ;
#17806=DIRECTION ( 'NONE',  ( 0.000000000000000000, -3.673940397442059868E-16, 1.000000000000000000 ) ) ;
#17807=ORIENTED_EDGE ( 'NONE', *, *, #28893, .F. ) ;
#17810=AXIS2_PLACEMENT_3D ( 'NONE', #39457, #27825, #59988 ) ;
#17826=VERTEX_POINT ( 'NONE', #52420 ) ;
#17832=ORIENTED_EDGE ( 'NONE', *, *, #47042, .F. ) ;
#17833=VERTEX_POINT ( 'NONE', #25192 ) ;
#17847=FACE_BOUND ( 'NONE', #64816, .T. ) ;
#17850=LINE ( 'NONE', #29498, #62516 ) ;
#17870=CYLINDRICAL_SURFACE ( 'NONE', #8671, 0.3499999999999996447 ) ;
#17872=ORIENTED_EDGE ( 'NONE', *, *, #15275, .T. ) ;
#17877=DIRECTION ( 'NONE',  ( 1.901462112903059913E-14, 1.000000000000000000, 1.836970198721045958E-16 ) ) ;
#17895=CARTESIAN_POINT ( 'NONE',  ( -4.141586236041125524, -5.793274621760837739, 26.00000000000000711 ) ) ;
#17913=LINE ( 'NONE', #24631, #23604 ) ;
#17914=DIRECTION ( 'NONE',  ( -0.7071067811865486830, -0.7071067811865464625, -2.597868168706476160E-16 ) ) ;
#17922=LINE ( 'NONE', #49435, #37719 ) ;
#17924=CARTESIAN_POINT ( 'NONE',  ( 8.930623737882818602, -10.05377373788282469, 54.00000000000000711 ) ) ;
#17930=ORIENTED_EDGE ( 'NONE', *, *, #58569, .F. ) ;
#17934=AXIS2_PLACEMENT_3D ( 'NONE', #53837, #87, #63741 ) ;
#17935=CARTESIAN_POINT ( 'NONE',  ( 9.929523737882751888, 0.9414762621171479662, 54.00000000000000711 ) ) ;
#17942=FACE_OUTER_BOUND ( 'NONE', #26878, .T. ) ;
#17943=VERTEX_POINT ( 'NONE', #24842 ) ;
#17951=ORIENTED_EDGE ( 'NONE', *, *, #42870, .F. ) ;
#17953=CIRCLE ( 'NONE', #57487, 0.7112000000000124889 ) ;
#17964=ORIENTED_EDGE ( 'NONE', *, *, #61710, .F. ) ;
#17975=FACE_OUTER_BOUND ( 'NONE', #2196, .T. ) ;
#17979=VERTEX_POINT ( 'NONE', #1030 ) ;
#17983=EDGE_CURVE ( 'NONE', #34294, #42050, #55115, .T. ) ;
#17988=ORIENTED_EDGE ( 'NONE', *, *, #63786, .T. ) ;
#17989=DIRECTION ( 'NONE',  ( -1.836970198721029934E-16, 1.836970198721036590E-16, -1.000000000000000000 ) ) ;
#17993=DIRECTION ( 'NONE',  ( 0.000000000000000000, 1.000000000000000000, 0.000000000000000000 ) ) ;
#17994=CARTESIAN_POINT ( 'NONE',  ( -10.49297626211726175, 3.650476262117184234, 26.00000000000000711 ) ) ;
#18007=ORIENTED_EDGE ( 'NONE', *, *, #10475, .T. ) ;
#18012=DIRECTION ( 'NONE',  ( -0.7071067811865446862, -0.7071067811865503483, 0.000000000000000000 ) ) ;
#18014=ORIENTED_EDGE ( 'NONE', *, *, #11518, .F. ) ;
#18015=CARTESIAN_POINT ( 'NONE',  ( 0.9555237378827827754, -9.929523737882782086, 26.00000000000000000 ) ) ;
#18017=DIRECTION ( 'NONE',  ( -1.836970198721029934E-16, 1.836970198721036344E-16, -1.000000000000000000 ) ) ;
#18018=CARTESIAN_POINT ( 'NONE',  ( -9.722976262117237312, 7.605476262117214503, 25.99999580000000421 ) ) ;
#18019=ORIENTED_EDGE ( 'NONE', *, *, #16883, .T. ) ;
#18021=AXIS2_PLACEMENT_3D ( 'NONE', #21241, #4288, #47399 ) ;
#18024=EDGE_LOOP ( 'NONE', ( #35344, #43830, #19210, #19702 ) ) ;
#18030=FACE_BOUND ( 'NONE', #20599, .T. ) ;
#18034=VECTOR ( 'NONE', #7355, 1000.000000000000000 ) ;
#18038=DIRECTION ( 'NONE',  ( -0.6414496315691617934, -0.7671651518152962090, 0.000000000000000000 ) ) ;
#18039=ORIENTED_EDGE ( 'NONE', *, *, #20460, .T. ) ;
#18044=EDGE_CURVE ( 'NONE', #26989, #46007, #17615, .T. ) ;
#18053=VECTOR ( 'NONE', #7856, 1000.000000000000000 ) ;
#18056=ADVANCED_FACE ( 'NONE', ( #65036 ), #6996, .T. ) ;
#18066=ORIENTED_EDGE ( 'NONE', *, *, #32679, .F. ) ;
#18067=VERTEX_POINT ( 'NONE', #16597 ) ;
#18070=EDGE_CURVE ( 'NONE', #8587, #34946, #63732, .T. ) ;
#18100=DIRECTION ( 'NONE',  ( 0.7071067811865527908, 0.7071067811865422437, 2.597868168706460875E-16 ) ) ;
#18104=CARTESIAN_POINT ( 'NONE',  ( -7.394232575409651176, -6.789561617636906909, 54.00000000000000711 ) ) ;
#18105=CARTESIAN_POINT ( 'NONE',  ( 5.793274621760843957, -6.358413763958971288, 26.00000000000000711 ) ) ;
#18108=CARTESIAN_POINT ( 'NONE',  ( -1.620245201994301665, 8.227189898828640935, 26.00000000000000711 ) ) ;
#18123=EDGE_CURVE ( 'NONE', #16599, #5747, #69024, .T. ) ;
#18131=EDGE_CURVE ( 'NONE', #52921, #51395, #23188, .T. ) ;
#18135=AXIS2_PLACEMENT_3D ( 'NONE', #36015, #30719, #57584 ) ;
#18142=CARTESIAN_POINT ( 'NONE',  ( -7.517976262117252340, -3.848229544836285321, 54.00000000000000711 ) ) ;
#18147=ORIENTED_EDGE ( 'NONE', *, *, #37622, .T. ) ;
#18156=CARTESIAN_POINT ( 'NONE',  ( -10.49297626211726175, 3.650476262117184234, 54.00000000000000711 ) ) ;
#18167=ORIENTED_EDGE ( 'NONE', *, *, #38239, .T. ) ;
#18180=CARTESIAN_POINT ( 'NONE',  ( 6.832023737882818359, -9.737023737882822161, 54.00000000000000711 ) ) ;
#18182=ORIENTED_EDGE ( 'NONE', *, *, #28102, .T. ) ;
#18183=DIRECTION ( 'NONE',  ( 0.000000000000000000, 0.000000000000000000, 1.000000000000000000 ) ) ;
#18185=FACE_OUTER_BOUND ( 'NONE', #20713, .T. ) ;
#18192=CARTESIAN_POINT ( 'NONE',  ( 3.664523737882815269, 10.49297626211721024, 26.00000000000000711 ) ) ;
#18193=CARTESIAN_POINT ( 'NONE',  ( -1.466476262117323737, -9.404523737882843903, 54.00000000000000711 ) ) ;
#18196=VECTOR ( 'NONE', #52423, 1000.000000000000000 ) ;
#18200=EDGE_CURVE ( 'NONE', #44308, #46469, #58234, .T. ) ;
#18203=CIRCLE ( 'NONE', #62268, 0.1749999999999980738 ) ;
#18208=CARTESIAN_POINT ( 'NONE',  ( -9.722976262117237312, 7.605476262117214503, 54.00000000000000711 ) ) ;
#18215=CARTESIAN_POINT ( 'NONE',  ( 10.05377373788278739, -9.703773737882814387, 26.00000000000000000 ) ) ;
#18222=VECTOR ( 'NONE', #35558, 1000.000000000000000 ) ;
#18226=ORIENTED_EDGE ( 'NONE', *, *, #15273, .F. ) ;
#18238=VERTEX_POINT ( 'NONE', #45519 ) ;
#18239=ADVANCED_FACE ( 'NONE', ( #7692 ), #40220, .T. ) ;
#18245=DIRECTION ( 'NONE',  ( -1.836970198721029934E-16, 1.836970198721036344E-16, -1.000000000000000000 ) ) ;
#18248=AXIS2_PLACEMENT_3D ( 'NONE', #36785, #68952, #62577 ) ;
#18252=EDGE_LOOP ( 'NONE', ( #53568, #14598, #48057, #20186, #10744, #17451, #4841, #56162, #57143, #68753, #62856, #7677, #63232, #59747, #28418, #35267, #48318, #37851, #9329, #18019, #28408, #4417, #17275, #3150, #24318, #26842, #18957, #59843, #22990, #69686, #35914, #30062, #28261, #34606, #5710, #64415, #10242, #19823, #34572, #43655, #29178, #52703, #30331, #22266, #63764, #66623, #32384, #18771, #43057, #16434, #67558, #14247, #53743, #40351, #56073, #27492, #16727, #54536, #62964, #20255, #24815, #68067, #44303, #14600, #68731, #7797, #21933, #39789, #26584, #37171, #45244, #29857, #24094, #7459, #64251, #5692, #13342, #1495, #3217, #66428, #23839, #36436, #18865, #26208, #16781, #61460, #55782, #3326, #49463, #5032, #66454, #54791, #58683, #61453, #22210, #34157, #1834, #69403, #2687, #19287, #63275, #54130, #34682, #41353, #57978, #40963, #25400, #37824, #34002, #8199, #67649, #4187, #14572, #67000, #23280, #8108, #62336, #58856, #30554, #12829, #46566, #15768, #30294, #16448, #41500, #20780, #47451, #10151, #5365, #7225, #69744, #20006, #5979, #56575, #56293, #54, #1226, #40941, #41741, #776, #14505, #11234, #12866, #50101, #51723, #25073, #25296, #18510, #61174, #39778, #53822, #3636, #617, #37099, #13762, #33512, #37348, #24500, #21810, #60140, #56835, #10439, #47922, #37671, #266, #900, #42719, #65909, #53227, #531, #4459, #39016, #61364, #31620, #27133, #36619, #50697, #25591, #20354, #20730, #27709, #67972, #20608, #59313, #60213, #40260, #24390, #39446, #56672, #360, #751, #57752, #60428, #63042, #30569, #59287, #42335, #28985, #54375, #53023, #38325, #26751, #61534, #4951, #64012, #23977, #47041, #64464, #63150, #44094, #10933, #25145, #43740, #49804 ) ) ;
#18256=DIRECTION ( 'NONE',  ( -0.000000000000000000, 3.673940397442059868E-16, -1.000000000000000000 ) ) ;
#18261=FACE_OUTER_BOUND ( 'NONE', #38018, .T. ) ;
#18265=DIRECTION ( 'NONE',  ( 0.7071067811865474617, -0.7071067811865474617, 0.000000000000000000 ) ) ;
#18266=PLANE ( 'NONE',  #49429 ) ;
#18268=EDGE_CURVE ( 'NONE', #52552, #52916, #24670, .T. ) ;
#18269=DIRECTION ( 'NONE',  ( 1.836970198721029934E-16, -1.836970198721036344E-16, 1.000000000000000000 ) ) ;
#18270=EDGE_CURVE ( 'NONE', #11023, #49648, #7379, .T. ) ;
#18273=EDGE_CURVE ( 'NONE', #29536, #39983, #64256, .T. ) ;
#18276=CARTESIAN_POINT ( 'NONE',  ( 7.357023737882806280, 6.651770455163672935, 54.00000000000000711 ) ) ;
#18282=LINE ( 'NONE', #50811, #69125 ) ;
#18288=VECTOR ( 'NONE', #10428, 1000.000000000000000 ) ;
#18316=FACE_OUTER_BOUND ( 'NONE', #52121, .T. ) ;
#18317=DIRECTION ( 'NONE',  ( 1.000000000000000000, 0.000000000000000000, 0.000000000000000000 ) ) ;
#18319=CARTESIAN_POINT ( 'NONE',  ( 10.05377373788281581, 9.689726262117151379, 54.00000000000000711 ) ) ;
#18325=CARTESIAN_POINT ( 'NONE',  ( 8.835729544836338434, -2.369523737882826886, 54.00000000000000711 ) ) ;
#18331=ORIENTED_EDGE ( 'NONE', *, *, #54716, .T. ) ;
#18332=VECTOR ( 'NONE', #40500, 1000.000000000000000 ) ;
#18333=DIRECTION ( 'NONE',  ( -1.836970198721029934E-16, 1.836970198721036590E-16, -1.000000000000000000 ) ) ;
#18334=DIRECTION ( 'NONE',  ( -1.000000000000000000, 1.047444401652940007E-14, -1.836970198721010706E-16 ) ) ;
#18336=DIRECTION ( 'NONE',  ( 9.912705577010336396E-15, 1.000000000000000000, 0.000000000000000000 ) ) ;
#18342=DIRECTION ( 'NONE',  ( 1.214636490590110272E-14, 1.000000000000000000, 1.836970198721032892E-16 ) ) ;
#18347=DIRECTION ( 'NONE',  ( 1.130039751537442024E-14, 1.000000000000000000, 1.836970198721015636E-16 ) ) ;
#18348=DIRECTION ( 'NONE',  ( -1.000000000000000000, 3.491481338843133355E-15, 1.836970198721036344E-16 ) ) ;
#18349=PLANE ( 'NONE',  #6480 ) ;
#18350=FACE_OUTER_BOUND ( 'NONE', #34452, .T. ) ;
#18355=CARTESIAN_POINT ( 'NONE',  ( 1.480523737882811552, 9.390476262117216422, 26.00000000000000711 ) ) ;
#18358=DIRECTION ( 'NONE',  ( -0.7071067811865530128, -0.7071067811865421326, 0.000000000000000000 ) ) ;
#18359=ORIENTED_EDGE ( 'NONE', *, *, #69112, .F. ) ;
#18376=VECTOR ( 'NONE', #63164, 1000.000000000000000 ) ;
#18378=ADVANCED_FACE ( 'NONE', ( #41271 ), #25023, .F. ) ;
#18379=CARTESIAN_POINT ( 'NONE',  ( -9.547976262117222390, -2.369523737882729186, 54.00000000000000711 ) ) ;
#18386=LINE ( 'NONE', #45611, #28394 ) ;
#18392=DIRECTION ( 'NONE',  ( -0.000000000000000000, 3.673940397442059868E-16, -1.000000000000000000 ) ) ;
#18394=CARTESIAN_POINT ( 'NONE',  ( 9.737023737882775976, 3.667976262117157660, 26.00000000000000711 ) ) ;
#18396=CIRCLE ( 'NONE', #57940, 0.1750000000000002387 ) ;
#18397=CARTESIAN_POINT ( 'NONE',  ( -7.172176262117259782, 5.242976262117182706, 54.00000000000000711 ) ) ;
#18398=DIRECTION ( 'NONE',  ( 1.836970198721029934E-16, -1.836970198721036344E-16, 1.000000000000000000 ) ) ;
#18408=CIRCLE ( 'NONE', #27467, 0.5249999999999990230 ) ;
#18411=EDGE_LOOP ( 'NONE', ( #14305, #64112, #66896, #31247 ) ) ;
#18417=ORIENTED_EDGE ( 'NONE', *, *, #25892, .F. ) ;
#18418=ORIENTED_EDGE ( 'NONE', *, *, #48827, .F. ) ;
#18421=CIRCLE ( 'NONE', #45476, 0.1749999999999998224 ) ;
#18431=LINE ( 'NONE', #39995, #23299 ) ;
#18433=CARTESIAN_POINT ( 'NONE',  ( 8.711985858128638682, 2.406732575409522568, 26.00000000000000711 ) ) ;
#18434=EDGE_CURVE ( 'NONE', #36010, #31923, #21118, .T. ) ;
#18447=FACE_OUTER_BOUND ( 'NONE', #39869, .T. ) ;
#18453=EDGE_CURVE ( 'NONE', #41857, #45178, #5208, .T. ) ;
#18458=VECTOR ( 'NONE', #61551, 1000.000000000000000 ) ;
#18459=EDGE_CURVE ( 'NONE', #59802, #40034, #13083, .T. ) ;
#18461=EDGE_CURVE ( 'NONE', #1371, #61947, #33104, .T. ) ;
#18472=DIRECTION ( 'NONE',  ( -1.000000000000000000, 3.016910393003147986E-15, 1.108394896831706469E-30 ) ) ;
#18477=VERTEX_POINT ( 'NONE', #11186 ) ;
#18481=CARTESIAN_POINT ( 'NONE',  ( 8.241237374594247100, 1.620245201994230611, 54.00000000000000711 ) ) ;
#18485=DIRECTION ( 'NONE',  ( 1.000000000000000000, 0.000000000000000000, 0.000000000000000000 ) ) ;
#18510=ORIENTED_EDGE ( 'NONE', *, *, #62600, .T. ) ;
#18516=ORIENTED_EDGE ( 'NONE', *, *, #60432, .T. ) ;
#18521=FACE_OUTER_BOUND ( 'NONE', #66688, .T. ) ;
#18524=EDGE_CURVE ( 'NONE', #64510, #35812, #5895, .T. ) ;
#18527=DIRECTION ( 'NONE',  ( -6.508391731846281342E-15, -1.000000000000000000, -1.836970198721024757E-16 ) ) ;
#18528=ADVANCED_FACE ( 'NONE', ( #10845 ), #32429, .F. ) ;
#18531=CARTESIAN_POINT ( 'NONE',  ( -3.834182069070763976, 7.517976262117170627, 54.00000000000000711 ) ) ;
#18536=CARTESIAN_POINT ( 'NONE',  ( -8.079219948824906794, 8.697938382363059162, 26.00000000000000711 ) ) ;
#18538=VERTEX_POINT ( 'NONE', #12220 ) ;
#18539=VECTOR ( 'NONE', #10063, 1000.000000000000000 ) ;
#18547=ADVANCED_FACE ( 'NONE', ( #1611 ), #51457, .F. ) ;
#18554=DIRECTION ( 'NONE',  ( 0.000000000000000000, 0.000000000000000000, 1.000000000000000000 ) ) ;
#18560=ORIENTED_EDGE ( 'NONE', *, *, #56249, .T. ) ;
#18563=ADVANCED_FACE ( 'NONE', ( #67014 ), #8310, .F. ) ;
#18566=CARTESIAN_POINT ( 'NONE',  ( -10.03972626211722918, 9.689726262117183353, 54.00000000000000711 ) ) ;
#18576=ORIENTED_EDGE ( 'NONE', *, *, #25510, .F. ) ;
#18585=ORIENTED_EDGE ( 'NONE', *, *, #50681, .T. ) ;
#18592=VECTOR ( 'NONE', #46914, 1000.000000000000000 ) ;
#18599=FACE_OUTER_BOUND ( 'NONE', #38435, .T. ) ;
#18604=VERTEX_POINT ( 'NONE', #66669 ) ;
#18605=CIRCLE ( 'NONE', #14071, 0.5249999999999990230 ) ;
#18619=FACE_OUTER_BOUND ( 'NONE', #16424, .T. ) ;
#18620=CARTESIAN_POINT ( 'NONE',  ( 6.849523737882814878, 10.49297626211720136, 26.00000000000000711 ) ) ;
#18623=FACE_OUTER_BOUND ( 'NONE', #37606, .T. ) ;
#18625=DIRECTION ( 'NONE',  ( 0.000000000000000000, 1.000000000000000000, 3.673940397442059868E-16 ) ) ;
#18629=EDGE_CURVE ( 'NONE', #47019, #61785, #40490, .T. ) ;
#18634=ORIENTED_EDGE ( 'NONE', *, *, #12999, .F. ) ;
#18637=CIRCLE ( 'NONE', #23136, 0.1749999999999989342 ) ;
#18638=ORIENTED_EDGE ( 'NONE', *, *, #68346, .F. ) ;
#18647=VECTOR ( 'NONE', #30739, 1000.000000000000000 ) ;
#18659=ORIENTED_EDGE ( 'NONE', *, *, #54480, .T. ) ;
#18663=VERTEX_POINT ( 'NONE', #51104 ) ;
#18665=DIRECTION ( 'NONE',  ( 0.000000000000000000, 0.000000000000000000, 1.000000000000000000 ) ) ;
#18668=LINE ( 'NONE', #60763, #61456 ) ;
#18679=VERTEX_POINT ( 'NONE', #35900 ) ;
#18691=CARTESIAN_POINT ( 'NONE',  ( -8.821682069070780230, 2.530476262117183683, 54.00000000000000711 ) ) ;
#18693=VECTOR ( 'NONE', #11271, 1000.000000000000000 ) ;
#18698=CARTESIAN_POINT ( 'NONE',  ( -3.663616288757055806, 4.135079735113128763, 54.00000000000000711 ) ) ;
#18709=VECTOR ( 'NONE', #14296, 1000.000000000000000 ) ;
#18710=AXIS2_PLACEMENT_3D ( 'NONE', #31399, #14767, #46935 ) ;
#18714=DIRECTION ( 'NONE',  ( -1.000000000000000000, 7.808916176531286882E-15, 0.000000000000000000 ) ) ;
#18729=ORIENTED_EDGE ( 'NONE', *, *, #374, .T. ) ;
#18742=VERTEX_POINT ( 'NONE', #47896 ) ;
#18745=CARTESIAN_POINT ( 'NONE',  ( 7.186223737882818874, -5.257023737882815517, 26.00000000000000711 ) ) ;
#18765=CIRCLE ( 'NONE', #60559, 0.1749999999999989342 ) ;
#18769=EDGE_LOOP ( 'NONE', ( #14749, #24628, #69929, #4783 ) ) ;
#18771=ORIENTED_EDGE ( 'NONE', *, *, #16847, .T. ) ;
#18773=ORIENTED_EDGE ( 'NONE', *, *, #67881, .T. ) ;
#18775=ADVANCED_FACE ( 'NONE', ( #3722 ), #53230, .F. ) ;
#18784=VERTEX_POINT ( 'NONE', #31317 ) ;
#18786=LINE ( 'NONE', #57318, #16118 ) ;
#18789=CARTESIAN_POINT ( 'NONE',  ( 9.404523737882817258, -1.480523737882815549, 26.00000000000000711 ) ) ;
#18790=LINE ( 'NONE', #35390, #37345 ) ;
#18792=LINE ( 'NONE', #20544, #47583 ) ;
#18799=CARTESIAN_POINT ( 'NONE',  ( -5.242976262117259978, 5.242976262117182706, 26.00000000000000711 ) ) ;
#18800=DIRECTION ( 'NONE',  ( 0.6414496315691575745, 0.7671651518152998728, 2.587583378555112027E-16 ) ) ;
#18806=CARTESIAN_POINT ( 'NONE',  ( -5.242976262117259978, 5.242976262117182706, 26.00000000000000711 ) ) ;
#18815=CIRCLE ( 'NONE', #21099, 1.224999999999999423 ) ;
#18820=EDGE_CURVE ( 'NONE', #42686, #31923, #26000, .T. ) ;
#18827=ORIENTED_EDGE ( 'NONE', *, *, #55895, .F. ) ;
#18830=VERTEX_POINT ( 'NONE', #32342 ) ;
#18831=LINE ( 'NONE', #40399, #59560 ) ;
#18842=VERTEX_POINT ( 'NONE', #49307 ) ;
#18852=ORIENTED_EDGE ( 'NONE', *, *, #37991, .F. ) ;
#18853=ORIENTED_EDGE ( 'NONE', *, *, #31995, .F. ) ;
#18865=ORIENTED_EDGE ( 'NONE', *, *, #36967, .T. ) ;
#18871=AXIS2_PLACEMENT_3D ( 'NONE', #19369, #7707, #56844 ) ;
#18875=CARTESIAN_POINT ( 'NONE',  ( 3.157023737882797665, 4.031976262117209053, 54.00000000000000711 ) ) ;
#18883=ORIENTED_EDGE ( 'NONE', *, *, #7106, .F. ) ;
#18891=EDGE_LOOP ( 'NONE', ( #42436, #49175, #33244, #41658 ) ) ;
#18892=ORIENTED_EDGE ( 'NONE', *, *, #43939, .T. ) ;
#18893=CARTESIAN_POINT ( 'NONE',  ( 7.357023737882784964, 3.834182069070697807, 54.00000000000000711 ) ) ;
#18905=DIRECTION ( 'NONE',  ( -1.000000000000000000, 1.280238727658158432E-15, 0.000000000000000000 ) ) ;
#18906=ORIENTED_EDGE ( 'NONE', *, *, #50945, .T. ) ;
#18914=PRODUCT_DEFINITION_FORMATION_WITH_SPECIFIED_SOURCE ( 'ANY', '', #6975, .NOT_KNOWN. ) ;
#18916=DIRECTION ( 'NONE',  ( -0.4999999999999695244, 0.8660254037844562491, 0.000000000000000000 ) ) ;
#18919=CIRCLE ( 'NONE', #66364, 1.224999999999999423 ) ;
#18923=ORIENTED_EDGE ( 'NONE', *, *, #26534, .F. ) ;
#18929=CARTESIAN_POINT ( 'NONE',  ( -8.697938382363135545, 8.079219948824830411, 26.00000000000000711 ) ) ;
#18930=ORIENTED_EDGE ( 'NONE', *, *, #47319, .F. ) ;
#18932=ORIENTED_EDGE ( 'NONE', *, *, #786, .T. ) ;
#18933=VECTOR ( 'NONE', #62815, 1000.000000000000000 ) ;
#18934=CARTESIAN_POINT ( 'NONE',  ( 10.50702373788277910, 3.650476262117147375, 26.00000000000000711 ) ) ;
#18945=CARTESIAN_POINT ( 'NONE',  ( -9.547976262117254365, 8.130476262117182884, 26.00000000000000711 ) ) ;
#18946=FACE_OUTER_BOUND ( 'NONE', #44125, .T. ) ;
#18957=ORIENTED_EDGE ( 'NONE', *, *, #45027, .T. ) ;
#18963=AXIS2_PLACEMENT_3D ( 'NONE', #49111, #5301, #22587 ) ;
#18966=EDGE_LOOP ( 'NONE', ( #53589, #16179, #55117, #23798 ) ) ;
#18973=AXIS2_PLACEMENT_3D ( 'NONE', #21428, #5869, #561 ) ;
#18978=CARTESIAN_POINT ( 'NONE',  ( 10.50702373788281996, -6.849523737882823760, 54.00000000000000711 ) ) ;
#18994=LINE ( 'NONE', #3437, #63478 ) ;
#18995=VERTEX_POINT ( 'NONE', #66929 ) ;
#18997=ADVANCED_FACE ( 'NONE', ( #23803 ), #17449, .F. ) ;
#19003=ADVANCED_FACE ( 'NONE', ( #33715 ), #40043, .F. ) ;
#19007=LINE ( 'NONE', #46568, #8158 ) ;
#19013=LINE ( 'NONE', #17619, #32609 ) ;
#19030=DIRECTION ( 'NONE',  ( 0.000000000000000000, -3.673940397442059868E-16, 1.000000000000000000 ) ) ;
#19032=CARTESIAN_POINT ( 'NONE',  ( -10.49297626211729551, -6.849523737882748264, 54.00000000000000711 ) ) ;
#19041=EDGE_CURVE ( 'NONE', #65847, #45123, #17805, .T. ) ;
#19050=EDGE_LOOP ( 'NONE', ( #26505, #730, #16965, #60515 ) ) ;
#19054=CARTESIAN_POINT ( 'NONE',  ( -3.842976262117332453, -10.31452373788281740, 54.00000000000000711 ) ) ;
#19069=CARTESIAN_POINT ( 'NONE',  ( 3.677663764522603795, 6.350872789121277506, 26.00000000000000711 ) ) ;
#19073=DIRECTION ( 'NONE',  ( 2.990116172375847553E-15, 1.000000000000000000, 0.000000000000000000 ) ) ;
#19074=CIRCLE ( 'NONE', #12288, 0.1749999999999998224 ) ;
#19080=EDGE_CURVE ( 'NONE', #17399, #35347, #6395, .T. ) ;
#19084=LINE ( 'NONE', #40647, #61384 ) ;
#19090=CARTESIAN_POINT ( 'NONE',  ( 1.480523737882788238, -9.404523737882783507, 26.00000000000000000 ) ) ;
#19093=DIRECTION ( 'NONE',  ( 2.135044278125299371E-15, 1.000000000000000000, 0.000000000000000000 ) ) ;
#19117=DIRECTION ( 'NONE',  ( -1.000000000000000000, 1.047444401652940007E-14, -1.836970198721010706E-16 ) ) ;
#19124=PLANE ( 'NONE',  #43443 ) ;
#19126=EDGE_CURVE ( 'NONE', #22770, #18604, #68338, .T. ) ;
#19138=ORIENTED_EDGE ( 'NONE', *, *, #34493, .T. ) ;
#19147=LINE ( 'NONE', #57679, #50995 ) ;
#19148=CARTESIAN_POINT ( 'NONE',  ( 5.257023737882819070, -7.186223737882813545, 26.00000000000000000 ) ) ;
#19151=CARTESIAN_POINT ( 'NONE',  ( -6.642976262117334940, -10.31452373788278898, 54.00000000000000711 ) ) ;
#19154=VECTOR ( 'NONE', #28314, 1000.000000000000000 ) ;
#19155=AXIS2_PLACEMENT_3D ( 'NONE', #42077, #31135, #9921 ) ;
#19158=VERTEX_POINT ( 'NONE', #46413 ) ;
#19179=ORIENTED_EDGE ( 'NONE', *, *, #27978, .T. ) ;
#19183=LINE ( 'NONE', #35431, #2635 ) ;
#19189=DIRECTION ( 'NONE',  ( -0.000000000000000000, -0.000000000000000000, -1.000000000000000000 ) ) ;
#19197=LINE ( 'NONE', #47469, #16151 ) ;
#19202=ORIENTED_EDGE ( 'NONE', *, *, #56149, .T. ) ;
#19207=SHAPE_REPRESENTATION_RELATIONSHIP ( 'NONE' , 'NONE' ,  #15926, #52879 ) ;
#19208=CARTESIAN_POINT ( 'NONE',  ( 9.404523737882819034, -0.9555237378828257411, 54.00000000000000711 ) ) ;
#19210=ORIENTED_EDGE ( 'NONE', *, *, #41391, .F. ) ;
#19218=VERTEX_POINT ( 'NONE', #53692 ) ;
#19221=ADVANCED_FACE ( 'NONE', ( #24808 ), #4560, .F. ) ;
#19236=AXIS2_PLACEMENT_3D ( 'NONE', #35055, #36111, #24101 ) ;
#19248=CARTESIAN_POINT ( 'NONE',  ( 6.849523737882817542, -10.50702373788282529, 54.00000000000000711 ) ) ;
#19250=ORIENTED_EDGE ( 'NONE', *, *, #26200, .F. ) ;
#19252=CARTESIAN_POINT ( 'NONE',  ( 3.157023737882819425, -4.046023737882825877, 54.00000000000000711 ) ) ;
#19255=ADVANCED_FACE ( 'NONE', ( #62276 ), #36728, .F. ) ;
#19256=VECTOR ( 'NONE', #42463, 1000.000000000000000 ) ;
#19266=CARTESIAN_POINT ( 'NONE',  ( -7.342976262117282715, -5.552858015815545834, 54.00000000000000711 ) ) ;
#19268=EDGE_CURVE ( 'NONE', #34611, #46340, #19968, .T. ) ;
#19271=VECTOR ( 'NONE', #30585, 1000.000000000000000 ) ;
#19273=EDGE_CURVE ( 'NONE', #32281, #40788, #46365, .T. ) ;
#19283=ORIENTED_EDGE ( 'NONE', *, *, #42574, .T. ) ;
#19284=LINE ( 'NONE', #61350, #29555 ) ;
#19287=ORIENTED_EDGE ( 'NONE', *, *, #53113, .T. ) ;
#19288=DIRECTION ( 'NONE',  ( -1.836970198721029934E-16, -1.836970198721010706E-16, 1.000000000000000000 ) ) ;
#19290=CARTESIAN_POINT ( 'NONE',  ( -5.242976262117259978, 7.172176262117182510, 26.00000000000000711 ) ) ;
#19292=ORIENTED_EDGE ( 'NONE', *, *, #31772, .T. ) ;
#19298=VERTEX_POINT ( 'NONE', #5595 ) ;
#19315=AXIS2_PLACEMENT_3D ( 'NONE', #46406, #14585, #57718 ) ;
#19318=DIRECTION ( 'NONE',  ( 1.073876437509453175E-14, 1.000000000000000000, 0.000000000000000000 ) ) ;
#19325=LINE ( 'NONE', #40888, #65793 ) ;
#19328=LINE ( 'NONE', #40893, #39853 ) ;
#19341=CARTESIAN_POINT ( 'NONE',  ( 6.364920264886884560, 6.822336235477388655, 26.00000000000000711 ) ) ;
#19343=DIRECTION ( 'NONE',  ( 1.000000000000000000, -5.626525616968433909E-15, -1.836970198721040534E-16 ) ) ;
#19350=LINE ( 'NONE', #62472, #17202 ) ;
#19354=CARTESIAN_POINT ( 'NONE',  ( 6.849523737882817542, -10.31452373788282095, 54.00000000000000711 ) ) ;
#19358=VERTEX_POINT ( 'NONE', #54382 ) ;
#19362=ORIENTED_EDGE ( 'NONE', *, *, #67721, .F. ) ;
#19364=CARTESIAN_POINT ( 'NONE',  ( -3.834182069070763976, 7.517976262117170627, 26.00000000000000711 ) ) ;
#19369=CARTESIAN_POINT ( 'NONE',  ( -10.30047626211729472, -6.849523737882750929, 54.00000000000000711 ) ) ;
#19370=CYLINDRICAL_SURFACE ( 'NONE', #37818, 0.1749999999999998224 ) ;
#19392=CARTESIAN_POINT ( 'NONE',  ( 3.664523737882814824, 10.30047626211720768, 26.00000000000000711 ) ) ;
#19393=VERTEX_POINT ( 'NONE', #45130 ) ;
#19405=DIRECTION ( 'NONE',  ( -1.000000000000000000, -1.671920889371702854E-15, -0.000000000000000000 ) ) ;
#19409=CARTESIAN_POINT ( 'NONE',  ( 8.930623737882818602, -8.580623737882856261, 54.00000000000000711 ) ) ;
#19410=ADVANCED_FACE ( 'NONE', ( #2014 ), #30290, .F. ) ;
#19411=FACE_OUTER_BOUND ( 'NONE', #15421, .T. ) ;
#19413=EDGE_CURVE ( 'NONE', #20669, #42591, #67416, .T. ) ;
#19425=CARTESIAN_POINT ( 'NONE',  ( 4.155633711806658859, -5.793274621760842180, 54.00000000000000711 ) ) ;
#19426=EDGE_CURVE ( 'NONE', #56509, #32175, #8349, .T. ) ;
#19433=ORIENTED_EDGE ( 'NONE', *, *, #26376, .F. ) ;
#19454=DIRECTION ( 'NONE',  ( -0.000000000000000000, 3.673940397442059868E-16, -1.000000000000000000 ) ) ;
#19461=CARTESIAN_POINT ( 'NONE',  ( 3.157023737882796333, 5.242976262117212016, 26.00000000000000711 ) ) ;
#19464=CARTESIAN_POINT ( 'NONE',  ( 10.31452373788280497, 6.642976262117183062, 54.00000000000000711 ) ) ;
#19469=EDGE_CURVE ( 'NONE', #51221, #27077, #19659, .T. ) ;
#19478=CARTESIAN_POINT ( 'NONE',  ( 4.149127210878720717, 6.822336235477395761, 26.00000000000000711 ) ) ;
#19483=EDGE_CURVE ( 'NONE', #59231, #20701, #56444, .T. ) ;
#19485=ORIENTED_EDGE ( 'NONE', *, *, #14059, .T. ) ;
#19488=DIRECTION ( 'NONE',  ( 0.6414496315691617934, -0.7671651518152962090, -2.818519042763987834E-16 ) ) ;
#19494=AXIS2_PLACEMENT_3D ( 'NONE', #15099, #62832, #53292 ) ;
#19504=ORIENTED_EDGE ( 'NONE', *, *, #12596, .F. ) ;
#19510=VERTEX_POINT ( 'NONE', #51856 ) ;
#19511=CARTESIAN_POINT ( 'NONE',  ( 8.144523737882817471, -9.562023737882809016, 26.00000000000000000 ) ) ;
#19513=ORIENTED_EDGE ( 'NONE', *, *, #38959, .T. ) ;
#19519=EDGE_LOOP ( 'NONE', ( #32042, #25225, #68147, #25589 ) ) ;
#19520=PLANE ( 'NONE',  #28209 ) ;
#19522=ADVANCED_FACE ( 'NONE', ( #3758 ), #14724, .F. ) ;
#19528=CARTESIAN_POINT ( 'NONE',  ( -3.142976262117274988, -5.257023737882822623, 26.00000000000000711 ) ) ;
#19529=VECTOR ( 'NONE', #56121, 1000.000000000000000 ) ;
#19533=CARTESIAN_POINT ( 'NONE',  ( -5.242976262117299946, -7.186223737882804663, 54.00000000000000711 ) ) ;
#19535=ORIENTED_EDGE ( 'NONE', *, *, #52380, .F. ) ;
#19546=ORIENTED_EDGE ( 'NONE', *, *, #35026, .F. ) ;
#19550=VECTOR ( 'NONE', #25399, 1000.000000000000000 ) ;
#19552=EDGE_CURVE ( 'NONE', #53664, #34294, #35643, .T. ) ;
#19570=ORIENTED_EDGE ( 'NONE', *, *, #16149, .T. ) ;
#19577=CARTESIAN_POINT ( 'NONE',  ( 3.677663764522620227, 4.135079735113113664, 54.00000000000000711 ) ) ;
#19581=VERTEX_POINT ( 'NONE', #42639 ) ;
#19584=VECTOR ( 'NONE', #20259, 1000.000000000000000 ) ;
#19590=VERTEX_POINT ( 'NONE', #69165 ) ;
#19594=EDGE_LOOP ( 'NONE', ( #26955, #13428, #19283, #23591 ) ) ;
#19595=DIRECTION ( 'NONE',  ( 1.062075597536821205E-14, 1.000000000000000000, 0.000000000000000000 ) ) ;
#19601=DIRECTION ( 'NONE',  ( 0.7071067811865401342, -0.7071067811865550112, 0.000000000000000000 ) ) ;
#19604=EDGE_CURVE ( 'NONE', #15802, #28927, #33397, .T. ) ;
#19620=CARTESIAN_POINT ( 'NONE',  ( -9.722976262117258628, 6.817976262117182884, 54.00000000000000711 ) ) ;
#19631=DIRECTION ( 'NONE',  ( -0.000000000000000000, 3.673940397442059868E-16, -1.000000000000000000 ) ) ;
#19637=AXIS2_PLACEMENT_3D ( 'NONE', #43901, #32616, #59131 ) ;
#19642=ORIENTED_EDGE ( 'NONE', *, *, #34273, .T. ) ;
#19643=CARTESIAN_POINT ( 'NONE',  ( -7.394232575409605879, -3.724485858128642413, 54.00000000000000711 ) ) ;
#19647=VERTEX_POINT ( 'NONE', #54651 ) ;
#19650=EDGE_CURVE ( 'NONE', #19510, #19647, #60279, .T. ) ;
#19651=ADVANCED_FACE ( 'NONE', ( #49681 ), #5517, .T. ) ;
#19656=EDGE_CURVE ( 'NONE', #29192, #53417, #62764, .T. ) ;
#19659=LINE ( 'NONE', #29568, #59499 ) ;
#19669=ORIENTED_EDGE ( 'NONE', *, *, #64147, .F. ) ;
#19687=CARTESIAN_POINT ( 'NONE',  ( -7.172176262117259782, 5.242976262117182706, 26.00000000000000711 ) ) ;
#19689=VERTEX_POINT ( 'NONE', #53961 ) ;
#19702=ORIENTED_EDGE ( 'NONE', *, *, #49073, .T. ) ;
#19727=VECTOR ( 'NONE', #32050, 1000.000000000000000 ) ;
#19733=CIRCLE ( 'NONE', #59228, 0.1749999999999998224 ) ;
#19734=CYLINDRICAL_SURFACE ( 'NONE', #44736, 1.929199999999998028 ) ;
#19737=EDGE_CURVE ( 'NONE', #2756, #18679, #65929, .T. ) ;
#19738=DIRECTION ( 'NONE',  ( 1.000000000000000000, -3.491481338843133355E-15, -1.836970198721036590E-16 ) ) ;
#19745=DIRECTION ( 'NONE',  ( -4.956352788505217896E-15, -1.000000000000000000, 0.000000000000000000 ) ) ;
#19768=AXIS2_PLACEMENT_3D ( 'NONE', #46072, #62325, #13892 ) ;
#19770=CARTESIAN_POINT ( 'NONE',  ( 9.912023737882815766, -6.832023737882823688, 54.00000000000000711 ) ) ;
#19783=ORIENTED_EDGE ( 'NONE', *, *, #58473, .F. ) ;
#19797=CARTESIAN_POINT ( 'NONE',  ( 9.795823737882802362, 10.49297626211719070, 26.00000000000000711 ) ) ;
#19805=CARTESIAN_POINT ( 'NONE',  ( -4.031976262117257903, -3.157023737882818981, 54.00000000000000711 ) ) ;
#19808=VERTEX_POINT ( 'NONE', #18536 ) ;
#19817=CIRCLE ( 'NONE', #3988, 0.5249999999999994671 ) ;
#19822=VERTEX_POINT ( 'NONE', #3337 ) ;
#19823=ORIENTED_EDGE ( 'NONE', *, *, #61813, .T. ) ;
#19824=ADVANCED_FACE ( 'NONE', ( #46462 ), #45406, .F. ) ;
#19826=AXIS2_PLACEMENT_3D ( 'NONE', #36430, #30429, #21233 ) ;
#19838=DIRECTION ( 'NONE',  ( -1.000000000000000000, 0.000000000000000000, 0.000000000000000000 ) ) ;
#19842=CIRCLE ( 'NONE', #68408, 0.1749999999999989342 ) ;
#19850=CARTESIAN_POINT ( 'NONE',  ( -8.227189898828694226, -1.634292677759810575, 26.00000000000000711 ) ) ;
#19853=DIRECTION ( 'NONE',  ( 0.000000000000000000, 1.000000000000000000, 0.000000000000000000 ) ) ;
#19854=VERTEX_POINT ( 'NONE', #8275 ) ;
#19858=DIRECTION ( 'NONE',  ( 1.836970198721029934E-16, 1.836970198721010706E-16, -1.000000000000000000 ) ) ;
#19861=DIRECTION ( 'NONE',  ( -1.836970198721029934E-16, 1.836970198721036590E-16, -1.000000000000000000 ) ) ;
#19869=VECTOR ( 'NONE', #67227, 1000.000000000000000 ) ;
#19870=AXIS2_PLACEMENT_3D ( 'NONE', #51873, #62823, #52213 ) ;
#19878=DIRECTION ( 'NONE',  ( 0.000000000000000000, -3.673940397442059868E-16, 1.000000000000000000 ) ) ;
#19879=CIRCLE ( 'NONE', #2919, 0.1749999999999998224 ) ;
#19882=VECTOR ( 'NONE', #13720, 1000.000000000000000 ) ;
#19889=ORIENTED_EDGE ( 'NONE', *, *, #48091, .F. ) ;
#19890=ORIENTED_EDGE ( 'NONE', *, *, #30878, .F. ) ;
#19895=FACE_OUTER_BOUND ( 'NONE', #34601, .T. ) ;
#19901=CARTESIAN_POINT ( 'NONE',  ( -8.697938382363098242, -2.420780051175094094, 26.00000000000000711 ) ) ;
#19904=ORIENTED_EDGE ( 'NONE', *, *, #58982, .F. ) ;
#19907=EDGE_LOOP ( 'NONE', ( #51135, #7700, #66689, #13446 ) ) ;
#19911=ORIENTED_EDGE ( 'NONE', *, *, #18453, .T. ) ;
#19920=VERTEX_POINT ( 'NONE', #36204 ) ;
#19921=VECTOR ( 'NONE', #36383, 1000.000000000000000 ) ;
#19925=CARTESIAN_POINT ( 'NONE',  ( 6.872275254348378937, 2.989207322240125198, 26.00000000000000711 ) ) ;
#19926=VERTEX_POINT ( 'NONE', #20995 ) ;
#19932=DIRECTION ( 'NONE',  ( 1.000000000000000000, 1.671920889371702854E-15, 6.142537696789956391E-31 ) ) ;
#19934=CARTESIAN_POINT ( 'NONE',  ( -9.547976262117256141, 7.955476262117183062, 26.00000000000000711 ) ) ;
#19945=AXIS2_PLACEMENT_3D ( 'NONE', #54136, #60113, #44190 ) ;
#19955=EDGE_CURVE ( 'NONE', #65565, #54361, #52850, .T. ) ;
#19957=EDGE_LOOP ( 'NONE', ( #62497, #56180, #29003, #51532 ) ) ;
#19968=CIRCLE ( 'NONE', #34473, 0.1749999999999989342 ) ;
#19980=ORIENTED_EDGE ( 'NONE', *, *, #17259, .T. ) ;
#19987=ORIENTED_EDGE ( 'NONE', *, *, #6529, .T. ) ;
#19989=CIRCLE ( 'NONE', #43711, 0.1749999999999998224 ) ;
#19990=CARTESIAN_POINT ( 'NONE',  ( 9.703773737882816164, 9.689726262117153155, 54.00000000000000711 ) ) ;
#19997=CARTESIAN_POINT ( 'NONE',  ( -3.650476262117329007, -10.31452373788281385, 26.00000000000000000 ) ) ;
#20001=EDGE_LOOP ( 'NONE', ( #38947, #41176, #56253, #56684 ) ) ;
#20002=ORIENTED_EDGE ( 'NONE', *, *, #5588, .F. ) ;
#20006=ORIENTED_EDGE ( 'NONE', *, *, #21976, .T. ) ;
#20018=ADVANCED_FACE ( 'NONE', ( #482 ), #59869, .F. ) ;
#20022=DIRECTION ( 'NONE',  ( -1.000000000000000000, 0.000000000000000000, 0.000000000000000000 ) ) ;
#20027=VECTOR ( 'NONE', #13873, 1000.000000000000000 ) ;
#20029=LINE ( 'NONE', #25697, #53956 ) ;
#20036=DIRECTION ( 'NONE',  ( 1.836970198721029934E-16, 1.836970198721010706E-16, -1.000000000000000000 ) ) ;
#20049=ORIENTED_EDGE ( 'NONE', *, *, #17983, .F. ) ;
#20056=DIRECTION ( 'NONE',  ( 0.7671651518152985405, 0.6414496315691592399, -2.309356642088639737E-17 ) ) ;
#20058=CARTESIAN_POINT ( 'NONE',  ( -3.650476262117223314, 10.30047626211716683, 54.00000000000000711 ) ) ;
#20059=EDGE_CURVE ( 'NONE', #6346, #62186, #21352, .T. ) ;
#20068=LINE ( 'NONE', #41631, #28440 ) ;
#20069=ORIENTED_EDGE ( 'NONE', *, *, #52806, .F. ) ;
#20070=AXIS2_PLACEMENT_3D ( 'NONE', #44427, #59329, #5932 ) ;
#20075=ORIENTED_EDGE ( 'NONE', *, *, #29369, .F. ) ;
#20076=ORIENTED_EDGE ( 'NONE', *, *, #37080, .T. ) ;
#20102=VERTEX_POINT ( 'NONE', #42910 ) ;
#20105=EDGE_CURVE ( 'NONE', #25597, #6930, #38002, .T. ) ;
#20107=ORIENTED_EDGE ( 'NONE', *, *, #52894, .F. ) ;
#20118=ORIENTED_EDGE ( 'NONE', *, *, #53945, .T. ) ;
#20119=LINE ( 'NONE', #42029, #53526 ) ;
#20122=LINE ( 'NONE', #14819, #9271 ) ;
#20129=AXIS2_PLACEMENT_3D ( 'NONE', #17271, #38836, #37815 ) ;
#20138=EDGE_LOOP ( 'NONE', ( #20291, #4540, #29372, #30163 ) ) ;
#20140=LINE ( 'NONE', #51968, #9800 ) ;
#20146=ORIENTED_EDGE ( 'NONE', *, *, #22440, .F. ) ;
#20150=VERTEX_POINT ( 'NONE', #56982 ) ;
#20162=CYLINDRICAL_SURFACE ( 'NONE', #18248, 0.1749999999999998224 ) ;
#20164=VERTEX_POINT ( 'NONE', #18105 ) ;
#20165=ORIENTED_EDGE ( 'NONE', *, *, #60643, .T. ) ;
#20186=ORIENTED_EDGE ( 'NONE', *, *, #68874, .T. ) ;
#20187=VERTEX_POINT ( 'NONE', #55603 ) ;
#20192=DIRECTION ( 'NONE',  ( 0.000000000000000000, -3.673940397442059868E-16, 1.000000000000000000 ) ) ;
#20193=CYLINDRICAL_SURFACE ( 'NONE', #11390, 1.224999999999998757 ) ;
#20198=ADVANCED_FACE ( 'NONE', ( #50640 ), #2203, .F. ) ;
#20201=CARTESIAN_POINT ( 'NONE',  ( 5.257023737882795977, 5.242976262117205799, 26.00000000000000711 ) ) ;
#20202=FACE_OUTER_BOUND ( 'NONE', #37454, .T. ) ;
#20212=EDGE_CURVE ( 'NONE', #54442, #53865, #67256, .T. ) ;
#20218=ORIENTED_EDGE ( 'NONE', *, *, #37103, .T. ) ;
#20221=DIRECTION ( 'NONE',  ( -0.000000000000000000, 3.673940397442059868E-16, -1.000000000000000000 ) ) ;
#20223=DIRECTION ( 'NONE',  ( 0.7671651518152998728, -0.6414496315691575745, 2.309356642088859447E-17 ) ) ;
#20228=ORIENTED_EDGE ( 'NONE', *, *, #69159, .T. ) ;
#20230=DIRECTION ( 'NONE',  ( 0.000000000000000000, 1.000000000000000000, 0.000000000000000000 ) ) ;
#20235=LINE ( 'NONE', #52792, #49853 ) ;
#20237=EDGE_CURVE ( 'NONE', #27218, #17399, #56643, .T. ) ;
#20238=ORIENTED_EDGE ( 'NONE', *, *, #48788, .F. ) ;
#20243=VECTOR ( 'NONE', #38817, 1000.000000000000000 ) ;
#20244=AXIS2_PLACEMENT_3D ( 'NONE', #15692, #59517, #38302 ) ;
#20255=ORIENTED_EDGE ( 'NONE', *, *, #47918, .T. ) ;
#20257=CARTESIAN_POINT ( 'NONE',  ( -0.9414762621172296786, 9.390476262117148920, 54.00000000000000711 ) ) ;
#20258=LINE ( 'NONE', #41822, #45648 ) ;
#20259=DIRECTION ( 'NONE',  ( -1.836970198721029934E-16, 1.836970198721036590E-16, -1.000000000000000000 ) ) ;
#20261=ORIENTED_EDGE ( 'NONE', *, *, #13677, .T. ) ;
#20262=ORIENTED_EDGE ( 'NONE', *, *, #56325, .T. ) ;
#20263=FACE_OUTER_BOUND ( 'NONE', #1550, .T. ) ;
#20282=EDGE_LOOP ( 'NONE', ( #55830, #11529, #9630, #27605 ) ) ;
#20289=DIRECTION ( 'NONE',  ( 0.000000000000000000, 0.000000000000000000, 1.000000000000000000 ) ) ;
#20290=EDGE_CURVE ( 'NONE', #6502, #69903, #69351, .T. ) ;
#20291=ORIENTED_EDGE ( 'NONE', *, *, #20865, .F. ) ;
#20299=ADVANCED_FACE ( 'NONE', ( #31190 ), #63358, .F. ) ;
#20302=CARTESIAN_POINT ( 'NONE',  ( -6.350872789121327244, 3.663616288756986084, 54.00000000000000711 ) ) ;
#20308=ADVANCED_FACE ( 'NONE', ( #25531 ), #42123, .F. ) ;
#20314=DIRECTION ( 'NONE',  ( 6.508391731846281342E-15, 1.000000000000000000, 0.000000000000000000 ) ) ;
#20315=CARTESIAN_POINT ( 'NONE',  ( -3.142976262117280317, -5.257023737882827952, 54.00000000000000711 ) ) ;
#20326=CARTESIAN_POINT ( 'NONE',  ( 8.930623737882818602, -10.05377373788281581, 26.00000000000000000 ) ) ;
#20330=CIRCLE ( 'NONE', #38400, 0.1749999999999989342 ) ;
#20331=DIRECTION ( 'NONE',  ( 0.6414496315691526895, 0.7671651518153038696, 2.587583378555111534E-16 ) ) ;
#20336=CARTESIAN_POINT ( 'NONE',  ( 6.665817930929288870, 7.342976262117195674, 54.00000000000000711 ) ) ;
#20349=DIRECTION ( 'NONE',  ( -0.6414496315691617934, 0.7671651518152962090, 0.000000000000000000 ) ) ;
#20354=ORIENTED_EDGE ( 'NONE', *, *, #2672, .T. ) ;
#20365=ORIENTED_EDGE ( 'NONE', *, *, #16604, .T. ) ;
#20367=ORIENTED_EDGE ( 'NONE', *, *, #57253, .T. ) ;
#20381=CARTESIAN_POINT ( 'NONE',  ( -8.916576262117340335, -8.580623737882760338, 26.00000000000000000 ) ) ;
#20399=DIRECTION ( 'NONE',  ( 9.912705577010386883E-15, 1.000000000000000000, 0.000000000000000000 ) ) ;
#20401=FACE_OUTER_BOUND ( 'NONE', #3365, .T. ) ;
#20402=DIRECTION ( 'NONE',  ( 0.000000000000000000, 1.000000000000000000, 3.673940397442059868E-16 ) ) ;
#20403=DIRECTION ( 'NONE',  ( 1.000000000000000000, 0.000000000000000000, 0.000000000000000000 ) ) ;
#20404=DIRECTION ( 'NONE',  ( -0.7671651518152985405, -0.6414496315691592399, 0.000000000000000000 ) ) ;
#20406=ORIENTED_EDGE ( 'NONE', *, *, #58322, .T. ) ;
#20412=ORIENTED_EDGE ( 'NONE', *, *, #49126, .F. ) ;
#20416=VERTEX_POINT ( 'NONE', #42827 ) ;
#20420=DIRECTION ( 'NONE',  ( -1.836970198721029934E-16, 1.836970198721036590E-16, -1.000000000000000000 ) ) ;
#20425=CIRCLE ( 'NONE', #36215, 0.1749999999999993783 ) ;
#20430=CARTESIAN_POINT ( 'NONE',  ( 4.155633711806658859, -4.720772854004808394, 54.00000000000000711 ) ) ;
#20431=CARTESIAN_POINT ( 'NONE',  ( -3.663616288757094885, -6.364920264886888113, 54.00000000000000711 ) ) ;
#20437=CIRCLE ( 'NONE', #48817, 0.5249999999999994671 ) ;
#20443=VECTOR ( 'NONE', #28071, 1000.000000000000114 ) ;
#20454=CARTESIAN_POINT ( 'NONE',  ( 8.930623737882848800, 9.689726262117154931, 54.00000000000000711 ) ) ;
#20460=EDGE_CURVE ( 'NONE', #21898, #59501, #50205, .T. ) ;
#20464=ORIENTED_EDGE ( 'NONE', *, *, #35520, .F. ) ;
#20465=CARTESIAN_POINT ( 'NONE',  ( -4.135079735113214916, -6.836383711243002814, 54.00000000000000711 ) ) ;
#20473=LINE ( 'NONE', #68917, #19921 ) ;
#20474=CARTESIAN_POINT ( 'NONE',  ( -9.722976262117258628, 3.667976262117184749, 54.00000000000000711 ) ) ;
#20487=VECTOR ( 'NONE', #6422, 1000.000000000000114 ) ;
#20490=DIRECTION ( 'NONE',  ( -0.000000000000000000, 3.673940397442059868E-16, -1.000000000000000000 ) ) ;
#20498=ORIENTED_EDGE ( 'NONE', *, *, #13681, .F. ) ;
#20504=CARTESIAN_POINT ( 'NONE',  ( 9.929523737882817613, -0.9555237378828257411, 54.00000000000000711 ) ) ;
#20506=VERTEX_POINT ( 'NONE', #7412 ) ;
#20508=CARTESIAN_POINT ( 'NONE',  ( -6.350872789121319251, -3.677663764522589140, 54.00000000000000711 ) ) ;
#20520=CARTESIAN_POINT ( 'NONE',  ( 5.793274621760843957, -4.155633711806670405, 54.00000000000000711 ) ) ;
#20526=AXIS2_PLACEMENT_3D ( 'NONE', #21600, #53784, #54476 ) ;
#20529=CARTESIAN_POINT ( 'NONE',  ( 6.665817930929297752, -7.357023737882824044, 54.00000000000000711 ) ) ;
#20532=VECTOR ( 'NONE', #26164, 1000.000000000000114 ) ;
#20539=EDGE_CURVE ( 'NONE', #18238, #42804, #26735, .T. ) ;
#20542=CARTESIAN_POINT ( 'NONE',  ( -10.49297626211725110, -3.664523737882711352, 54.00000000000000711 ) ) ;
#20543=ADVANCED_FACE ( 'NONE', ( #28634 ), #51247, .F. ) ;
#20544=CARTESIAN_POINT ( 'NONE',  ( 3.677663764522614454, -4.149127210878770455, 54.00000000000000711 ) ) ;
#20556=LINE ( 'NONE', #14548, #69916 ) ;
#20557=ORIENTED_EDGE ( 'NONE', *, *, #65780, .F. ) ;
#20563=CARTESIAN_POINT ( 'NONE',  ( 10.50702373788281996, -6.849523737882814878, 26.00000000000000000 ) ) ;
#20568=DIRECTION ( 'NONE',  ( -0.6414496315691565753, 0.7671651518153006499, 0.000000000000000000 ) ) ;
#20572=FACE_OUTER_BOUND ( 'NONE', #50676, .T. ) ;
#20580=DIRECTION ( 'NONE',  ( -0.000000000000000000, 3.673940397442059868E-16, -1.000000000000000000 ) ) ;
#20583=EDGE_CURVE ( 'NONE', #1459, #8910, #55522, .T. ) ;
#20584=DIRECTION ( 'NONE',  ( -0.7671651518153006499, -0.6414496315691565753, -2.356647714346250026E-16 ) ) ;
#20599=EDGE_LOOP ( 'NONE', ( #50616, #57614, #29263, #20075, #55134, #19362, #50674, #44862, #2490, #64187, #62404, #20915, #33857, #18226, #16879, #8338, #17807 ) ) ;
#20608=ORIENTED_EDGE ( 'NONE', *, *, #61380, .T. ) ;
#20620=EDGE_LOOP ( 'NONE', ( #26361, #39677, #67854, #46593 ) ) ;
#20637=EDGE_CURVE ( 'NONE', #37879, #35090, #14118, .T. ) ;
#20639=DIRECTION ( 'NONE',  ( -0.7071067811865474617, 0.7071067811865474617, 2.597868168706479611E-16 ) ) ;
#20640=AXIS2_PLACEMENT_3D ( 'NONE', #515, #22082, #43645 ) ;
#20649=CIRCLE ( 'NONE', #49969, 0.5250000000000003553 ) ;
#20655=CARTESIAN_POINT ( 'NONE',  ( -6.822336235477446387, -4.149127210878696737, 54.00000000000000711 ) ) ;
#20657=CARTESIAN_POINT ( 'NONE',  ( -7.517976262117260333, 3.834182069070703580, 26.00000000000000711 ) ) ;
#20662=LINE ( 'NONE', #4430, #28880 ) ;
#20663=EDGE_CURVE ( 'NONE', #49486, #49797, #62918, .T. ) ;
#20664=CARTESIAN_POINT ( 'NONE',  ( 7.357023737882797398, 4.947141984184415087, 54.00000000000000711 ) ) ;
#20669=VERTEX_POINT ( 'NONE', #68577 ) ;
#20671=DIRECTION ( 'NONE',  ( -0.000000000000000000, -0.000000000000000000, -1.000000000000000000 ) ) ;
#20682=EDGE_CURVE ( 'NONE', #49997, #16772, #67872, .T. ) ;
#20692=DIRECTION ( 'NONE',  ( 1.000000000000000000, -3.491481338843133355E-15, -1.836970198721036344E-16 ) ) ;
#20693=ORIENTED_EDGE ( 'NONE', *, *, #8803, .T. ) ;
#20695=VECTOR ( 'NONE', #30519, 1000.000000000000000 ) ;
#20701=VERTEX_POINT ( 'NONE', #69965 ) ;
#20703=VECTOR ( 'NONE', #53280, 1000.000000000000000 ) ;
#20712=ORIENTED_EDGE ( 'NONE', *, *, #25487, .F. ) ;
#20713=EDGE_LOOP ( 'NONE', ( #50944, #43529, #35553, #45276 ) ) ;
#20715=DIRECTION ( 'NONE',  ( 0.000000000000000000, 1.000000000000000000, 0.000000000000000000 ) ) ;
#20718=ORIENTED_EDGE ( 'NONE', *, *, #2494, .F. ) ;
#20729=DIRECTION ( 'NONE',  ( -1.836970198721029934E-16, 1.836970198721036344E-16, -1.000000000000000000 ) ) ;
#20730=ORIENTED_EDGE ( 'NONE', *, *, #36056, .T. ) ;
#20731=LINE ( 'NONE', #9428, #60646 ) ;
#20733=CARTESIAN_POINT ( 'NONE',  ( -0.9414762621172249046, 9.915476262117151052, 54.00000000000000711 ) ) ;
#20734=DIRECTION ( 'NONE',  ( -1.836970198721029934E-16, 1.836970198721036590E-16, -1.000000000000000000 ) ) ;
#20745=LINE ( 'NONE', #57180, #26500 ) ;
#20748=CARTESIAN_POINT ( 'NONE',  ( 7.408280051175172076, -3.724485858128690818, 26.00000000000000711 ) ) ;
#20751=VECTOR ( 'NONE', #12412, 1000.000000000000000 ) ;
#20757=DIRECTION ( 'NONE',  ( 0.000000000000000000, 1.000000000000000000, 0.000000000000000000 ) ) ;
#20758=ORIENTED_EDGE ( 'NONE', *, *, #52722, .F. ) ;
#20759=EDGE_CURVE ( 'NONE', #68364, #18995, #10918, .T. ) ;
#20775=ORIENTED_EDGE ( 'NONE', *, *, #54393, .F. ) ;
#20779=VERTEX_POINT ( 'NONE', #19252 ) ;
#20780=ORIENTED_EDGE ( 'NONE', *, *, #12467, .T. ) ;
#20781=EDGE_CURVE ( 'NONE', #3816, #2345, #1011, .T. ) ;
#20795=DIRECTION ( 'NONE',  ( 0.000000000000000000, 3.673940397442059868E-16, -1.000000000000000000 ) ) ;
#20799=AXIS2_PLACEMENT_3D ( 'NONE', #31839, #33206, #10598 ) ;
#20801=EDGE_CURVE ( 'NONE', #45585, #43786, #24569, .T. ) ;
#20803=ADVANCED_FACE ( 'NONE', ( #17244 ), #45415, .F. ) ;
#20807=VERTEX_POINT ( 'NONE', #29511 ) ;
#20810=VECTOR ( 'NONE', #61530, 1000.000000000000000 ) ;
#20812=DIRECTION ( 'NONE',  ( -1.000000000000000000, 0.000000000000000000, 0.000000000000000000 ) ) ;
#20815=CARTESIAN_POINT ( 'NONE',  ( 6.849523737882818430, 10.30047626211719169, 54.00000000000000711 ) ) ;
#20816=ORIENTED_EDGE ( 'NONE', *, *, #64702, .F. ) ;
#20818=DIRECTION ( 'NONE',  ( -0.000000000000000000, -0.000000000000000000, -1.000000000000000000 ) ) ;
#20829=CARTESIAN_POINT ( 'NONE',  ( 4.155633711806658859, -5.793274621760832410, 26.00000000000000711 ) ) ;
#20831=AXIS2_PLACEMENT_3D ( 'NONE', #15693, #42556, #64146 ) ;
#20832=VERTEX_POINT ( 'NONE', #68046 ) ;
#20836=ADVANCED_FACE ( 'NONE', ( #41164 ), #56382, .T. ) ;
#20845=ADVANCED_FACE ( 'NONE', ( #46470 ), #34804, .F. ) ;
#20856=ORIENTED_EDGE ( 'NONE', *, *, #56465, .F. ) ;
#20858=DIRECTION ( 'NONE',  ( 0.000000000000000000, -3.673940397442059868E-16, 1.000000000000000000 ) ) ;
#20863=VECTOR ( 'NONE', #48743, 1000.000000000000000 ) ;
#20865=EDGE_CURVE ( 'NONE', #16269, #1435, #27937, .T. ) ;
#20869=DIRECTION ( 'NONE',  ( -1.000000000000000000, 0.000000000000000000, 0.000000000000000000 ) ) ;
#20870=DIRECTION ( 'NONE',  ( -1.836970198721029934E-16, 1.836970198721036344E-16, -1.000000000000000000 ) ) ;
#20871=EDGE_LOOP ( 'NONE', ( #641, #56667, #17930, #26253 ) ) ;
#20875=DIRECTION ( 'NONE',  ( -0.8660254037844400399, -0.4999999999999973910, 6.723777587268495961E-17 ) ) ;
#20880=LINE ( 'NONE', #6017, #60554 ) ;
#20881=AXIS2_PLACEMENT_3D ( 'NONE', #41147, #68737, #41849 ) ;
#20891=FACE_OUTER_BOUND ( 'NONE', #50294, .T. ) ;
#20892=CARTESIAN_POINT ( 'NONE',  ( 4.046023737882794791, 3.142976262117205266, 54.00000000000000711 ) ) ;
#20904=CARTESIAN_POINT ( 'NONE',  ( -7.342976262117259623, 3.834182069070703580, 54.00000000000000711 ) ) ;
#20905=AXIS2_PLACEMENT_3D ( 'NONE', #20257, #63753, #41821 ) ;
#20912=DIRECTION ( 'NONE',  ( 1.836970198721029934E-16, 1.836970198721010706E-16, -1.000000000000000000 ) ) ;
#20913=VECTOR ( 'NONE', #29073, 1000.000000000000000 ) ;
#20915=ORIENTED_EDGE ( 'NONE', *, *, #15181, .F. ) ;
#20917=FACE_OUTER_BOUND ( 'NONE', #18411, .T. ) ;
#20920=EDGE_CURVE ( 'NONE', #26334, #62286, #41869, .T. ) ;
#20923=CARTESIAN_POINT ( 'NONE',  ( 3.848229544836322180, -7.532023737882811432, 54.00000000000000711 ) ) ;
#20926=CARTESIAN_POINT ( 'NONE',  ( 9.703773737882785966, -8.930623737882855906, 54.00000000000000711 ) ) ;
#20931=ORIENTED_EDGE ( 'NONE', *, *, #9528, .T. ) ;
#20939=AXIS2_PLACEMENT_3D ( 'NONE', #13384, #45911, #8064 ) ;
#20956=LINE ( 'NONE', #64118, #41167 ) ;
#20982=AXIS2_PLACEMENT_3D ( 'NONE', #50826, #66406, #2396 ) ;
#20984=DIRECTION ( 'NONE',  ( -0.000000000000000000, 3.673940397442059868E-16, -1.000000000000000000 ) ) ;
#20990=ORIENTED_EDGE ( 'NONE', *, *, #34809, .F. ) ;
#20995=CARTESIAN_POINT ( 'NONE',  ( 10.50702373788280219, 6.835476262117187396, 26.00000000000000711 ) ) ;
#21001=VECTOR ( 'NONE', #30971, 1000.000000000000000 ) ;
#21004=PLANE ( 'NONE',  #59319 ) ;
#21005=VECTOR ( 'NONE', #22408, 1000.000000000000000 ) ;
#21021=EDGE_LOOP ( 'NONE', ( #32873, #58095, #27339, #36408 ) ) ;
#21023=CARTESIAN_POINT ( 'NONE',  ( 6.364920264886885448, -6.836383711243011696, 26.00000000000000000 ) ) ;
#21026=CARTESIAN_POINT ( 'NONE',  ( 9.562023737882764607, 2.355476262117153663, 54.00000000000000711 ) ) ;
#21028=EDGE_CURVE ( 'NONE', #46021, #40627, #44292, .T. ) ;
#21033=VECTOR ( 'NONE', #53305, 1000.000000000000000 ) ;
#21040=EDGE_CURVE ( 'NONE', #47795, #47021, #50541, .T. ) ;
#21041=PLANE ( 'NONE',  #36585 ) ;
#21047=VECTOR ( 'NONE', #39557, 1000.000000000000114 ) ;
#21049=ORIENTED_EDGE ( 'NONE', *, *, #57640, .F. ) ;
#21057=ORIENTED_EDGE ( 'NONE', *, *, #22563, .F. ) ;
#21059=CARTESIAN_POINT ( 'NONE',  ( 6.665817930929288870, 7.342976262117195674, 54.00000000000000711 ) ) ;
#21086=PLANE ( 'NONE',  #37630 ) ;
#21095=VERTEX_POINT ( 'NONE', #5460 ) ;
#21096=LINE ( 'NONE', #4146, #43912 ) ;
#21099=AXIS2_PLACEMENT_3D ( 'NONE', #10994, #54485, #1083 ) ;
#21108=DIRECTION ( 'NONE',  ( 1.000000000000000000, 0.000000000000000000, 0.000000000000000000 ) ) ;
#21111=DIRECTION ( 'NONE',  ( 0.000000000000000000, 0.000000000000000000, 1.000000000000000000 ) ) ;
#21118=LINE ( 'NONE', #42676, #21033 ) ;
#21137=CARTESIAN_POINT ( 'NONE',  ( 5.552858015815581361, -7.357023737882824044, 54.00000000000000711 ) ) ;
#21138=LINE ( 'NONE', #264, #8986 ) ;
#21140=ORIENTED_EDGE ( 'NONE', *, *, #69269, .F. ) ;
#21145=VECTOR ( 'NONE', #62521, 1000.000000000000000 ) ;
#21149=DIRECTION ( 'NONE',  ( -1.000000000000000000, 0.000000000000000000, 0.000000000000000000 ) ) ;
#21171=ORIENTED_EDGE ( 'NONE', *, *, #33608, .F. ) ;
#21175=DIRECTION ( 'NONE',  ( 1.836970198721029934E-16, 1.836970198721010706E-16, -1.000000000000000000 ) ) ;
#21188=AXIS2_PLACEMENT_3D ( 'NONE', #34727, #13164, #3262 ) ;
#21190=ADVANCED_FACE ( 'NONE', ( #2907 ), #55954, .F. ) ;
#21195=CYLINDRICAL_SURFACE ( 'NONE', #7187, 0.1749999999999989342 ) ;
#21199=ADVANCED_FACE ( 'NONE', ( #50297 ), #29084, .T. ) ;
#21203=VECTOR ( 'NONE', #15781, 1000.000000000000000 ) ;
#21206=DIRECTION ( 'NONE',  ( -9.912705577010344285E-15, -1.000000000000000000, 0.000000000000000000 ) ) ;
#21211=ORIENTED_EDGE ( 'NONE', *, *, #2482, .F. ) ;
#21213=CARTESIAN_POINT ( 'NONE',  ( -6.822336235477441946, -4.149127210878692296, 26.00000000000000711 ) ) ;
#21215=ORIENTED_EDGE ( 'NONE', *, *, #38588, .T. ) ;
#21219=LINE ( 'NONE', #5305, #41175 ) ;
#21222=ORIENTED_EDGE ( 'NONE', *, *, #33567, .T. ) ;
#21224=ADVANCED_FACE ( 'NONE', ( #8553 ), #7510, .F. ) ;
#21225=ORIENTED_EDGE ( 'NONE', *, *, #67052, .T. ) ;
#21227=EDGE_CURVE ( 'NONE', #114, #4139, #67617, .T. ) ;
#21231=CARTESIAN_POINT ( 'NONE',  ( 2.420780051175147829, -8.711985858128677762, 54.00000000000000711 ) ) ;
#21233=DIRECTION ( 'NONE',  ( 1.000000000000000000, 0.000000000000000000, 0.000000000000000000 ) ) ;
#21239=ORIENTED_EDGE ( 'NONE', *, *, #63778, .F. ) ;
#21240=FACE_OUTER_BOUND ( 'NONE', #35030, .T. ) ;
#21241=CARTESIAN_POINT ( 'NONE',  ( -9.689726262117227762, 8.916576262117214213, 54.00000000000000711 ) ) ;
#21243=ORIENTED_EDGE ( 'NONE', *, *, #37412, .F. ) ;
#21257=EDGE_LOOP ( 'NONE', ( #13403, #50149, #22426, #37856, #27343, #47308, #17561, #47862, #67249, #27374, #10493, #31123, #62897, #38954, #41976, #2241, #66852 ) ) ;
#21270=ADVANCED_FACE ( 'NONE', ( #14929 ), #63367, .F. ) ;
#21274=CARTESIAN_POINT ( 'NONE',  ( -7.290476262117262074, 9.722976262117178692, 54.00000000000000711 ) ) ;
#21282=DIRECTION ( 'NONE',  ( 1.836970198721029934E-16, 1.836970198721010706E-16, -1.000000000000000000 ) ) ;
#21288=ORIENTED_EDGE ( 'NONE', *, *, #12599, .T. ) ;
#21295=EDGE_LOOP ( 'NONE', ( #53902, #29368, #52693, #52953 ) ) ;
#21306=AXIS2_PLACEMENT_3D ( 'NONE', #2101, #67850, #46275 ) ;
#21324=CYLINDRICAL_SURFACE ( 'NONE', #12803, 0.1749999999999998224 ) ;
#21325=CARTESIAN_POINT ( 'NONE',  ( -8.821682069070780230, 7.955476262117183062, 26.00000000000000711 ) ) ;
#21326=ORIENTED_EDGE ( 'NONE', *, *, #62252, .T. ) ;
#21331=ADVANCED_FACE ( 'NONE', ( #20572 ), #63014, .F. ) ;
#21338=ADVANCED_FACE ( 'NONE', ( #30482 ), #15278, .F. ) ;
#21341=EDGE_CURVE ( 'NONE', #7480, #11799, #31894, .T. ) ;
#21352=LINE ( 'NONE', #38652, #51505 ) ;
#21360=CARTESIAN_POINT ( 'NONE',  ( -6.344366288193441505, -5.793274621760819088, 54.00000000000000711 ) ) ;
#21363=FACE_OUTER_BOUND ( 'NONE', #23303, .T. ) ;
#21366=FACE_OUTER_BOUND ( 'NONE', #54038, .T. ) ;
#21385=LINE ( 'NONE', #31323, #18288 ) ;
#21386=VERTEX_POINT ( 'NONE', #37895 ) ;
#21390=ORIENTED_EDGE ( 'NONE', *, *, #48435, .T. ) ;
#21392=VECTOR ( 'NONE', #7085, 1000.000000000000000 ) ;
#21393=AXIS2_PLACEMENT_3D ( 'NONE', #28240, #49811, #1376 ) ;
#21400=ORIENTED_EDGE ( 'NONE', *, *, #66579, .F. ) ;
#21406=VERTEX_POINT ( 'NONE', #59797 ) ;
#21407=AXIS2_PLACEMENT_3D ( 'NONE', #66995, #18554, #40111 ) ;
#21410=MANIFOLD_SOLID_BREP ( 'Scale1', #4703 ) ;
#21411=LINE ( 'NONE', #36623, #29052 ) ;
#21414=FACE_OUTER_BOUND ( 'NONE', #28843, .T. ) ;
#21416=EDGE_LOOP ( 'NONE', ( #3053, #41460, #11166, #20367 ) ) ;
#21424=ORIENTED_EDGE ( 'NONE', *, *, #31581, .F. ) ;
#21428=CARTESIAN_POINT ( 'NONE',  ( -0.9414762621173239365, -9.404523737882849233, 54.00000000000000711 ) ) ;
#21438=VECTOR ( 'NONE', #50126, 1000.000000000000000 ) ;
#21439=VERTEX_POINT ( 'NONE', #50575 ) ;
#21440=DIRECTION ( 'NONE',  ( 1.000000000000000000, -1.047444401652940007E-14, 0.000000000000000000 ) ) ;
#21447=CARTESIAN_POINT ( 'NONE',  ( -8.821682069070751808, -2.544523737882741887, 54.00000000000000711 ) ) ;
#21450=DIRECTION ( 'NONE',  ( -3.491481338843133355E-15, -1.000000000000000000, -1.836970198721029934E-16 ) ) ;
#21451=DIRECTION ( 'NONE',  ( -2.439149994343049068E-15, -1.000000000000000000, 0.000000000000000000 ) ) ;
#21455=ORIENTED_EDGE ( 'NONE', *, *, #61100, .F. ) ;
#21464=ADVANCED_FACE ( 'NONE', ( #12364, #2129, #60820, #18030, #45249, #7424, #66132, #50219, #39597, #28642 ), #30046, .F. ) ;
#21476=CARTESIAN_POINT ( 'NONE',  ( -8.916576262117358098, -9.703773737882734451, 54.00000000000000711 ) ) ;
#21477=DIRECTION ( 'NONE',  ( 0.000000000000000000, 3.673940397442059868E-16, -1.000000000000000000 ) ) ;
#21488=VERTEX_POINT ( 'NONE', #19090 ) ;
#21508=ORIENTED_EDGE ( 'NONE', *, *, #22748, .F. ) ;
#21509=DIRECTION ( 'NONE',  ( -1.034072152899300274E-14, -1.000000000000000000, 0.000000000000000000 ) ) ;
#21512=CARTESIAN_POINT ( 'NONE',  ( 9.404523737882753309, 1.466476262117160312, 26.00000000000000711 ) ) ;
#21515=LINE ( 'NONE', #16570, #8218 ) ;
#21525=VECTOR ( 'NONE', #10021, 1000.000000000000000 ) ;
#21529=ORIENTED_EDGE ( 'NONE', *, *, #45261, .T. ) ;
#21538=AXIS2_PLACEMENT_3D ( 'NONE', #62527, #56876, #3153 ) ;
#21550=EDGE_CURVE ( 'NONE', #23129, #39526, #31814, .T. ) ;
#21554=EDGE_LOOP ( 'NONE', ( #68452, #65383, #34067, #920 ) ) ;
#21586=ORIENTED_EDGE ( 'NONE', *, *, #3004, .F. ) ;
#21588=EDGE_CURVE ( 'NONE', #50155, #41366, #9186, .T. ) ;
#21598=ADVANCED_FACE ( 'NONE', ( #57968 ), #15196, .T. ) ;
#21600=CARTESIAN_POINT ( 'NONE',  ( 8.835729544836338434, -2.544523737882825820, 54.00000000000000711 ) ) ;
#21603=EDGE_LOOP ( 'NONE', ( #62576, #9582, #7709, #30427 ) ) ;
#21619=ORIENTED_EDGE ( 'NONE', *, *, #36019, .T. ) ;
#21621=ORIENTED_EDGE ( 'NONE', *, *, #19080, .F. ) ;
#21626=VERTEX_POINT ( 'NONE', #26158 ) ;
#21627=CARTESIAN_POINT ( 'NONE',  ( 6.665817930929297752, -7.357023737882824044, 54.00000000000000711 ) ) ;
#21628=CARTESIAN_POINT ( 'NONE',  ( -10.30047626211725742, 3.650476262117184234, 26.00000000000000711 ) ) ;
#21633=DIRECTION ( 'NONE',  ( 0.000000000000000000, 1.000000000000000000, 0.000000000000000000 ) ) ;
#21646=EDGE_CURVE ( 'NONE', #13697, #65251, #1023, .T. ) ;
#21657=ADVANCED_FACE ( 'NONE', ( #32148 ), #33181, .F. ) ;
#21658=FACE_OUTER_BOUND ( 'NONE', #51657, .T. ) ;
#21659=VERTEX_POINT ( 'NONE', #10576 ) ;
#21664=FACE_OUTER_BOUND ( 'NONE', #28800, .T. ) ;
#21672=VECTOR ( 'NONE', #69719, 1000.000000000000000 ) ;
#21681=VERTEX_POINT ( 'NONE', #37462 ) ;
#21684=LINE ( 'NONE', #22384, #63386 ) ;
#21687=CYLINDRICAL_SURFACE ( 'NONE', #52970, 0.1749999999999980738 ) ;
#21691=LINE ( 'NONE', #43936, #69614 ) ;
#21694=ADVANCED_FACE ( 'NONE', ( #26857 ), #27198, .T. ) ;
#21698=ORIENTED_EDGE ( 'NONE', *, *, #66476, .T. ) ;
#21721=DIRECTION ( 'NONE',  ( -1.836970198721029934E-16, 1.836970198721036590E-16, -1.000000000000000000 ) ) ;
#21726=DIRECTION ( 'NONE',  ( -0.000000000000000000, -0.000000000000000000, -1.000000000000000000 ) ) ;
#21732=LINE ( 'NONE', #65231, #40909 ) ;
#21752=ORIENTED_EDGE ( 'NONE', *, *, #50852, .F. ) ;
#21757=ORIENTED_EDGE ( 'NONE', *, *, #14556, .T. ) ;
#21758=DIRECTION ( 'NONE',  ( 0.6414496315691494699, 0.7671651518153064231, 0.000000000000000000 ) ) ;
#21774=EDGE_LOOP ( 'NONE', ( #10047, #34849, #48193, #56215 ) ) ;
#21781=EDGE_CURVE ( 'NONE', #65232, #9638, #58084, .T. ) ;
#21784=CARTESIAN_POINT ( 'NONE',  ( -7.342976262117293373, -6.665817930929262225, 54.00000000000000711 ) ) ;
#21787=DIRECTION ( 'NONE',  ( -0.000000000000000000, -0.000000000000000000, -1.000000000000000000 ) ) ;
#21790=LINE ( 'NONE', #54323, #16112 ) ;
#21791=AXIS2_PLACEMENT_3D ( 'NONE', #43128, #15921, #31846 ) ;
#21798=CARTESIAN_POINT ( 'NONE',  ( -6.486996718459908884, -3.157023737882779013, 26.00000000000000711 ) ) ;
#21805=CARTESIAN_POINT ( 'NONE',  ( -2.617976262117251540, 6.486996718459834277, 54.00000000000000711 ) ) ;
#21810=ORIENTED_EDGE ( 'NONE', *, *, #53413, .T. ) ;
#21818=DIRECTION ( 'NONE',  ( 0.7671651518152963201, -0.6414496315691619044, -2.356647714346269747E-16 ) ) ;
#21823=ORIENTED_EDGE ( 'NONE', *, *, #56146, .T. ) ;
#21827=VERTEX_POINT ( 'NONE', #12283 ) ;
#21830=ORIENTED_EDGE ( 'NONE', *, *, #5079, .T. ) ;
#21835=ORIENTED_EDGE ( 'NONE', *, *, #62952, .F. ) ;
#21837=CARTESIAN_POINT ( 'NONE',  ( 9.404523737882747980, 0.9414762621171599566, 26.00000000000000711 ) ) ;
#21840=VECTOR ( 'NONE', #7365, 1000.000000000000114 ) ;
#21846=VECTOR ( 'NONE', #45592, 1000.000000000000000 ) ;
#21850=ORIENTED_EDGE ( 'NONE', *, *, #8941, .T. ) ;
#21851=ORIENTED_EDGE ( 'NONE', *, *, #10600, .T. ) ;
#21852=VECTOR ( 'NONE', #44133, 1000.000000000000000 ) ;
#21856=CIRCLE ( 'NONE', #60211, 1.929199999999998916 ) ;
#21871=CARTESIAN_POINT ( 'NONE',  ( -9.897976262117243351, -3.682023737882718972, 26.00000000000000000 ) ) ;
#21873=DIRECTION ( 'NONE',  ( 0.7071067811865446862, -0.7071067811865503483, 0.000000000000000000 ) ) ;
#21878=LINE ( 'NONE', #43436, #22121 ) ;
#21892=PLANE ( 'NONE',  #54767 ) ;
#21898=VERTEX_POINT ( 'NONE', #45512 ) ;
#21901=LINE ( 'NONE', #26177, #15513 ) ;
#21906=EDGE_CURVE ( 'NONE', #33844, #63336, #29600, .T. ) ;
#21908=CARTESIAN_POINT ( 'NONE',  ( 7.532023737882783898, 3.834182069070696031, 54.00000000000000711 ) ) ;
#21918=ORIENTED_EDGE ( 'NONE', *, *, #58097, .F. ) ;
#21933=ORIENTED_EDGE ( 'NONE', *, *, #47067, .T. ) ;
#21940=ORIENTED_EDGE ( 'NONE', *, *, #54954, .T. ) ;
#21944=CARTESIAN_POINT ( 'NONE',  ( 3.857023737882783188, -9.912023737882810437, 54.00000000000000711 ) ) ;
#21945=EDGE_CURVE ( 'NONE', #16520, #4997, #3445, .T. ) ;
#21947=CARTESIAN_POINT ( 'NONE',  ( -3.842976262117332453, -10.31452373788281740, 54.00000000000000711 ) ) ;
#21953=ORIENTED_EDGE ( 'NONE', *, *, #64928, .F. ) ;
#21957=LINE ( 'NONE', #26574, #21672 ) ;
#21960=VERTEX_POINT ( 'NONE', #20748 ) ;
#21965=DIRECTION ( 'NONE',  ( -1.000000000000000000, 0.000000000000000000, 0.000000000000000000 ) ) ;
#21973=EDGE_CURVE ( 'NONE', #39038, #15670, #3789, .T. ) ;
#21974=ORIENTED_EDGE ( 'NONE', *, *, #34809, .T. ) ;
#21976=EDGE_CURVE ( 'NONE', #33844, #11146, #47623, .T. ) ;
#21979=EDGE_CURVE ( 'NONE', #14406, #12509, #57878, .T. ) ;
#21981=EDGE_CURVE ( 'NONE', #45407, #19689, #41260, .T. ) ;
#21983=CARTESIAN_POINT ( 'NONE',  ( 9.737023737882815055, -2.544523737882825820, 54.00000000000000711 ) ) ;
#21986=DIRECTION ( 'NONE',  ( 0.7071067811865451302, -0.7071067811865500152, -2.597868168706484048E-16 ) ) ;
#21999=PLANE ( 'NONE',  #64640 ) ;
#22000=VERTEX_POINT ( 'NONE', #25725 ) ;
#22001=VECTOR ( 'NONE', #16842, 1000.000000000000000 ) ;
#22016=AXIS2_PLACEMENT_3D ( 'NONE', #32524, #54087, #10586 ) ;
#22018=LINE ( 'NONE', #54206, #24362 ) ;
#22020=ORIENTED_EDGE ( 'NONE', *, *, #65253, .F. ) ;
#22022=CARTESIAN_POINT ( 'NONE',  ( 3.682023737882814007, 9.722976262117208890, 26.00000000000000711 ) ) ;
#22048=LINE ( 'NONE', #15707, #12199 ) ;
#22049=EDGE_CURVE ( 'NONE', #9283, #22404, #5197, .T. ) ;
#22052=AXIS2_PLACEMENT_3D ( 'NONE', #52229, #68141, #67791 ) ;
#22060=DIRECTION ( 'NONE',  ( 0.000000000000000000, 0.000000000000000000, 1.000000000000000000 ) ) ;
#22062=EDGE_CURVE ( 'NONE', #32555, #13545, #582, .T. ) ;
#22066=VECTOR ( 'NONE', #53153, 1000.000000000000000 ) ;
#22067=ORIENTED_EDGE ( 'NONE', *, *, #14208, .F. ) ;
#22069=CARTESIAN_POINT ( 'NONE',  ( -10.49297626211726175, 6.835476262117182955, 26.00000000000000711 ) ) ;
#22071=EDGE_CURVE ( 'NONE', #43831, #46841, #15464, .T. ) ;
#22077=VERTEX_POINT ( 'NONE', #59278 ) ;
#22082=DIRECTION ( 'NONE',  ( -0.000000000000000000, -0.000000000000000000, -1.000000000000000000 ) ) ;
#22088=ORIENTED_EDGE ( 'NONE', *, *, #33550, .T. ) ;
#22089=ORIENTED_EDGE ( 'NONE', *, *, #48320, .F. ) ;
#22103=VECTOR ( 'NONE', #22832, 1000.000000000000000 ) ;
#22108=CIRCLE ( 'NONE', #66153, 0.1749999999999998224 ) ;
#22111=DIRECTION ( 'NONE',  ( 1.000000000000000000, 0.000000000000000000, -0.000000000000000000 ) ) ;
#22114=VECTOR ( 'NONE', #208, 1000.000000000000000 ) ;
#22115=VECTOR ( 'NONE', #54007, 1000.000000000000000 ) ;
#22121=VECTOR ( 'NONE', #65026, 1000.000000000000000 ) ;
#22124=LINE ( 'NONE', #10119, #64116 ) ;
#22131=ADVANCED_FACE ( 'NONE', ( #4731 ), #52115, .T. ) ;
#22135=EDGE_CURVE ( 'NONE', #46851, #29966, #24255, .T. ) ;
#22143=LINE ( 'NONE', #39084, #11589 ) ;
#22144=CARTESIAN_POINT ( 'NONE',  ( -9.722976262117294155, -6.832023737882757963, 54.00000000000000711 ) ) ;
#22155=ORIENTED_EDGE ( 'NONE', *, *, #18123, .F. ) ;
#22157=CIRCLE ( 'NONE', #68489, 0.1750000000000002387 ) ;
#22160=DIRECTION ( 'NONE',  ( -0.000000000000000000, 3.673940397442059868E-16, -1.000000000000000000 ) ) ;
#22174=FACE_OUTER_BOUND ( 'NONE', #42890, .T. ) ;
#22181=ADVANCED_FACE ( 'NONE', ( #57414 ), #62712, .T. ) ;
#22183=CARTESIAN_POINT ( 'NONE',  ( -10.30047626211725742, 6.642976262117184838, 26.00000000000000711 ) ) ;
#22201=CIRCLE ( 'NONE', #34590, 0.1749999999999980738 ) ;
#22208=CARTESIAN_POINT ( 'NONE',  ( 2.420780051175169145, 8.697938382363084031, 54.00000000000000711 ) ) ;
#22209=DIRECTION ( 'NONE',  ( 1.836970198721029934E-16, 1.836970198721010706E-16, -1.000000000000000000 ) ) ;
#22210=ORIENTED_EDGE ( 'NONE', *, *, #51481, .T. ) ;
#22216=FACE_OUTER_BOUND ( 'NONE', #22380, .T. ) ;
#22219=EDGE_CURVE ( 'NONE', #7598, #67007, #53187, .T. ) ;
#22221=LINE ( 'NONE', #54741, #16606 ) ;
#22225=LINE ( 'NONE', #49775, #54811 ) ;
#22226=EDGE_LOOP ( 'NONE', ( #45518, #19433, #61473, #69757 ) ) ;
#22249=LINE ( 'NONE', #46016, #28007 ) ;
#22253=CIRCLE ( 'NONE', #31307, 0.7112000000000124889 ) ;
#22259=VERTEX_POINT ( 'NONE', #69074 ) ;
#22263=CARTESIAN_POINT ( 'NONE',  ( 5.257023737882819070, -7.186223737882822427, 54.00000000000000711 ) ) ;
#22264=FACE_OUTER_BOUND ( 'NONE', #10086, .T. ) ;
#22266=ORIENTED_EDGE ( 'NONE', *, *, #68882, .T. ) ;
#22268=EDGE_CURVE ( 'NONE', #58579, #27218, #63953, .T. ) ;
#22269=LINE ( 'NONE', #22604, #31217 ) ;
#22273=CARTESIAN_POINT ( 'NONE',  ( -2.406732575409589625, 8.697938382363036069, 54.00000000000000711 ) ) ;
#22277=LINE ( 'NONE', #69677, #41005 ) ;
#22283=AXIS2_PLACEMENT_3D ( 'NONE', #56203, #34621, #7749 ) ;
#22286=ORIENTED_EDGE ( 'NONE', *, *, #3176, .T. ) ;
#22289=VERTEX_POINT ( 'NONE', #38640 ) ;
#22295=DIRECTION ( 'NONE',  ( 0.8660254037844322683, -0.5000000000000111022, 6.723777587268230953E-17 ) ) ;
#22296=VECTOR ( 'NONE', #32494, 1000.000000000000000 ) ;
#22303=FACE_OUTER_BOUND ( 'NONE', #35654, .T. ) ;
#22310=FACE_OUTER_BOUND ( 'NONE', #42438, .T. ) ;
#22322=VECTOR ( 'NONE', #62371, 1000.000000000000000 ) ;
#22326=LINE ( 'NONE', #65109, #54623 ) ;
#22327=CARTESIAN_POINT ( 'NONE',  ( 2.369523737882815784, 8.821682069070730492, 54.00000000000000711 ) ) ;
#22344=DIRECTION ( 'NONE',  ( -1.920885163218982051E-15, -1.000000000000000000, 0.000000000000000000 ) ) ;
#22345=DIRECTION ( 'NONE',  ( -0.000000000000000000, 3.673940397442059868E-16, -1.000000000000000000 ) ) ;
#22347=ORIENTED_EDGE ( 'NONE', *, *, #53856, .F. ) ;
#22352=CARTESIAN_POINT ( 'NONE',  ( -4.141586236041129077, -4.720772854004773755, 54.00000000000000711 ) ) ;
#22362=ORIENTED_EDGE ( 'NONE', *, *, #59422, .T. ) ;
#22364=DIRECTION ( 'NONE',  ( -1.836970198721029934E-16, 1.836970198721036590E-16, -1.000000000000000000 ) ) ;
#22367=LINE ( 'NONE', #17049, #38729 ) ;
#22368=VERTEX_POINT ( 'NONE', #32645 ) ;
#22380=EDGE_LOOP ( 'NONE', ( #12090, #44486, #24389, #38914 ) ) ;
#22384=CARTESIAN_POINT ( 'NONE',  ( -10.03972626211722918, 8.916576262117214213, 54.00000000000000711 ) ) ;
#22387=CARTESIAN_POINT ( 'NONE',  ( -10.30047626211724321, -3.664523737882710464, 26.00000000000000000 ) ) ;
#22389=CARTESIAN_POINT ( 'NONE',  ( -8.598420958951683346, 1.991476262117183316, 54.00000000000000711 ) ) ;
#22394=PLANE ( 'NONE',  #62011 ) ;
#22397=CARTESIAN_POINT ( 'NONE',  ( -10.49297626211726175, 3.650476262117184234, 26.00000000000000711 ) ) ;
#22401=DIRECTION ( 'NONE',  ( 9.050731179009442381E-15, 1.000000000000000000, 3.673940397442060361E-16 ) ) ;
#22404=VERTEX_POINT ( 'NONE', #59858 ) ;
#22408=DIRECTION ( 'NONE',  ( -1.836970198721029934E-16, 1.836970198721036590E-16, -1.000000000000000000 ) ) ;
#22417=CARTESIAN_POINT ( 'NONE',  ( 3.682023737882786918, -9.737023737882799068, 26.00000000000000000 ) ) ;
#22421=FACE_OUTER_BOUND ( 'NONE', #25213, .T. ) ;
#22425=LINE ( 'NONE', #60232, #11407 ) ;
#22426=ORIENTED_EDGE ( 'NONE', *, *, #25510, .T. ) ;
#22435=VERTEX_POINT ( 'NONE', #32296 ) ;
#22440=EDGE_CURVE ( 'NONE', #34368, #51768, #40370, .T. ) ;
#22459=AXIS2_PLACEMENT_3D ( 'NONE', #13705, #23272, #44827 ) ;
#22460=FACE_OUTER_BOUND ( 'NONE', #45278, .T. ) ;
#22470=EDGE_CURVE ( 'NONE', #26653, #5963, #2882, .T. ) ;
#22471=CARTESIAN_POINT ( 'NONE',  ( -7.517976262117260333, 6.651770455163663165, 54.00000000000000711 ) ) ;
#22484=LINE ( 'NONE', #44025, #54034 ) ;
#22488=EDGE_CURVE ( 'NONE', #5502, #28088, #26702, .T. ) ;
#22496=LINE ( 'NONE', #53983, #26277 ) ;
#22502=CARTESIAN_POINT ( 'NONE',  ( -10.30047626211724321, -3.664523737882710464, 26.00000000000000000 ) ) ;
#22509=EDGE_LOOP ( 'NONE', ( #17872, #19911, #55853, #66538 ) ) ;
#22521=EDGE_CURVE ( 'NONE', #30867, #36429, #18431, .T. ) ;
#22535=DIRECTION ( 'NONE',  ( 0.7071067811865500152, 0.7071067811865451302, -4.429638872090642462E-31 ) ) ;
#22538=CARTESIAN_POINT ( 'NONE',  ( 8.711985858128693749, -2.420780051175170478, 26.00000000000000711 ) ) ;
#22539=LINE ( 'NONE', #33486, #32825 ) ;
#22540=VECTOR ( 'NONE', #52730, 1000.000000000000000 ) ;
#22541=ORIENTED_EDGE ( 'NONE', *, *, #63414, .F. ) ;
#22545=CARTESIAN_POINT ( 'NONE',  ( -0.9414762621173239365, -9.404523737882849233, 54.00000000000000711 ) ) ;
#22546=VERTEX_POINT ( 'NONE', #66197 ) ;
#22547=CIRCLE ( 'NONE', #28191, 1.224999999999998757 ) ;
#22561=FACE_OUTER_BOUND ( 'NONE', #54880, .T. ) ;
#22563=EDGE_CURVE ( 'NONE', #37419, #59900, #17761, .T. ) ;
#22565=VECTOR ( 'NONE', #26585, 1000.000000000000000 ) ;
#22568=CARTESIAN_POINT ( 'NONE',  ( 1.634292677759874746, 8.227189898828697778, 54.00000000000000711 ) ) ;
#22577=LINE ( 'NONE', #32835, #65031 ) ;
#22579=DIRECTION ( 'NONE',  ( 1.836970198721029934E-16, 1.836970198721010706E-16, -1.000000000000000000 ) ) ;
#22585=CARTESIAN_POINT ( 'NONE',  ( -6.350872789121327244, 6.822336235477381550, 54.00000000000000711 ) ) ;
#22586=ORIENTED_EDGE ( 'NONE', *, *, #47629, .F. ) ;
#22587=DIRECTION ( 'NONE',  ( -1.000000000000000000, 0.000000000000000000, 0.000000000000000000 ) ) ;
#22604=CARTESIAN_POINT ( 'NONE',  ( 2.420780051175148273, -8.711985858128677762, 54.00000000000000711 ) ) ;
#22612=ADVANCED_FACE ( 'NONE', ( #14746 ), #57870, .F. ) ;
#22627=CARTESIAN_POINT ( 'NONE',  ( -9.722976262117294155, -6.832023737882757963, 54.00000000000000711 ) ) ;
#22632=CARTESIAN_POINT ( 'NONE',  ( 9.737023737882816832, -3.682023737882817116, 26.00000000000000711 ) ) ;
#22637=CARTESIAN_POINT ( 'NONE',  ( -8.697938382363135545, 8.079219948824830411, 54.00000000000000711 ) ) ;
#22638=CYLINDRICAL_SURFACE ( 'NONE', #22790, 0.3499999999999996447 ) ;
#22639=CARTESIAN_POINT ( 'NONE',  ( 7.357023737882802727, 5.538810540049955655, 54.00000000000000711 ) ) ;
#22648=ORIENTED_EDGE ( 'NONE', *, *, #5216, .F. ) ;
#22649=FACE_OUTER_BOUND ( 'NONE', #14519, .T. ) ;
#22657=ORIENTED_EDGE ( 'NONE', *, *, #56336, .T. ) ;
#22665=CARTESIAN_POINT ( 'NONE',  ( 9.737023737882815055, -2.544523737882816050, 26.00000000000000711 ) ) ;
#22672=CIRCLE ( 'NONE', #19236, 0.1750000000000002387 ) ;
#22678=DIRECTION ( 'NONE',  ( -1.836970198721029934E-16, -1.836970198721010706E-16, 1.000000000000000000 ) ) ;
#22687=CARTESIAN_POINT ( 'NONE',  ( 10.50702373788281641, 9.781776262117171328, 54.00000000000000711 ) ) ;
#22693=LINE ( 'NONE', #38617, #8464 ) ;
#22696=CIRCLE ( 'NONE', #35088, 1.224999999999998757 ) ;
#22702=EDGE_LOOP ( 'NONE', ( #55266, #38754, #50459, #17416 ) ) ;
#22703=EDGE_CURVE ( 'NONE', #1953, #1721, #58587, .T. ) ;
#22704=ORIENTED_EDGE ( 'NONE', *, *, #47130, .F. ) ;
#22706=DIRECTION ( 'NONE',  ( -0.000000000000000000, -0.000000000000000000, -1.000000000000000000 ) ) ;
#22714=VERTEX_POINT ( 'NONE', #4839 ) ;
#22720=CARTESIAN_POINT ( 'NONE',  ( 7.408280051175172076, -6.789561617636949542, 54.00000000000000711 ) ) ;
#22723=CARTESIAN_POINT ( 'NONE',  ( 3.677663764522614454, -6.364920264886869461, 26.00000000000000711 ) ) ;
#22726=LINE ( 'NONE', #6124, #55212 ) ;
#22734=CARTESIAN_POINT ( 'NONE',  ( -3.710438382363119736, 7.394232575409525943, 54.00000000000000711 ) ) ;
#22735=ORIENTED_EDGE ( 'NONE', *, *, #51271, .T. ) ;
#22741=VECTOR ( 'NONE', #34701, 999.9999999999998863 ) ;
#22745=ORIENTED_EDGE ( 'NONE', *, *, #41744, .F. ) ;
#22748=EDGE_CURVE ( 'NONE', #32481, #38364, #31263, .T. ) ;
#22757=ORIENTED_EDGE ( 'NONE', *, *, #33950, .F. ) ;
#22762=DIRECTION ( 'NONE',  ( 1.836970198721029934E-16, 1.836970198721010706E-16, -1.000000000000000000 ) ) ;
#22764=VERTEX_POINT ( 'NONE', #26065 ) ;
#22765=AXIS2_PLACEMENT_3D ( 'NONE', #25177, #19858, #40386 ) ;
#22769=VERTEX_POINT ( 'NONE', #15791 ) ;
#22770=VERTEX_POINT ( 'NONE', #58928 ) ;
#22775=CARTESIAN_POINT ( 'NONE',  ( 0.000000000000000000, 0.000000000000000000, 0.000000000000000000 ) ) ;
#22790=AXIS2_PLACEMENT_3D ( 'NONE', #66107, #7399, #17676 ) ;
#22798=CARTESIAN_POINT ( 'NONE',  ( 10.31452373788280141, 6.835476262117187396, 26.00000000000000711 ) ) ;
#22799=ORIENTED_EDGE ( 'NONE', *, *, #19650, .F. ) ;
#22800=FACE_OUTER_BOUND ( 'NONE', #66533, .T. ) ;
#22803=CARTESIAN_POINT ( 'NONE',  ( 4.149127210878726935, -6.836383711242993044, 26.00000000000000000 ) ) ;
#22807=PLANE ( 'NONE',  #26960 ) ;
#22819=LINE ( 'NONE', #60650, #40713 ) ;
#22822=CARTESIAN_POINT ( 'NONE',  ( -9.897976262117257562, 3.667976262117184749, 54.00000000000000711 ) ) ;
#22826=CARTESIAN_POINT ( 'NONE',  ( 10.05377373788278739, -8.930623737882845248, 26.00000000000000000 ) ) ;
#22830=CARTESIAN_POINT ( 'NONE',  ( -7.447976262117260049, 9.880476262117177555, 54.00000000000000711 ) ) ;
#22832=DIRECTION ( 'NONE',  ( 0.000000000000000000, 1.000000000000000000, 3.673940397442059868E-16 ) ) ;
#22850=CARTESIAN_POINT ( 'NONE',  ( 3.664523737882778853, -10.50702373788281285, 54.00000000000000711 ) ) ;
#22852=VERTEX_POINT ( 'NONE', #12889 ) ;
#22853=CARTESIAN_POINT ( 'NONE',  ( -9.689726262117321909, -9.703773737882720241, 26.00000000000000000 ) ) ;
#22858=VECTOR ( 'NONE', #15734, 1000.000000000000000 ) ;
#22860=VERTEX_POINT ( 'NONE', #22826 ) ;
#22864=VECTOR ( 'NONE', #40901, 1000.000000000000000 ) ;
#22874=EDGE_CURVE ( 'NONE', #3520, #9024, #574, .T. ) ;
#22879=ORIENTED_EDGE ( 'NONE', *, *, #44053, .F. ) ;
#22880=CIRCLE ( 'NONE', #1426, 0.3499999999999996447 ) ;
#22889=VERTEX_POINT ( 'NONE', #43710 ) ;
#22894=LINE ( 'NONE', #6631, #9145 ) ;
#22903=LINE ( 'NONE', #22568, #28116 ) ;
#22911=EDGE_CURVE ( 'NONE', #42804, #34394, #60990, .T. ) ;
#22925=EDGE_LOOP ( 'NONE', ( #65437, #63480, #68683, #2575 ) ) ;
#22927=VECTOR ( 'NONE', #62745, 1000.000000000000114 ) ;
#22928=ADVANCED_FACE ( 'NONE', ( #66317 ), #17870, .F. ) ;
#22929=DIRECTION ( 'NONE',  ( -0.000000000000000000, -0.000000000000000000, -1.000000000000000000 ) ) ;
#22932=VECTOR ( 'NONE', #60522, 1000.000000000000000 ) ;
#22938=DIRECTION ( 'NONE',  ( -0.000000000000000000, -0.000000000000000000, -1.000000000000000000 ) ) ;
#22949=DIRECTION ( 'NONE',  ( -0.7671651518153074223, -0.6414496315691484707, -2.587583378555112027E-16 ) ) ;
#22951=EDGE_CURVE ( 'NONE', #12647, #26351, #23868, .T. ) ;
#22952=CARTESIAN_POINT ( 'NONE',  ( 9.703773737882812611, 10.03972626211715813, 26.00000000000000711 ) ) ;
#22958=CYLINDRICAL_SURFACE ( 'NONE', #14336, 1.929199999999998028 ) ;
#22963=DIRECTION ( 'NONE',  ( 1.000000000000000000, -3.491481338843133750E-15, -1.836970198721036590E-16 ) ) ;
#22967=ORIENTED_EDGE ( 'NONE', *, *, #14484, .F. ) ;
#22969=CARTESIAN_POINT ( 'NONE',  ( -4.947141984184534991, -7.357023737882802727, 26.00000000000000711 ) ) ;
#22970=VERTEX_POINT ( 'NONE', #34815 ) ;
#22978=CARTESIAN_POINT ( 'NONE',  ( -9.547976262117254365, 2.355476262117183417, 54.00000000000000711 ) ) ;
#22984=ADVANCED_FACE ( 'NONE', ( #45425 ), #24220, .F. ) ;
#22985=CARTESIAN_POINT ( 'NONE',  ( 7.969523737882813208, 9.722976262117192903, 26.00000000000000711 ) ) ;
#22990=ORIENTED_EDGE ( 'NONE', *, *, #21040, .T. ) ;
#22991=CARTESIAN_POINT ( 'NONE',  ( -0.9414762621172249046, 9.915476262117151052, 54.00000000000000711 ) ) ;
#22993=CARTESIAN_POINT ( 'NONE',  ( 9.912023737882799779, 6.817976262117189989, 26.00000000000000711 ) ) ;
#23008=EDGE_LOOP ( 'NONE', ( #46922, #17030, #45030, #33421 ) ) ;
#23009=VERTEX_POINT ( 'NONE', #56391 ) ;
#23018=ORIENTED_EDGE ( 'NONE', *, *, #42538, .T. ) ;
#23023=CARTESIAN_POINT ( 'NONE',  ( -4.031976262117261456, 3.142976262117183506, 26.00000000000000711 ) ) ;
#23024=DIRECTION ( 'NONE',  ( -0.000000000000000000, -0.000000000000000000, -1.000000000000000000 ) ) ;
#23025=DIRECTION ( 'NONE',  ( -1.836970198721029934E-16, 1.836970198721036590E-16, -1.000000000000000000 ) ) ;
#23029=ORIENTED_EDGE ( 'NONE', *, *, #32771, .F. ) ;
#23034=DIRECTION ( 'NONE',  ( -1.836970198721029934E-16, 1.836970198721036344E-16, -1.000000000000000000 ) ) ;
#23048=VECTOR ( 'NONE', #54068, 1000.000000000000114 ) ;
#23060=CARTESIAN_POINT ( 'NONE',  ( 6.832023737882818359, -9.737023737882811503, 26.00000000000000000 ) ) ;
#23065=LINE ( 'NONE', #8537, #34407 ) ;
#23091=CARTESIAN_POINT ( 'NONE',  ( -8.079219948824961861, -8.711985858128649340, 54.00000000000000711 ) ) ;
#23105=DIRECTION ( 'NONE',  ( 0.000000000000000000, -1.000000000000000000, 0.000000000000000000 ) ) ;
#23107=ORIENTED_EDGE ( 'NONE', *, *, #67048, .T. ) ;
#23121=CARTESIAN_POINT ( 'NONE',  ( 0.9555237378828163042, 9.390476262117214645, 54.00000000000000711 ) ) ;
#23129=VERTEX_POINT ( 'NONE', #4763 ) ;
#23136=AXIS2_PLACEMENT_3D ( 'NONE', #64175, #15723, #59550 ) ;
#23145=CARTESIAN_POINT ( 'NONE',  ( -10.30047626211728762, -6.657023737882746595, 26.00000000000000000 ) ) ;
#23147=VECTOR ( 'NONE', #9570, 1000.000000000000000 ) ;
#23149=DIRECTION ( 'NONE',  ( 9.912705577010336396E-15, 1.000000000000000000, 0.000000000000000000 ) ) ;
#23154=ORIENTED_EDGE ( 'NONE', *, *, #60185, .F. ) ;
#23155=VECTOR ( 'NONE', #31926, 1000.000000000000000 ) ;
#23156=CARTESIAN_POINT ( 'NONE',  ( -9.897976262117257562, 6.817976262117182884, 54.00000000000000711 ) ) ;
#23158=DIRECTION ( 'NONE',  ( -1.836970198721029934E-16, 1.836970198721036590E-16, -1.000000000000000000 ) ) ;
#23159=FACE_OUTER_BOUND ( 'NONE', #28972, .T. ) ;
#23160=ADVANCED_FACE ( 'NONE', ( #21366 ), #64171, .F. ) ;
#23166=EDGE_CURVE ( 'NONE', #5963, #34600, #68593, .T. ) ;
#23168=AXIS2_PLACEMENT_3D ( 'NONE', #56448, #29570, #57501 ) ;
#23185=DIRECTION ( 'NONE',  ( -0.000000000000000000, -0.000000000000000000, -1.000000000000000000 ) ) ;
#23187=CARTESIAN_POINT ( 'NONE',  ( -3.650476262117333892, -10.31452373788281740, 54.00000000000000711 ) ) ;
#23188=CIRCLE ( 'NONE', #20982, 0.5249999999999994671 ) ;
#23194=CARTESIAN_POINT ( 'NONE',  ( -6.775514141871385121, 7.394232575409538377, 54.00000000000000711 ) ) ;
#23215=DIRECTION ( 'NONE',  ( -0.000000000000000000, 3.673940397442059868E-16, -1.000000000000000000 ) ) ;
#23225=DIRECTION ( 'NONE',  ( 0.7071067811865451302, -0.7071067811865500152, 0.000000000000000000 ) ) ;
#23245=VECTOR ( 'NONE', #47267, 1000.000000000000000 ) ;
#23251=VECTOR ( 'NONE', #23025, 1000.000000000000000 ) ;
#23255=CARTESIAN_POINT ( 'NONE',  ( 8.930623737882818602, -8.580623737882845603, 26.00000000000000000 ) ) ;
#23270=DIRECTION ( 'NONE',  ( 1.000000000000000000, 0.000000000000000000, 0.000000000000000000 ) ) ;
#23272=DIRECTION ( 'NONE',  ( -5.120954910632640039E-15, -1.000000000000000000, -3.673940397442059868E-16 ) ) ;
#23273=EDGE_CURVE ( 'NONE', #16440, #69650, #13204, .T. ) ;
#23275=DIRECTION ( 'NONE',  ( -1.000000000000000000, 0.000000000000000000, 0.000000000000000000 ) ) ;
#23280=ORIENTED_EDGE ( 'NONE', *, *, #54940, .T. ) ;
#23285=PLANE ( 'NONE',  #53827 ) ;
#23290=ORIENTED_EDGE ( 'NONE', *, *, #30535, .F. ) ;
#23299=VECTOR ( 'NONE', #61567, 1000.000000000000000 ) ;
#23303=EDGE_LOOP ( 'NONE', ( #40856, #39900, #67194, #49579 ) ) ;
#23313=FACE_OUTER_BOUND ( 'NONE', #49288, .T. ) ;
#23325=EDGE_CURVE ( 'NONE', #23844, #58579, #59883, .T. ) ;
#23328=DIRECTION ( 'NONE',  ( -1.000000000000000000, 3.491481338843133355E-15, 1.836970198721036344E-16 ) ) ;
#23331=PLANE ( 'NONE',  #17021 ) ;
#23333=ORIENTED_EDGE ( 'NONE', *, *, #63786, .F. ) ;
#23335=CARTESIAN_POINT ( 'NONE',  ( -5.242976262117280406, -5.257023737882805747, 54.00000000000000711 ) ) ;
#23349=CARTESIAN_POINT ( 'NONE',  ( -2.530476262117325792, -9.562023737882828556, 54.00000000000000711 ) ) ;
#23353=ADVANCED_FACE ( 'NONE', ( #6819 ), #61247, .F. ) ;
#23363=DIRECTION ( 'NONE',  ( -0.000000000000000000, -0.000000000000000000, -1.000000000000000000 ) ) ;
#23365=VECTOR ( 'NONE', #57909, 1000.000000000000000 ) ;
#23369=ORIENTED_EDGE ( 'NONE', *, *, #36262, .T. ) ;
#23375=DIRECTION ( 'NONE',  ( -1.034072152899300747E-14, -1.000000000000000000, 0.000000000000000000 ) ) ;
#23378=FACE_OUTER_BOUND ( 'NONE', #18024, .T. ) ;
#23381=EDGE_LOOP ( 'NONE', ( #67770, #10098, #47600, #17787 ) ) ;
#23389=CARTESIAN_POINT ( 'NONE',  ( 10.31452373788278187, 3.842976262117144159, 54.00000000000000711 ) ) ;
#23393=EDGE_CURVE ( 'NONE', #36809, #39691, #3627, .T. ) ;
#23407=VERTEX_POINT ( 'NONE', #29432 ) ;
#23410=VECTOR ( 'NONE', #20671, 1000.000000000000000 ) ;
#23420=DIRECTION ( 'NONE',  ( -1.000000000000000000, 0.000000000000000000, 0.000000000000000000 ) ) ;
#23429=DIRECTION ( 'NONE',  ( -1.047444401652940007E-14, -1.000000000000000000, 0.000000000000000000 ) ) ;
#23430=DIRECTION ( 'NONE',  ( 0.000000000000000000, 1.000000000000000000, 0.000000000000000000 ) ) ;
#23433=ORIENTED_EDGE ( 'NONE', *, *, #55599, .F. ) ;
#23434=ORIENTED_EDGE ( 'NONE', *, *, #47854, .F. ) ;
#23448=FACE_OUTER_BOUND ( 'NONE', #51614, .T. ) ;
#23450=LINE ( 'NONE', #29436, #36593 ) ;
#23461=AXIS2_PLACEMENT_3D ( 'NONE', #9162, #18347, #40629 ) ;
#23468=ORIENTED_EDGE ( 'NONE', *, *, #40324, .T. ) ;
#23473=EDGE_CURVE ( 'NONE', #42663, #47684, #18831, .T. ) ;
#23483=ORIENTED_EDGE ( 'NONE', *, *, #38452, .F. ) ;
#23487=CARTESIAN_POINT ( 'NONE',  ( 7.186223737882800222, 5.242976262117193365, 54.00000000000000711 ) ) ;
#23503=FACE_OUTER_BOUND ( 'NONE', #51824, .T. ) ;
#23505=ORIENTED_EDGE ( 'NONE', *, *, #21550, .F. ) ;
#23511=CYLINDRICAL_SURFACE ( 'NONE', #49751, 0.3499999999999996447 ) ;
#23513=DIRECTION ( 'NONE',  ( -1.836970198721029934E-16, 1.836970198721036344E-16, -1.000000000000000000 ) ) ;
#23520=ADVANCED_FACE ( 'NONE', ( #5023 ), #69022, .F. ) ;
#23521=EDGE_CURVE ( 'NONE', #17119, #56196, #25190, .T. ) ;
#23529=DIRECTION ( 'NONE',  ( 1.836970198721029934E-16, 1.836970198721010706E-16, -1.000000000000000000 ) ) ;
#23549=EDGE_LOOP ( 'NONE', ( #5935, #63999, #22967, #54912 ) ) ;
#23557=DIRECTION ( 'NONE',  ( 0.000000000000000000, -3.673940397442059868E-16, 1.000000000000000000 ) ) ;
#23564=EDGE_CURVE ( 'NONE', #12532, #49486, #63022, .T. ) ;
#23575=ORIENTED_EDGE ( 'NONE', *, *, #15900, .F. ) ;
#23577=DIRECTION ( 'NONE',  ( -1.836970198721029934E-16, 1.836970198721036590E-16, -1.000000000000000000 ) ) ;
#23581=CARTESIAN_POINT ( 'NONE',  ( 10.31452373788281562, -6.657023737882825642, 54.00000000000000711 ) ) ;
#23591=ORIENTED_EDGE ( 'NONE', *, *, #2716, .T. ) ;
#23592=CARTESIAN_POINT ( 'NONE',  ( -3.842976262117221875, 10.30047626211716860, 54.00000000000000711 ) ) ;
#23597=EDGE_CURVE ( 'NONE', #19158, #57625, #880, .T. ) ;
#23599=CARTESIAN_POINT ( 'NONE',  ( 8.835729544836290472, 2.530476262117160591, 54.00000000000000711 ) ) ;
#23604=VECTOR ( 'NONE', #39477, 1000.000000000000000 ) ;
#23605=DIRECTION ( 'NONE',  ( 0.8660254037844375974, -0.5000000000000019984, 0.000000000000000000 ) ) ;
#23607=CARTESIAN_POINT ( 'NONE',  ( -8.566576262117260754, 8.916576262117214213, 54.00000000000000711 ) ) ;
#23608=ORIENTED_EDGE ( 'NONE', *, *, #23632, .T. ) ;
#23610=VECTOR ( 'NONE', #63704, 1000.000000000000000 ) ;
#23613=EDGE_CURVE ( 'NONE', #21626, #23904, #14429, .T. ) ;
#23616=ORIENTED_EDGE ( 'NONE', *, *, #49909, .F. ) ;
#23621=CARTESIAN_POINT ( 'NONE',  ( -4.947141984184481700, 7.342976262117180575, 54.00000000000000711 ) ) ;
#23625=DIRECTION ( 'NONE',  ( -9.912705577010336396E-15, -1.000000000000000000, 0.000000000000000000 ) ) ;
#23632=EDGE_CURVE ( 'NONE', #9398, #17833, #10329, .T. ) ;
#23643=ORIENTED_EDGE ( 'NONE', *, *, #18453, .F. ) ;
#23647=ADVANCED_FACE ( 'NONE', ( #36137 ), #41451, .T. ) ;
#23648=EDGE_LOOP ( 'NONE', ( #42782, #45549, #38823, #40625 ) ) ;
#23649=AXIS2_PLACEMENT_3D ( 'NONE', #52493, #58141, #4060 ) ;
#23651=DIRECTION ( 'NONE',  ( 1.047444401652940007E-14, 1.000000000000000000, 1.836970198721029934E-16 ) ) ;
#23664=DIRECTION ( 'NONE',  ( 1.000000000000000000, 1.671920889371702854E-15, 6.142537696789956391E-31 ) ) ;
#23667=CARTESIAN_POINT ( 'NONE',  ( -6.858227778582867806, 2.989207322240119868, 26.00000000000000711 ) ) ;
#23673=ORIENTED_EDGE ( 'NONE', *, *, #23793, .T. ) ;
#23677=CARTESIAN_POINT ( 'NONE',  ( 5.257023737882795977, 5.242976262117205799, 26.00000000000000711 ) ) ;
#23681=EDGE_LOOP ( 'NONE', ( #29974, #60530, #51585, #27150 ) ) ;
#23683=LINE ( 'NONE', #12026, #24418 ) ;
#23689=AXIS2_PLACEMENT_3D ( 'NONE', #43738, #10861, #54352 ) ;
#23694=DIRECTION ( 'NONE',  ( 0.000000000000000000, -1.000000000000000000, -3.673940397442060361E-16 ) ) ;
#23699=LINE ( 'NONE', #61888, #37003 ) ;
#23705=CARTESIAN_POINT ( 'NONE',  ( -10.49297626211726175, 3.650476262117184234, 54.00000000000000711 ) ) ;
#23713=LINE ( 'NONE', #18394, #14022 ) ;
#23718=VECTOR ( 'NONE', #10041, 1000.000000000000000 ) ;
#23724=ORIENTED_EDGE ( 'NONE', *, *, #56609, .T. ) ;
#23733=VECTOR ( 'NONE', #34939, 1000.000000000000000 ) ;
#23744=FACE_OUTER_BOUND ( 'NONE', #4866, .T. ) ;
#23755=CYLINDRICAL_SURFACE ( 'NONE', #26523, 0.5249999999999994671 ) ;
#23766=LINE ( 'NONE', #34352, #20913 ) ;
#23767=ORIENTED_EDGE ( 'NONE', *, *, #43236, .F. ) ;
#23780=DIRECTION ( 'NONE',  ( -1.000000000000000000, 9.799566706031580591E-15, 1.836970198721048176E-16 ) ) ;
#23793=EDGE_CURVE ( 'NONE', #2123, #37879, #23699, .T. ) ;
#23798=ORIENTED_EDGE ( 'NONE', *, *, #69036, .T. ) ;
#23803=FACE_OUTER_BOUND ( 'NONE', #61611, .T. ) ;
#23808=ORIENTED_EDGE ( 'NONE', *, *, #1585, .T. ) ;
#23812=CIRCLE ( 'NONE', #63347, 0.3499999999999996447 ) ;
#23820=ORIENTED_EDGE ( 'NONE', *, *, #47823, .F. ) ;
#23821=ORIENTED_EDGE ( 'NONE', *, *, #45202, .F. ) ;
#23823=CARTESIAN_POINT ( 'NONE',  ( -8.821682069070741150, -2.369523737882737624, 26.00000000000000711 ) ) ;
#23826=ORIENTED_EDGE ( 'NONE', *, *, #56325, .F. ) ;
#23836=ADVANCED_FACE ( 'NONE', ( #50918 ), #24755, .F. ) ;
#23839=ORIENTED_EDGE ( 'NONE', *, *, #68346, .T. ) ;
#23841=LINE ( 'NONE', #50365, #18709 ) ;
#23844=VERTEX_POINT ( 'NONE', #45259 ) ;
#23845=DIRECTION ( 'NONE',  ( -1.000000000000000000, 0.000000000000000000, 0.000000000000000000 ) ) ;
#23846=CARTESIAN_POINT ( 'NONE',  ( -2.406732575409590069, 8.697938382363036069, 54.00000000000000711 ) ) ;
#23847=AXIS2_PLACEMENT_3D ( 'NONE', #40710, #3236, #9592 ) ;
#23851=LINE ( 'NONE', #67349, #40315 ) ;
#23853=CARTESIAN_POINT ( 'NONE',  ( -10.30047626211729295, -6.657023737882751924, 54.00000000000000711 ) ) ;
#23854=AXIS2_PLACEMENT_3D ( 'NONE', #57011, #30496, #41458 ) ;
#23856=VERTEX_POINT ( 'NONE', #18745 ) ;
#23860=LINE ( 'NONE', #66992, #35656 ) ;
#23862=ORIENTED_EDGE ( 'NONE', *, *, #10662, .F. ) ;
#23865=CARTESIAN_POINT ( 'NONE',  ( 5.552858015815581361, -7.357023737882824044, 54.00000000000000711 ) ) ;
#23868=LINE ( 'NONE', #2644, #24474 ) ;
#23871=CARTESIAN_POINT ( 'NONE',  ( -4.141586236041130853, -5.793274621760842180, 54.00000000000000711 ) ) ;
#23882=VERTEX_POINT ( 'NONE', #40664 ) ;
#23889=ORIENTED_EDGE ( 'NONE', *, *, #64928, .T. ) ;
#23892=EDGE_LOOP ( 'NONE', ( #54362, #62473, #26022, #3665 ) ) ;
#23899=ORIENTED_EDGE ( 'NONE', *, *, #35563, .F. ) ;
#23900=ORIENTED_EDGE ( 'NONE', *, *, #53075, .T. ) ;
#23903=EDGE_LOOP ( 'NONE', ( #14517, #20758, #28851, #26795 ) ) ;
#23904=VERTEX_POINT ( 'NONE', #56916 ) ;
#23908=DIRECTION ( 'NONE',  ( 0.000000000000000000, -1.000000000000000000, 0.000000000000000000 ) ) ;
#23910=ORIENTED_EDGE ( 'NONE', *, *, #29502, .T. ) ;
#23915=VERTEX_POINT ( 'NONE', #41006 ) ;
#23918=EDGE_CURVE ( 'NONE', #6834, #902, #63648, .T. ) ;
#23923=LINE ( 'NONE', #9773, #12331 ) ;
#23927=CARTESIAN_POINT ( 'NONE',  ( 6.657023737882818537, -9.912023737882810437, 26.00000000000000000 ) ) ;
#23928=ORIENTED_EDGE ( 'NONE', *, *, #56112, .F. ) ;
#23931=CARTESIAN_POINT ( 'NONE',  ( -8.079219948824906794, 8.697938382363059162, 54.00000000000000711 ) ) ;
#23934=DIRECTION ( 'NONE',  ( 5.163402228214836012E-15, 1.000000000000000000, 0.000000000000000000 ) ) ;
#23935=ORIENTED_EDGE ( 'NONE', *, *, #63377, .T. ) ;
#23937=CARTESIAN_POINT ( 'NONE',  ( -2.989207322240185594, 6.858227778582772771, 54.00000000000000711 ) ) ;
#23938=VECTOR ( 'NONE', #50462, 1000.000000000000000 ) ;
#23945=ORIENTED_EDGE ( 'NONE', *, *, #18268, .T. ) ;
#23957=DIRECTION ( 'NONE',  ( 0.5000000000000019984, 0.8660254037844375974, 0.000000000000000000 ) ) ;
#23970=DIRECTION ( 'NONE',  ( -1.073876437509453175E-14, -1.000000000000000000, 0.000000000000000000 ) ) ;
#23974=CARTESIAN_POINT ( 'NONE',  ( -3.663616288757055806, 6.350872789121238426, 54.00000000000000711 ) ) ;
#23977=ORIENTED_EDGE ( 'NONE', *, *, #54771, .T. ) ;
#23979=CARTESIAN_POINT ( 'NONE',  ( 3.848229544836324845, 7.342976262117209885, 26.00000000000000711 ) ) ;
#23990=LINE ( 'NONE', #9142, #14712 ) ;
#24011=FACE_OUTER_BOUND ( 'NONE', #44766, .T. ) ;
#24013=FACE_OUTER_BOUND ( 'NONE', #43446, .T. ) ;
#24026=AXIS2_PLACEMENT_3D ( 'NONE', #44961, #49248, #44599 ) ;
#24036=CARTESIAN_POINT ( 'NONE',  ( 9.929523737882817613, -0.9555237378828257411, 54.00000000000000711 ) ) ;
#24043=EDGE_CURVE ( 'NONE', #1385, #44762, #52695, .T. ) ;
#24046=CARTESIAN_POINT ( 'NONE',  ( -5.242976262117280406, -5.257023737882805747, 54.00000000000000711 ) ) ;
#24053=ADVANCED_FACE ( 'NONE', ( #41715 ), #37128, .F. ) ;
#24065=DIRECTION ( 'NONE',  ( 1.836970198721029934E-16, 1.836970198721010706E-16, -1.000000000000000000 ) ) ;
#24068=VECTOR ( 'NONE', #20056, 1000.000000000000000 ) ;
#24072=ORIENTED_EDGE ( 'NONE', *, *, #63778, .T. ) ;
#24073=ORIENTED_EDGE ( 'NONE', *, *, #44000, .T. ) ;
#24090=ORIENTED_EDGE ( 'NONE', *, *, #58903, .F. ) ;
#24094=ORIENTED_EDGE ( 'NONE', *, *, #38423, .T. ) ;
#24101=DIRECTION ( 'NONE',  ( -1.000000000000000000, 0.000000000000000000, 0.000000000000000000 ) ) ;
#24103=PLANE ( 'NONE',  #33762 ) ;
#24105=DIRECTION ( 'NONE',  ( 0.000000000000000000, 1.000000000000000000, 0.000000000000000000 ) ) ;
#24126=VECTOR ( 'NONE', #58786, 1000.000000000000000 ) ;
#24139=LINE ( 'NONE', #34371, #25161 ) ;
#24145=EDGE_CURVE ( 'NONE', #8910, #20164, #12186, .T. ) ;
#24149=EDGE_CURVE ( 'NONE', #61865, #17044, #22249, .T. ) ;
#24150=ORIENTED_EDGE ( 'NONE', *, *, #4209, .F. ) ;
#24153=DIRECTION ( 'NONE',  ( -1.000000000000000000, 0.000000000000000000, 0.000000000000000000 ) ) ;
#24156=CARTESIAN_POINT ( 'NONE',  ( -3.663616288757090000, -6.364920264886882784, 26.00000000000000711 ) ) ;
#24164=( NAMED_UNIT ( * ) PLANE_ANGLE_UNIT ( ) SI_UNIT ( $, .RADIAN. ) );
#24172=ORIENTED_EDGE ( 'NONE', *, *, #38873, .F. ) ;
#24174=VERTEX_POINT ( 'NONE', #16937 ) ;
#24175=FACE_OUTER_BOUND ( 'NONE', #1142, .T. ) ;
#24176=ORIENTED_EDGE ( 'NONE', *, *, #47102, .T. ) ;
#24188=ADVANCED_FACE ( 'NONE', ( #65719 ), #27895, .F. ) ;
#24200=DIRECTION ( 'NONE',  ( -0.5000000000000019984, -0.8660254037844375974, 0.000000000000000000 ) ) ;
#24210=ORIENTED_EDGE ( 'NONE', *, *, #31252, .F. ) ;
#24211=CARTESIAN_POINT ( 'NONE',  ( -10.03972626211731978, -8.930623737882752877, 54.00000000000000711 ) ) ;
#24216=EDGE_LOOP ( 'NONE', ( #62255, #63696, #68889, #24930 ) ) ;
#24218=PLANE ( 'NONE',  #58024 ) ;
#24220=PLANE ( 'NONE',  #36909 ) ;
#24225=AXIS2_PLACEMENT_3D ( 'NONE', #12789, #13153, #17079 ) ;
#24232=ADVANCED_FACE ( 'NONE', ( #51184 ), #55460, .F. ) ;
#24237=LINE ( 'NONE', #12905, #54212 ) ;
#24244=ORIENTED_EDGE ( 'NONE', *, *, #4736, .T. ) ;
#24251=ORIENTED_EDGE ( 'NONE', *, *, #28901, .T. ) ;
#24253=LINE ( 'NONE', #45817, #51950 ) ;
#24254=ORIENTED_EDGE ( 'NONE', *, *, #28901, .F. ) ;
#24255=CIRCLE ( 'NONE', #20881, 0.3499999999999996447 ) ;
#24260=VERTEX_POINT ( 'NONE', #66049 ) ;
#24261=EDGE_CURVE ( 'NONE', #22368, #62934, #35252, .T. ) ;
#24269=VECTOR ( 'NONE', #59382, 1000.000000000000000 ) ;
#24276=EDGE_CURVE ( 'NONE', #13431, #41511, #19013, .T. ) ;
#24278=CIRCLE ( 'NONE', #43517, 0.7112000000000124889 ) ;
#24285=LINE ( 'NONE', #56113, #11759 ) ;
#24311=ADVANCED_FACE ( 'NONE', ( #62135 ), #28919, .F. ) ;
#24318=ORIENTED_EDGE ( 'NONE', *, *, #47606, .T. ) ;
#24324=VECTOR ( 'NONE', #56092, 1000.000000000000000 ) ;
#24327=VERTEX_POINT ( 'NONE', #36323 ) ;
#24342=ORIENTED_EDGE ( 'NONE', *, *, #50059, .F. ) ;
#24348=LINE ( 'NONE', #30711, #23733 ) ;
#24356=PLANE ( 'NONE',  #36926 ) ;
#24362=VECTOR ( 'NONE', #11063, 1000.000000000000000 ) ;
#24363=EDGE_CURVE ( 'NONE', #30244, #26273, #25734, .T. ) ;
#24365=DIRECTION ( 'NONE',  ( -1.000000000000000000, 3.016910393003147986E-15, 0.000000000000000000 ) ) ;
#24375=CARTESIAN_POINT ( 'NONE',  ( 9.737023737882781305, 3.667976262117152775, 54.00000000000000711 ) ) ;
#24377=CIRCLE ( 'NONE', #27817, 0.1749999999999993783 ) ;
#24382=LINE ( 'NONE', #49860, #42418 ) ;
#24389=ORIENTED_EDGE ( 'NONE', *, *, #54856, .F. ) ;
#24390=ORIENTED_EDGE ( 'NONE', *, *, #58468, .T. ) ;
#24391=DIRECTION ( 'NONE',  ( 1.836970198721029934E-16, 1.836970198721010706E-16, -1.000000000000000000 ) ) ;
#24392=CARTESIAN_POINT ( 'NONE',  ( -3.650476262117331228, -10.50702373788281641, 26.00000000000000000 ) ) ;
#24394=PLANE ( 'NONE',  #27853 ) ;
#24396=CARTESIAN_POINT ( 'NONE',  ( -9.722976262117258628, 6.817976262117182884, 54.00000000000000711 ) ) ;
#24401=VECTOR ( 'NONE', #69087, 999.9999999999998863 ) ;
#24410=VECTOR ( 'NONE', #17099, 1000.000000000000000 ) ;
#24418=VECTOR ( 'NONE', #66477, 1000.000000000000000 ) ;
#24419=VECTOR ( 'NONE', #12328, 1000.000000000000000 ) ;
#24429=FACE_OUTER_BOUND ( 'NONE', #26976, .T. ) ;
#24443=CARTESIAN_POINT ( 'NONE',  ( -7.342976262117259623, 6.651770455163663165, 26.00000000000000711 ) ) ;
#24448=EDGE_LOOP ( 'NONE', ( #42353, #23505, #6748, #56352 ) ) ;
#24472=DIRECTION ( 'NONE',  ( -1.813998472013049822E-14, -1.000000000000000000, -1.836970198721044232E-16 ) ) ;
#24474=VECTOR ( 'NONE', #25271, 1000.000000000000000 ) ;
#24475=AXIS2_PLACEMENT_3D ( 'NONE', #14408, #46561, #63185 ) ;
#24481=CIRCLE ( 'NONE', #64026, 1.224999999999998757 ) ;
#24488=CARTESIAN_POINT ( 'NONE',  ( 5.552858015815581361, -7.357023737882824044, 54.00000000000000711 ) ) ;
#24499=CARTESIAN_POINT ( 'NONE',  ( -7.394232575409614761, 6.775514141871308738, 26.00000000000000711 ) ) ;
#24500=ORIENTED_EDGE ( 'NONE', *, *, #9207, .T. ) ;
#24502=CARTESIAN_POINT ( 'NONE',  ( -8.079219948824906794, 8.697938382363059162, 54.00000000000000711 ) ) ;
#24503=ORIENTED_EDGE ( 'NONE', *, *, #69179, .T. ) ;
#24509=VECTOR ( 'NONE', #58753, 1000.000000000000000 ) ;
#24510=FACE_OUTER_BOUND ( 'NONE', #11128, .T. ) ;
#24515=VERTEX_POINT ( 'NONE', #16157 ) ;
#24522=AXIS2_PLACEMENT_3D ( 'NONE', #34370, #35791, #13172 ) ;
#24523=VECTOR ( 'NONE', #52915, 1000.000000000000000 ) ;
#24536=EDGE_CURVE ( 'NONE', #50773, #64510, #61260, .T. ) ;
#24538=EDGE_LOOP ( 'NONE', ( #20406, #53735, #35548, #10441 ) ) ;
#24548=EDGE_LOOP ( 'NONE', ( #29238, #38820, #46734, #49925 ) ) ;
#24550=CARTESIAN_POINT ( 'NONE',  ( 9.795823737882807691, 10.49297626211718537, 54.00000000000000711 ) ) ;
#24553=ADVANCED_FACE ( 'NONE', ( #32432 ), #60923, .F. ) ;
#24557=LINE ( 'NONE', #25257, #51321 ) ;
#24564=LINE ( 'NONE', #13944, #13314 ) ;
#24569=LINE ( 'NONE', #57434, #30159 ) ;
#24585=EDGE_CURVE ( 'NONE', #35090, #5797, #51777, .T. ) ;
#24590=ORIENTED_EDGE ( 'NONE', *, *, #56112, .T. ) ;
#24592=AXIS2_PLACEMENT_3D ( 'NONE', #3082, #55429, #56803 ) ;
#24600=ORIENTED_EDGE ( 'NONE', *, *, #36262, .F. ) ;
#24601=ORIENTED_EDGE ( 'NONE', *, *, #29347, .T. ) ;
#24623=EDGE_LOOP ( 'NONE', ( #52628, #53251, #56658, #66634 ) ) ;
#24626=CARTESIAN_POINT ( 'NONE',  ( 8.930623737882848800, 10.03972626211715635, 54.00000000000000711 ) ) ;
#24628=ORIENTED_EDGE ( 'NONE', *, *, #18273, .F. ) ;
#24630=AXIS2_PLACEMENT_3D ( 'NONE', #51231, #2787, #24365 ) ;
#24631=CARTESIAN_POINT ( 'NONE',  ( 9.737023737882816832, -3.682023737882826886, 54.00000000000000711 ) ) ;
#24632=DIRECTION ( 'NONE',  ( -1.836970198721029934E-16, 1.836970198721036344E-16, -1.000000000000000000 ) ) ;
#24637=DIRECTION ( 'NONE',  ( 1.836970198721029934E-16, 1.836970198721010706E-16, -1.000000000000000000 ) ) ;
#24638=CARTESIAN_POINT ( 'NONE',  ( -1.991476262117310325, -8.612468434717257537, 26.00000000000000711 ) ) ;
#24640=ORIENTED_EDGE ( 'NONE', *, *, #37321, .F. ) ;
#24642=LINE ( 'NONE', #2703, #60311 ) ;
#24648=CARTESIAN_POINT ( 'NONE',  ( -9.547976262117304103, -7.969523737882760805, 54.00000000000000711 ) ) ;
#24651=FACE_OUTER_BOUND ( 'NONE', #34261, .T. ) ;
#24656=DIRECTION ( 'NONE',  ( -1.819560449471430698E-15, -1.000000000000000000, 0.000000000000000000 ) ) ;
#24664=VERTEX_POINT ( 'NONE', #8580 ) ;
#24667=DIRECTION ( 'NONE',  ( 3.596772705736698833E-15, 1.000000000000000000, 0.000000000000000000 ) ) ;
#24668=ORIENTED_EDGE ( 'NONE', *, *, #7597, .T. ) ;
#24670=LINE ( 'NONE', #39860, #45799 ) ;
#24675=EDGE_CURVE ( 'NONE', #51724, #41366, #35093, .T. ) ;
#24689=CARTESIAN_POINT ( 'NONE',  ( 8.930623737882818602, -8.930623737882845248, 26.00000000000000000 ) ) ;
#24691=CARTESIAN_POINT ( 'NONE',  ( -8.079219948824956532, -8.711985858128644011, 26.00000000000000000 ) ) ;
#24699=CARTESIAN_POINT ( 'NONE',  ( 7.969523737882809655, 8.821682069070714505, 26.00000000000000711 ) ) ;
#24704=ORIENTED_EDGE ( 'NONE', *, *, #27187, .F. ) ;
#24711=EDGE_CURVE ( 'NONE', #54124, #16704, #50668, .T. ) ;
#24716=CYLINDRICAL_SURFACE ( 'NONE', #21306, 0.1750000000000002387 ) ;
#24726=LINE ( 'NONE', #9165, #59919 ) ;
#24727=AXIS2_PLACEMENT_3D ( 'NONE', #25455, #2828, #57626 ) ;
#24730=DIRECTION ( 'NONE',  ( -1.671920889371702854E-15, -1.000000000000000000, -3.673940397442059868E-16 ) ) ;
#24736=ORIENTED_EDGE ( 'NONE', *, *, #2679, .F. ) ;
#24746=DIRECTION ( 'NONE',  ( -1.836970198721029934E-16, 1.836970198721036590E-16, -1.000000000000000000 ) ) ;
#24748=EDGE_CURVE ( 'NONE', #64891, #63857, #29106, .T. ) ;
#24753=ORIENTED_EDGE ( 'NONE', *, *, #20781, .F. ) ;
#24755=CYLINDRICAL_SURFACE ( 'NONE', #59605, 1.224999999999998757 ) ;
#24757=ADVANCED_FACE ( 'NONE', ( #19895 ), #41465, .F. ) ;
#24792=DIRECTION ( 'NONE',  ( -1.000000000000000000, 0.000000000000000000, 0.000000000000000000 ) ) ;
#24795=VERTEX_POINT ( 'NONE', #15996 ) ;
#24808=FACE_OUTER_BOUND ( 'NONE', #22226, .T. ) ;
#24815=ORIENTED_EDGE ( 'NONE', *, *, #63353, .T. ) ;
#24816=CARTESIAN_POINT ( 'NONE',  ( -10.49297626211726175, 3.650476262117184234, 26.00000000000000711 ) ) ;
#24819=ORIENTED_EDGE ( 'NONE', *, *, #31518, .F. ) ;
#24842=CARTESIAN_POINT ( 'NONE',  ( -10.30047626211725742, 6.835476262117182955, 54.00000000000000711 ) ) ;
#24847=ADVANCED_FACE ( 'NONE', ( #26602 ), #9290, .T. ) ;
#24851=DIRECTION ( 'NONE',  ( 1.836970198721029934E-16, 1.836970198721010706E-16, -1.000000000000000000 ) ) ;
#24855=AXIS2_PLACEMENT_3D ( 'NONE', #45116, #18245, #7640 ) ;
#24860=EDGE_LOOP ( 'NONE', ( #31188, #4228, #67981, #1444 ) ) ;
#24885=PLANE ( 'NONE',  #28907 ) ;
#24896=EDGE_CURVE ( 'NONE', #8571, #19298, #2146, .T. ) ;
#24904=PLANE ( 'NONE',  #3128 ) ;
#24910=DIRECTION ( 'NONE',  ( -1.836970198721029934E-16, 1.836970198721036590E-16, -1.000000000000000000 ) ) ;
#24916=FACE_OUTER_BOUND ( 'NONE', #26079, .T. ) ;
#24929=CARTESIAN_POINT ( 'NONE',  ( 4.961189459950039904, -7.357023737882811609, 26.00000000000000000 ) ) ;
#24930=ORIENTED_EDGE ( 'NONE', *, *, #66361, .T. ) ;
#24932=LINE ( 'NONE', #13271, #59799 ) ;
#24935=CARTESIAN_POINT ( 'NONE',  ( -2.530476262117325792, -9.562023737882828556, 54.00000000000000711 ) ) ;
#24941=ORIENTED_EDGE ( 'NONE', *, *, #27331, .T. ) ;
#24944=ORIENTED_EDGE ( 'NONE', *, *, #46826, .T. ) ;
#24946=EDGE_CURVE ( 'NONE', #65821, #54028, #59751, .T. ) ;
#24950=DIRECTION ( 'NONE',  ( 9.756599977372196271E-15, 1.000000000000000000, 0.000000000000000000 ) ) ;
#24972=CIRCLE ( 'NONE', #14843, 0.1749999999999989342 ) ;
#24981=PLANE ( 'NONE',  #67469 ) ;
#24983=VERTEX_POINT ( 'NONE', #59477 ) ;
#24996=CARTESIAN_POINT ( 'NONE',  ( -4.031976262117261456, 3.142976262117183506, 54.00000000000000711 ) ) ;
#25000=DIRECTION ( 'NONE',  ( 1.836970198721029934E-16, -1.836970198721036344E-16, 1.000000000000000000 ) ) ;
#25007=ORIENTED_EDGE ( 'NONE', *, *, #11052, .T. ) ;
#25009=ADVANCED_FACE ( 'NONE', ( #17367 ), #793, .F. ) ;
#25011=CYLINDRICAL_SURFACE ( 'NONE', #24475, 1.224999999999998757 ) ;
#25012=CARTESIAN_POINT ( 'NONE',  ( 6.832023737882812142, 9.722976262117196455, 26.00000000000000711 ) ) ;
#25023=CYLINDRICAL_SURFACE ( 'NONE', #30057, 0.1749999999999998224 ) ;
#25026=EDGE_CURVE ( 'NONE', #37598, #65595, #45984, .T. ) ;
#25030=FACE_OUTER_BOUND ( 'NONE', #7959, .T. ) ;
#25042=CARTESIAN_POINT ( 'NONE',  ( -9.722976262117256852, 7.955476262117183062, 54.00000000000000711 ) ) ;
#25059=CARTESIAN_POINT ( 'NONE',  ( -10.30047626211729472, -6.849523737882750929, 54.00000000000000711 ) ) ;
#25073=ORIENTED_EDGE ( 'NONE', *, *, #30037, .T. ) ;
#25074=EDGE_CURVE ( 'NONE', #53050, #22714, #39391, .T. ) ;
#25076=DIRECTION ( 'NONE',  ( -0.000000000000000000, 3.673940397442059868E-16, -1.000000000000000000 ) ) ;
#25085=PLANE ( 'NONE',  #32457 ) ;
#25095=CARTESIAN_POINT ( 'NONE',  ( 3.664523737882781518, -10.31452373788281029, 54.00000000000000711 ) ) ;
#25097=EDGE_CURVE ( 'NONE', #41013, #6189, #22547, .T. ) ;
#25098=CARTESIAN_POINT ( 'NONE',  ( -8.821682069070828192, -7.969523737882767911, 54.00000000000000711 ) ) ;
#25103=FACE_OUTER_BOUND ( 'NONE', #840, .T. ) ;
#25105=ORIENTED_EDGE ( 'NONE', *, *, #19426, .F. ) ;
#25106=ORIENTED_EDGE ( 'NONE', *, *, #59683, .T. ) ;
#25109=CARTESIAN_POINT ( 'NONE',  ( -7.172176262117273993, -5.257023737882780878, 26.00000000000000711 ) ) ;
#25110=DIRECTION ( 'NONE',  ( -1.836970198721029934E-16, 1.836970198721036590E-16, -1.000000000000000000 ) ) ;
#25130=ORIENTED_EDGE ( 'NONE', *, *, #19483, .T. ) ;
#25134=CARTESIAN_POINT ( 'NONE',  ( -9.547976262117222390, -2.369523737882729186, 54.00000000000000711 ) ) ;
#25137=ORIENTED_EDGE ( 'NONE', *, *, #28010, .F. ) ;
#25139=CIRCLE ( 'NONE', #8210, 1.929199999999997139 ) ;
#25145=ORIENTED_EDGE ( 'NONE', *, *, #17643, .T. ) ;
#25151=CIRCLE ( 'NONE', #15008, 1.929199999999998028 ) ;
#25152=CYLINDRICAL_SURFACE ( 'NONE', #44731, 0.7112000000000124889 ) ;
#25153=PLANE ( 'NONE',  #13651 ) ;
#25154=FACE_OUTER_BOUND ( 'NONE', #27110, .T. ) ;
#25156=ORIENTED_EDGE ( 'NONE', *, *, #68188, .T. ) ;
#25157=EDGE_CURVE ( 'NONE', #4457, #49409, #29357, .T. ) ;
#25161=VECTOR ( 'NONE', #45341, 1000.000000000000000 ) ;
#25163=EDGE_CURVE ( 'NONE', #14797, #68930, #67904, .T. ) ;
#25164=DIRECTION ( 'NONE',  ( -0.000000000000000000, 3.673940397442059868E-16, -1.000000000000000000 ) ) ;
#25172=CYLINDRICAL_SURFACE ( 'NONE', #62742, 0.1749999999999998224 ) ;
#25177=CARTESIAN_POINT ( 'NONE',  ( -9.689726262117318356, -8.930623737882756430, 54.00000000000000711 ) ) ;
#25181=ORIENTED_EDGE ( 'NONE', *, *, #14568, .T. ) ;
#25183=CARTESIAN_POINT ( 'NONE',  ( 2.544523737882792069, -8.835729544836324223, 54.00000000000000711 ) ) ;
#25190=LINE ( 'NONE', #47452, #55070 ) ;
#25192=CARTESIAN_POINT ( 'NONE',  ( -9.390476262117203987, -1.480523737882726731, 26.00000000000000711 ) ) ;
#25196=DIRECTION ( 'NONE',  ( -1.000000000000000000, -1.671920889371702854E-15, -0.000000000000000000 ) ) ;
#25200=ORIENTED_EDGE ( 'NONE', *, *, #40807, .F. ) ;
#25203=CARTESIAN_POINT ( 'NONE',  ( -8.227189898828694226, -1.634292677759810575, 26.00000000000000711 ) ) ;
#25208=EDGE_CURVE ( 'NONE', #67341, #97, #62956, .T. ) ;
#25210=DIRECTION ( 'NONE',  ( 0.000000000000000000, 0.000000000000000000, 1.000000000000000000 ) ) ;
#25213=EDGE_LOOP ( 'NONE', ( #21830, #43080, #39410, #49408 ) ) ;
#25225=ORIENTED_EDGE ( 'NONE', *, *, #17660, .F. ) ;
#25229=CARTESIAN_POINT ( 'NONE',  ( 3.677663764522620671, 4.135079735113112775, 54.00000000000000711 ) ) ;
#25237=ADVANCED_FACE ( 'NONE', ( #68250 ), #4270, .F. ) ;
#25243=ORIENTED_EDGE ( 'NONE', *, *, #20920, .T. ) ;
#25245=ORIENTED_EDGE ( 'NONE', *, *, #39349, .F. ) ;
#25250=CYLINDRICAL_SURFACE ( 'NONE', #1127, 0.5249999999999994671 ) ;
#25257=CARTESIAN_POINT ( 'NONE',  ( 9.562023737882812569, -2.369523737882825998, 54.00000000000000711 ) ) ;
#25259=ORIENTED_EDGE ( 'NONE', *, *, #35873, .F. ) ;
#25266=DIRECTION ( 'NONE',  ( -0.5000000000000129896, -0.8660254037844311581, -2.509347957447868930E-16 ) ) ;
#25271=DIRECTION ( 'NONE',  ( 1.836970198721029934E-16, 1.836970198721010706E-16, -1.000000000000000000 ) ) ;
#25279=ORIENTED_EDGE ( 'NONE', *, *, #17196, .F. ) ;
#25286=DIRECTION ( 'NONE',  ( 0.000000000000000000, 3.673940397442059868E-16, -1.000000000000000000 ) ) ;
#25289=ADVANCED_FACE ( 'NONE', ( #63303 ), #26176, .F. ) ;
#25290=EDGE_CURVE ( 'NONE', #21406, #6346, #15743, .T. ) ;
#25291=FACE_OUTER_BOUND ( 'NONE', #43560, .T. ) ;
#25292=CIRCLE ( 'NONE', #30947, 0.1749999999999998224 ) ;
#25294=AXIS2_PLACEMENT_3D ( 'NONE', #37091, #38719, #25784 ) ;
#25296=ORIENTED_EDGE ( 'NONE', *, *, #20539, .T. ) ;
#25307=FACE_OUTER_BOUND ( 'NONE', #43891, .T. ) ;
#25308=VECTOR ( 'NONE', #44240, 1000.000000000000000 ) ;
#25311=ORIENTED_EDGE ( 'NONE', *, *, #52253, .T. ) ;
#25319=CARTESIAN_POINT ( 'NONE',  ( -6.835476262117260227, 10.49297626211718359, 26.00000000000000711 ) ) ;
#25327=EDGE_CURVE ( 'NONE', #47065, #46851, #64352, .T. ) ;
#25330=DIRECTION ( 'NONE',  ( -1.000000000000000000, 1.047444401652940007E-14, -1.836970198721010706E-16 ) ) ;
#25332=ADVANCED_FACE ( 'NONE', ( #65047 ), #48783, .F. ) ;
#25333=CYLINDRICAL_SURFACE ( 'NONE', #23168, 0.1749999999999998224 ) ;
#25334=VERTEX_POINT ( 'NONE', #697 ) ;
#25347=CARTESIAN_POINT ( 'NONE',  ( -1.466476262117324181, -9.404523737882843903, 54.00000000000000711 ) ) ;
#25355=CARTESIAN_POINT ( 'NONE',  ( 6.789561617636934443, 7.394232575409549035, 54.00000000000000711 ) ) ;
#25357=CARTESIAN_POINT ( 'NONE',  ( -4.947141984184481700, 7.342976262117180575, 54.00000000000000711 ) ) ;
#25361=PLANE ( 'NONE',  #22052 ) ;
#25363=CARTESIAN_POINT ( 'NONE',  ( -10.49297626211732748, -9.795823737882738413, 54.00000000000000711 ) ) ;
#25365=ORIENTED_EDGE ( 'NONE', *, *, #38239, .F. ) ;
#25367=DIRECTION ( 'NONE',  ( 0.7071067811865500152, 0.7071067811865451302, 0.000000000000000000 ) ) ;
#25368=DIRECTION ( 'NONE',  ( -1.836970198721029934E-16, 1.836970198721036590E-16, -1.000000000000000000 ) ) ;
#25378=CARTESIAN_POINT ( 'NONE',  ( -9.722976262117303037, -7.969523737882757253, 54.00000000000000711 ) ) ;
#25382=DIRECTION ( 'NONE',  ( 1.000000000000000000, -1.047444401652940007E-14, 1.836970198721010706E-16 ) ) ;
#25399=DIRECTION ( 'NONE',  ( -0.000000000000000000, -0.000000000000000000, -1.000000000000000000 ) ) ;
#25400=ORIENTED_EDGE ( 'NONE', *, *, #59583, .T. ) ;
#25411=CARTESIAN_POINT ( 'NONE',  ( 6.364920264886885448, -3.677663764522628664, 54.00000000000000711 ) ) ;
#25413=FACE_OUTER_BOUND ( 'NONE', #43958, .T. ) ;
#25422=VERTEX_POINT ( 'NONE', #55472 ) ;
#25429=VERTEX_POINT ( 'NONE', #27224 ) ;
#25435=ORIENTED_EDGE ( 'NONE', *, *, #53323, .F. ) ;
#25442=CARTESIAN_POINT ( 'NONE',  ( -2.355476262117229158, 9.547976262117156665, 54.00000000000000711 ) ) ;
#25443=ORIENTED_EDGE ( 'NONE', *, *, #50341, .F. ) ;
#25455=CARTESIAN_POINT ( 'NONE',  ( 8.835729544836338434, -7.969523737882814984, 26.00000000000000000 ) ) ;
#25458=ORIENTED_EDGE ( 'NONE', *, *, #62952, .T. ) ;
#25469=ADVANCED_FACE ( 'NONE', ( #55131 ), #6670, .F. ) ;
#25475=EDGE_LOOP ( 'NONE', ( #18007, #52721, #9774, #67852 ) ) ;
#25478=DIRECTION ( 'NONE',  ( 1.836970198721029934E-16, 1.836970198721010706E-16, -1.000000000000000000 ) ) ;
#25484=AXIS2_PLACEMENT_3D ( 'NONE', #22585, #58437, #17269 ) ;
#25487=EDGE_CURVE ( 'NONE', #52552, #40627, #39533, .T. ) ;
#25491=AXIS2_PLACEMENT_3D ( 'NONE', #28016, #65163, #6101 ) ;
#25506=DIRECTION ( 'NONE',  ( 1.836970198721029934E-16, 1.836970198721010706E-16, -1.000000000000000000 ) ) ;
#25510=EDGE_CURVE ( 'NONE', #30361, #61947, #7706, .T. ) ;
#25514=DIRECTION ( 'NONE',  ( -1.836970198721029934E-16, 1.836970198721036590E-16, -1.000000000000000000 ) ) ;
#25526=DIRECTION ( 'NONE',  ( 1.000000000000000000, 0.000000000000000000, 0.000000000000000000 ) ) ;
#25527=DIRECTION ( 'NONE',  ( 1.836970198721029934E-16, 1.836970198721010706E-16, -1.000000000000000000 ) ) ;
#25531=FACE_OUTER_BOUND ( 'NONE', #22509, .T. ) ;
#25550=VECTOR ( 'NONE', #5163, 1000.000000000000114 ) ;
#25553=VECTOR ( 'NONE', #10173, 1000.000000000000000 ) ;
#25555=VECTOR ( 'NONE', #35928, 1000.000000000000000 ) ;
#25563=EDGE_CURVE ( 'NONE', #62241, #43177, #34991, .T. ) ;
#25567=DIRECTION ( 'NONE',  ( -0.000000000000000000, -0.000000000000000000, -1.000000000000000000 ) ) ;
#25569=EDGE_CURVE ( 'NONE', #61947, #66569, #9010, .T. ) ;
#25572=DIRECTION ( 'NONE',  ( -0.000000000000000000, 3.673940397442059868E-16, -1.000000000000000000 ) ) ;
#25573=ADVANCED_FACE ( 'NONE', ( #8050 ), #2066, .F. ) ;
#25579=EDGE_CURVE ( 'NONE', #36648, #21659, #40589, .T. ) ;
#25581=DIRECTION ( 'NONE',  ( 0.000000000000000000, 1.000000000000000000, 0.000000000000000000 ) ) ;
#25582=CARTESIAN_POINT ( 'NONE',  ( -5.242976262117259978, 5.242976262117182706, 54.00000000000000711 ) ) ;
#25585=AXIS2_PLACEMENT_3D ( 'NONE', #50372, #39409, #1938 ) ;
#25587=DIRECTION ( 'NONE',  ( -0.000000000000000000, 0.000000000000000000, -1.000000000000000000 ) ) ;
#25589=ORIENTED_EDGE ( 'NONE', *, *, #32642, .T. ) ;
#25591=ORIENTED_EDGE ( 'NONE', *, *, #27213, .T. ) ;
#25597=VERTEX_POINT ( 'NONE', #23974 ) ;
#25606=VERTEX_POINT ( 'NONE', #29978 ) ;
#25615=CARTESIAN_POINT ( 'NONE',  ( 6.358413763958968623, -5.793274621760859944, 54.00000000000000711 ) ) ;
#25617=VECTOR ( 'NONE', #62628, 1000.000000000000114 ) ;
#25622=CARTESIAN_POINT ( 'NONE',  ( -7.342976262117259623, 3.834182069070703580, 26.00000000000000711 ) ) ;
#25632=EDGE_CURVE ( 'NONE', #47780, #64355, #56441, .T. ) ;
#25643=DIRECTION ( 'NONE',  ( 1.836970198721029934E-16, 1.836970198721010706E-16, -1.000000000000000000 ) ) ;
#25644=LINE ( 'NONE', #47209, #59947 ) ;
#25655=VERTEX_POINT ( 'NONE', #51908 ) ;
#25657=AXIS2_PLACEMENT_3D ( 'NONE', #7356, #38522, #33548 ) ;
#25663=EDGE_CURVE ( 'NONE', #23407, #41000, #4178, .T. ) ;
#25664=VECTOR ( 'NONE', #1647, 1000.000000000000000 ) ;
#25674=ORIENTED_EDGE ( 'NONE', *, *, #48178, .F. ) ;
#25676=LINE ( 'NONE', #35916, #50417 ) ;
#25684=ORIENTED_EDGE ( 'NONE', *, *, #61282, .T. ) ;
#25690=CYLINDRICAL_SURFACE ( 'NONE', #65072, 0.1749999999999998224 ) ;
#25697=CARTESIAN_POINT ( 'NONE',  ( -10.30047626211729295, -6.657023737882751924, 54.00000000000000711 ) ) ;
#25703=ADVANCED_FACE ( 'NONE', ( #57904 ), #69576, .F. ) ;
#25707=LINE ( 'NONE', #46895, #18933 ) ;
#25710=ORIENTED_EDGE ( 'NONE', *, *, #30584, .F. ) ;
#25714=CARTESIAN_POINT ( 'NONE',  ( 10.50702373788278265, 3.650476262117142934, 54.00000000000000711 ) ) ;
#25716=DIRECTION ( 'NONE',  ( -0.7671651518153087546, -0.6414496315691469164, 2.309356642089053889E-17 ) ) ;
#25719=CARTESIAN_POINT ( 'NONE',  ( 9.703773737882816164, 9.689726262117153155, 54.00000000000000711 ) ) ;
#25725=CARTESIAN_POINT ( 'NONE',  ( 9.737023737882799068, 6.817976262117189989, 26.00000000000000711 ) ) ;
#25727=FACE_OUTER_BOUND ( 'NONE', #7079, .T. ) ;
#25734=LINE ( 'NONE', #68859, #61953 ) ;
#25747=LINE ( 'NONE', #4179, #69772 ) ;
#25760=ORIENTED_EDGE ( 'NONE', *, *, #50648, .F. ) ;
#25767=EDGE_CURVE ( 'NONE', #69660, #49465, #27086, .T. ) ;
#25781=DIRECTION ( 'NONE',  ( 9.756599977372196271E-15, 1.000000000000000000, 0.000000000000000000 ) ) ;
#25784=DIRECTION ( 'NONE',  ( -1.000000000000000000, 0.000000000000000000, 0.000000000000000000 ) ) ;
#25788=DIRECTION ( 'NONE',  ( 1.000000000000000000, -3.491481338843133355E-15, -1.836970198721036344E-16 ) ) ;
#25789=CARTESIAN_POINT ( 'NONE',  ( 9.737023737882816832, -3.682023737882826886, 54.00000000000000711 ) ) ;
#25801=VECTOR ( 'NONE', #17989, 1000.000000000000000 ) ;
#25811=ADVANCED_FACE ( 'NONE', ( #17541 ), #5909, .F. ) ;
#25812=CARTESIAN_POINT ( 'NONE',  ( -6.350872789121377870, -6.836383711242978833, 54.00000000000000711 ) ) ;
#25815=EDGE_LOOP ( 'NONE', ( #14622, #63918, #19292, #13111 ) ) ;
#25821=ADVANCED_FACE ( 'NONE', ( #59987 ), #59299, .T. ) ;
#25829=DIRECTION ( 'NONE',  ( 1.000000000000000000, 0.000000000000000000, 0.000000000000000000 ) ) ;
#25832=EDGE_CURVE ( 'NONE', #65287, #69896, #32085, .T. ) ;
#25834=ORIENTED_EDGE ( 'NONE', *, *, #60195, .F. ) ;
#25841=EDGE_LOOP ( 'NONE', ( #37244, #40498, #55706, #58332 ) ) ;
#25842=ORIENTED_EDGE ( 'NONE', *, *, #65780, .T. ) ;
#25866=DIRECTION ( 'NONE',  ( -1.836970198721029934E-16, 1.836970198721036590E-16, -1.000000000000000000 ) ) ;
#25867=ORIENTED_EDGE ( 'NONE', *, *, #67786, .T. ) ;
#25871=LINE ( 'NONE', #58032, #12043 ) ;
#25878=CARTESIAN_POINT ( 'NONE',  ( 5.257023737882819070, -5.257023737882825287, 54.00000000000000711 ) ) ;
#25887=CARTESIAN_POINT ( 'NONE',  ( 10.50702373788280752, 6.835476262117182067, 54.00000000000000711 ) ) ;
#25892=EDGE_CURVE ( 'NONE', #48101, #14855, #55309, .T. ) ;
#25893=AXIS2_PLACEMENT_3D ( 'NONE', #33636, #6754, #17723 ) ;
#25894=DIRECTION ( 'NONE',  ( 0.000000000000000000, 1.000000000000000000, 0.000000000000000000 ) ) ;
#25901=VECTOR ( 'NONE', #58497, 1000.000000000000000 ) ;
#25910=DIRECTION ( 'NONE',  ( -1.836970198721029934E-16, 1.836970198721036344E-16, -1.000000000000000000 ) ) ;
#25922=EDGE_CURVE ( 'NONE', #32175, #55318, #29545, .T. ) ;
#25925=DIRECTION ( 'NONE',  ( -0.7671651518153105309, -0.6414496315691445849, 0.000000000000000000 ) ) ;
#25929=ORIENTED_EDGE ( 'NONE', *, *, #790, .T. ) ;
#25941=DIRECTION ( 'NONE',  ( -3.491481338843133355E-15, -1.000000000000000000, -1.836970198721029934E-16 ) ) ;
#25958=DIRECTION ( 'NONE',  ( -0.6414496315691494699, 0.7671651518153064231, 0.000000000000000000 ) ) ;
#25959=CARTESIAN_POINT ( 'NONE',  ( -2.355476262117325525, -9.562023737882830332, 54.00000000000000711 ) ) ;
#25966=PLANE ( 'NONE',  #64875 ) ;
#25974=VERTEX_POINT ( 'NONE', #19290 ) ;
#25981=CARTESIAN_POINT ( 'NONE',  ( -9.897976262117259338, 3.842976262117183683, 54.00000000000000711 ) ) ;
#25986=LINE ( 'NONE', #47202, #16303 ) ;
#25995=DIRECTION ( 'NONE',  ( 1.000000000000000000, 1.570596175624152290E-15, 5.770276737693577136E-31 ) ) ;
#25997=AXIS2_PLACEMENT_3D ( 'NONE', #53659, #54697, #54015 ) ;
#26000=LINE ( 'NONE', #47558, #68478 ) ;
#26008=AXIS2_PLACEMENT_3D ( 'NONE', #33865, #38829, #60055 ) ;
#26018=VECTOR ( 'NONE', #29067, 1000.000000000000000 ) ;
#26022=ORIENTED_EDGE ( 'NONE', *, *, #42659, .F. ) ;
#26034=DIRECTION ( 'NONE',  ( -1.836970198721029934E-16, 1.836970198721036590E-16, -1.000000000000000000 ) ) ;
#26045=AXIS2_PLACEMENT_3D ( 'NONE', #11163, #28458, #54314 ) ;
#26058=FACE_OUTER_BOUND ( 'NONE', #28948, .T. ) ;
#26062=DIRECTION ( 'NONE',  ( 1.000000000000000000, 0.000000000000000000, 0.000000000000000000 ) ) ;
#26064=VECTOR ( 'NONE', #67154, 1000.000000000000000 ) ;
#26065=CARTESIAN_POINT ( 'NONE',  ( -6.835476262117333057, -10.31452373788278543, 54.00000000000000711 ) ) ;
#26070=DIRECTION ( 'NONE',  ( -1.000000000000000000, -1.570596175624152290E-15, 0.000000000000000000 ) ) ;
#26072=DIRECTION ( 'NONE',  ( 1.836970198721029934E-16, 1.836970198721010706E-16, -1.000000000000000000 ) ) ;
#26079=EDGE_LOOP ( 'NONE', ( #28341, #3362, #10020, #68632 ) ) ;
#26090=DIRECTION ( 'NONE',  ( 1.836970198721029934E-16, 1.836970198721010706E-16, -1.000000000000000000 ) ) ;
#26097=LINE ( 'NONE', #25042, #56022 ) ;
#26099=LINE ( 'NONE', #6848, #36089 ) ;
#26103=ORIENTED_EDGE ( 'NONE', *, *, #43886, .F. ) ;
#26119=ORIENTED_EDGE ( 'NONE', *, *, #20105, .T. ) ;
#26121=CARTESIAN_POINT ( 'NONE',  ( 4.149127210878726935, -3.677663764522648204, 54.00000000000000711 ) ) ;
#26132=CARTESIAN_POINT ( 'NONE',  ( -2.406732575409666008, -8.711985858128704407, 26.00000000000000711 ) ) ;
#26137=ORIENTED_EDGE ( 'NONE', *, *, #4469, .F. ) ;
#26154=DIRECTION ( 'NONE',  ( -1.000000000000000000, 8.359604446858500663E-15, 3.071268848394972853E-30 ) ) ;
#26158=CARTESIAN_POINT ( 'NONE',  ( 10.05377373788278739, -8.930623737882855906, 54.00000000000000711 ) ) ;
#26164=DIRECTION ( 'NONE',  ( 0.6414496315691367023, -0.7671651518153173033, -2.309356642089295169E-17 ) ) ;
#26176=PLANE ( 'NONE',  #13502 ) ;
#26177=CARTESIAN_POINT ( 'NONE',  ( -4.706725378239257296, -6.358413763958960629, 54.00000000000000711 ) ) ;
#26191=AXIS2_PLACEMENT_3D ( 'NONE', #32902, #54483, #7748 ) ;
#26200=EDGE_CURVE ( 'NONE', #58466, #7367, #60832, .T. ) ;
#26208=ORIENTED_EDGE ( 'NONE', *, *, #28411, .T. ) ;
#26213=CARTESIAN_POINT ( 'NONE',  ( 10.31452373788277832, 3.842976262117149044, 26.00000000000000711 ) ) ;
#26225=LINE ( 'NONE', #37536, #52142 ) ;
#26234=EDGE_CURVE ( 'NONE', #65595, #64473, #10040, .T. ) ;
#26242=ORIENTED_EDGE ( 'NONE', *, *, #45644, .F. ) ;
#26244=AXIS2_PLACEMENT_3D ( 'NONE', #13110, #2848, #44581 ) ;
#26246=LINE ( 'NONE', #62657, #54551 ) ;
#26247=AXIS2_PLACEMENT_3D ( 'NONE', #66248, #5485, #23105 ) ;
#26253=ORIENTED_EDGE ( 'NONE', *, *, #27397, .T. ) ;
#26273=VERTEX_POINT ( 'NONE', #11464 ) ;
#26277=VECTOR ( 'NONE', #27790, 1000.000000000000000 ) ;
#26283=LINE ( 'NONE', #64472, #39052 ) ;
#26292=DIRECTION ( 'NONE',  ( 0.000000000000000000, 3.673940397442059868E-16, -1.000000000000000000 ) ) ;
#26299=ORIENTED_EDGE ( 'NONE', *, *, #25327, .F. ) ;
#26300=DIRECTION ( 'NONE',  ( -1.000000000000000000, 3.491481338843133355E-15, 1.836970198721036344E-16 ) ) ;
#26304=EDGE_CURVE ( 'NONE', #58150, #39317, #33727, .T. ) ;
#26308=CIRCLE ( 'NONE', #4858, 0.5249999999999994671 ) ;
#26320=DIRECTION ( 'NONE',  ( 0.000000000000000000, 3.673940397442059868E-16, -1.000000000000000000 ) ) ;
#26334=VERTEX_POINT ( 'NONE', #50335 ) ;
#26351=VERTEX_POINT ( 'NONE', #51035 ) ;
#26358=AXIS2_PLACEMENT_3D ( 'NONE', #44588, #60859, #66173 ) ;
#26361=ORIENTED_EDGE ( 'NONE', *, *, #65925, .T. ) ;
#26370=DIRECTION ( 'NONE',  ( 1.836970198721029934E-16, 1.836970198721010706E-16, -1.000000000000000000 ) ) ;
#26376=EDGE_CURVE ( 'NONE', #46858, #11718, #28415, .T. ) ;
#26382=ADVANCED_FACE ( 'NONE', ( #59453 ), #48851, .F. ) ;
#26383=CARTESIAN_POINT ( 'NONE',  ( -3.667976262117328190, -9.737023737882820384, 54.00000000000000711 ) ) ;
#26388=CARTESIAN_POINT ( 'NONE',  ( 8.093267424590454340, 8.697938382363069820, 26.00000000000000711 ) ) ;
#26391=PLANE ( 'NONE',  #45514 ) ;
#26393=CARTESIAN_POINT ( 'NONE',  ( -8.821682069070780230, 2.355476262117184305, 54.00000000000000711 ) ) ;
#26396=DIRECTION ( 'NONE',  ( 3.491481338843133355E-15, 1.000000000000000000, 1.836970198721029934E-16 ) ) ;
#26399=CIRCLE ( 'NONE', #33144, 0.1749999999999998224 ) ;
#26401=CARTESIAN_POINT ( 'NONE',  ( -8.916576262117260399, 8.916576262117214213, 54.00000000000000711 ) ) ;
#26409=DIRECTION ( 'NONE',  ( -0.7071067811865474617, 0.7071067811865474617, -0.000000000000000000 ) ) ;
#26418=CARTESIAN_POINT ( 'NONE',  ( -10.03972626211732688, -9.703773737882722017, 54.00000000000000711 ) ) ;
#26422=EDGE_CURVE ( 'NONE', #17979, #26351, #32232, .T. ) ;
#26439=DIRECTION ( 'NONE',  ( -1.000000000000000000, 0.000000000000000000, 0.000000000000000000 ) ) ;
#26441=ORIENTED_EDGE ( 'NONE', *, *, #10798, .F. ) ;
#26443=AXIS2_PLACEMENT_3D ( 'NONE', #6316, #43098, #32839 ) ;
#26449=EDGE_CURVE ( 'NONE', #64879, #32175, #34877, .T. ) ;
#26466=DIRECTION ( 'NONE',  ( -0.000000000000000000, 3.673940397442059868E-16, -1.000000000000000000 ) ) ;
#26467=ORIENTED_EDGE ( 'NONE', *, *, #53453, .T. ) ;
#26469=DIRECTION ( 'NONE',  ( 1.836970198721029934E-16, 1.836970198721010706E-16, -1.000000000000000000 ) ) ;
#26481=DIRECTION ( 'NONE',  ( -1.000000000000000000, 1.047444401652940007E-14, 0.000000000000000000 ) ) ;
#26485=EDGE_CURVE ( 'NONE', #19647, #30244, #8955, .T. ) ;
#26498=DIRECTION ( 'NONE',  ( 1.836970198721029934E-16, 1.836970198721010706E-16, -1.000000000000000000 ) ) ;
#26500=VECTOR ( 'NONE', #47620, 1000.000000000000000 ) ;
#26505=ORIENTED_EDGE ( 'NONE', *, *, #55593, .F. ) ;
#26510=LINE ( 'NONE', #52698, #28754 ) ;
#26516=ORIENTED_EDGE ( 'NONE', *, *, #44313, .T. ) ;
#26523=AXIS2_PLACEMENT_3D ( 'NONE', #17401, #50276, #38976 ) ;
#26531=ORIENTED_EDGE ( 'NONE', *, *, #43993, .F. ) ;
#26534=EDGE_CURVE ( 'NONE', #8859, #40018, #57507, .T. ) ;
#26535=DIRECTION ( 'NONE',  ( -1.000000000000000000, 0.000000000000000000, 0.000000000000000000 ) ) ;
#26539=VECTOR ( 'NONE', #44480, 1000.000000000000000 ) ;
#26540=DIRECTION ( 'NONE',  ( -1.000000000000000000, 0.000000000000000000, 0.000000000000000000 ) ) ;
#26541=DIRECTION ( 'NONE',  ( -0.000000000000000000, -0.000000000000000000, -1.000000000000000000 ) ) ;
#26548=EDGE_LOOP ( 'NONE', ( #22657, #38757, #48434, #63914 ) ) ;
#26554=ORIENTED_EDGE ( 'NONE', *, *, #40562, .F. ) ;
#26555=CARTESIAN_POINT ( 'NONE',  ( 9.562023737882805463, 8.130476262117184660, 54.00000000000000711 ) ) ;
#26562=DIRECTION ( 'NONE',  ( 3.540251991789405856E-15, 1.000000000000000000, 0.000000000000000000 ) ) ;
#26564=VECTOR ( 'NONE', #43910, 1000.000000000000000 ) ;
#26565=LINE ( 'NONE', #35764, #55230 ) ;
#26566=ORIENTED_EDGE ( 'NONE', *, *, #59158, .F. ) ;
#26573=EDGE_CURVE ( 'NONE', #38860, #19920, #34854, .T. ) ;
#26574=CARTESIAN_POINT ( 'NONE',  ( -10.30047626211728762, -6.657023737882746595, 26.00000000000000000 ) ) ;
#26584=ORIENTED_EDGE ( 'NONE', *, *, #47002, .T. ) ;
#26585=DIRECTION ( 'NONE',  ( -0.000000000000000000, 3.673940397442059868E-16, -1.000000000000000000 ) ) ;
#26593=DIRECTION ( 'NONE',  ( 0.000000000000000000, 3.673940397442059868E-16, -1.000000000000000000 ) ) ;
#26595=VERTEX_POINT ( 'NONE', #3056 ) ;
#26602=FACE_OUTER_BOUND ( 'NONE', #41111, .T. ) ;
#26614=VECTOR ( 'NONE', #35202, 1000.000000000000000 ) ;
#26625=ORIENTED_EDGE ( 'NONE', *, *, #16689, .F. ) ;
#26631=LINE ( 'NONE', #48200, #1798 ) ;
#26653=VERTEX_POINT ( 'NONE', #67038 ) ;
#26665=EDGE_LOOP ( 'NONE', ( #53354, #22704, #28532, #61256 ) ) ;
#26668=VECTOR ( 'NONE', #61589, 1000.000000000000000 ) ;
#26672=DIRECTION ( 'NONE',  ( 0.7671651518153173033, 0.6414496315691367023, 2.587583378555108576E-16 ) ) ;
#26681=ADVANCED_FACE ( 'NONE', ( #40164 ), #7286, .T. ) ;
#26686=LINE ( 'NONE', #52155, #55353 ) ;
#26689=ORIENTED_EDGE ( 'NONE', *, *, #64567, .F. ) ;
#26691=DIRECTION ( 'NONE',  ( 0.000000000000000000, 3.673940397442059868E-16, -1.000000000000000000 ) ) ;
#26694=ORIENTED_EDGE ( 'NONE', *, *, #30919, .T. ) ;
#26697=VECTOR ( 'NONE', #63424, 1000.000000000000114 ) ;
#26702=CIRCLE ( 'NONE', #14283, 1.929199999999997139 ) ;
#26710=AXIS2_PLACEMENT_3D ( 'NONE', #67114, #8054, #56849 ) ;
#26714=EDGE_LOOP ( 'NONE', ( #45145, #5733, #15752, #51147 ) ) ;
#26733=DIRECTION ( 'NONE',  ( -8.339399738404101090E-15, -1.000000000000000000, -1.836970198721025990E-16 ) ) ;
#26735=CIRCLE ( 'NONE', #16598, 0.1749999999999989342 ) ;
#26742=AXIS2_PLACEMENT_3D ( 'NONE', #43852, #7393, #11321 ) ;
#26743=CARTESIAN_POINT ( 'NONE',  ( 9.737023737882816832, -3.682023737882817116, 26.00000000000000711 ) ) ;
#26745=CARTESIAN_POINT ( 'NONE',  ( 10.50702373788281641, 9.781776262117171328, 54.00000000000000711 ) ) ;
#26747=EDGE_CURVE ( 'NONE', #3920, #25334, #19817, .T. ) ;
#26751=ORIENTED_EDGE ( 'NONE', *, *, #17983, .T. ) ;
#26758=LINE ( 'NONE', #25355, #39772 ) ;
#26764=AXIS2_PLACEMENT_3D ( 'NONE', #49066, #33824, #12253 ) ;
#26767=EDGE_CURVE ( 'NONE', #22289, #10947, #58189, .T. ) ;
#26788=CARTESIAN_POINT ( 'NONE',  ( -7.394232575409645847, -6.789561617636902469, 26.00000000000000000 ) ) ;
#26790=CARTESIAN_POINT ( 'NONE',  ( -7.342976262117293373, -6.665817930929262225, 54.00000000000000711 ) ) ;
#26792=EDGE_CURVE ( 'NONE', #54627, #21960, #52910, .T. ) ;
#26795=ORIENTED_EDGE ( 'NONE', *, *, #6823, .T. ) ;
#26797=DIRECTION ( 'NONE',  ( 1.836970198721029934E-16, 1.836970198721010706E-16, -1.000000000000000000 ) ) ;
#26803=VECTOR ( 'NONE', #13679, 1000.000000000000000 ) ;
#26808=VERTEX_POINT ( 'NONE', #69148 ) ;
#26811=VECTOR ( 'NONE', #12674, 1000.000000000000000 ) ;
#26822=LINE ( 'NONE', #31779, #41441 ) ;
#26826=DIRECTION ( 'NONE',  ( 0.000000000000000000, 0.000000000000000000, 1.000000000000000000 ) ) ;
#26831=CARTESIAN_POINT ( 'NONE',  ( -8.697938382363103571, -2.420780051175099423, 54.00000000000000711 ) ) ;
#26837=PLANE ( 'NONE',  #64064 ) ;
#26842=ORIENTED_EDGE ( 'NONE', *, *, #22440, .T. ) ;
#26851=FACE_OUTER_BOUND ( 'NONE', #49502, .T. ) ;
#26852=EDGE_LOOP ( 'NONE', ( #26516, #44958, #2745, #51117 ) ) ;
#26857=FACE_OUTER_BOUND ( 'NONE', #37862, .T. ) ;
#26864=ORIENTED_EDGE ( 'NONE', *, *, #30037, .F. ) ;
#26866=VERTEX_POINT ( 'NONE', #16804 ) ;
#26870=AXIS2_PLACEMENT_3D ( 'NONE', #42690, #64272, #15821 ) ;
#26871=EDGE_CURVE ( 'NONE', #42883, #11023, #48985, .T. ) ;
#26876=LINE ( 'NONE', #49118, #5907 ) ;
#26877=ORIENTED_EDGE ( 'NONE', *, *, #22911, .F. ) ;
#26878=EDGE_LOOP ( 'NONE', ( #46537, #31337, #19504, #41829 ) ) ;
#26882=DIRECTION ( 'NONE',  ( -1.836970198721029934E-16, 1.836970198721036590E-16, -1.000000000000000000 ) ) ;
#26891=ORIENTED_EDGE ( 'NONE', *, *, #57492, .F. ) ;
#26892=DIRECTION ( 'NONE',  ( 1.836970198721029934E-16, 1.836970198721010706E-16, -1.000000000000000000 ) ) ;
#26896=AXIS2_PLACEMENT_3D ( 'NONE', #68315, #15634, #36857 ) ;
#26899=LINE ( 'NONE', #47750, #49325 ) ;
#26905=CARTESIAN_POINT ( 'NONE',  ( -10.49297626211724754, -3.664523737882706023, 26.00000000000000000 ) ) ;
#26937=ORIENTED_EDGE ( 'NONE', *, *, #60280, .F. ) ;
#26939=DIRECTION ( 'NONE',  ( 1.836970198721029934E-16, -1.836970198721036344E-16, 1.000000000000000000 ) ) ;
#26941=EDGE_CURVE ( 'NONE', #48716, #17051, #37333, .T. ) ;
#26945=ORIENTED_EDGE ( 'NONE', *, *, #39819, .F. ) ;
#26955=ORIENTED_EDGE ( 'NONE', *, *, #28527, .F. ) ;
#26960=AXIS2_PLACEMENT_3D ( 'NONE', #39405, #56371, #28789 ) ;
#26972=VECTOR ( 'NONE', #35066, 1000.000000000000000 ) ;
#26976=EDGE_LOOP ( 'NONE', ( #21225, #8689, #46064, #12735 ) ) ;
#26982=DIRECTION ( 'NONE',  ( 0.000000000000000000, 1.000000000000000000, 0.000000000000000000 ) ) ;
#26984=EDGE_CURVE ( 'NONE', #61547, #17833, #8253, .T. ) ;
#26988=DIRECTION ( 'NONE',  ( 1.047444401652940007E-14, 1.000000000000000000, 1.836970198721029934E-16 ) ) ;
#26989=VERTEX_POINT ( 'NONE', #23487 ) ;
#26996=DIRECTION ( 'NONE',  ( 1.000000000000000000, 0.000000000000000000, 0.000000000000000000 ) ) ;
#26997=DIRECTION ( 'NONE',  ( -1.000000000000000000, 0.000000000000000000, 0.000000000000000000 ) ) ;
#27003=ORIENTED_EDGE ( 'NONE', *, *, #59732, .T. ) ;
#27009=DIRECTION ( 'NONE',  ( -1.836970198721029934E-16, -1.836970198721010706E-16, 1.000000000000000000 ) ) ;
#27010=ORIENTED_EDGE ( 'NONE', *, *, #37891, .T. ) ;
#27022=DIRECTION ( 'NONE',  ( -9.973078850062115052E-15, -1.000000000000000000, 0.000000000000000000 ) ) ;
#27033=ADVANCED_FACE ( 'NONE', ( #13219 ), #66277, .F. ) ;
#27037=CARTESIAN_POINT ( 'NONE',  ( 9.912023737882815766, -6.657023737882824754, 54.00000000000000711 ) ) ;
#27041=ORIENTED_EDGE ( 'NONE', *, *, #50341, .T. ) ;
#27043=VECTOR ( 'NONE', #67742, 1000.000000000000000 ) ;
#27045=CARTESIAN_POINT ( 'NONE',  ( -10.30047626211724499, -3.857023737882708581, 26.00000000000000000 ) ) ;
#27047=VECTOR ( 'NONE', #18665, 1000.000000000000000 ) ;
#27048=DIRECTION ( 'NONE',  ( -1.836970198721029934E-16, 1.836970198721036344E-16, -1.000000000000000000 ) ) ;
#27049=VERTEX_POINT ( 'NONE', #1233 ) ;
#27053=ORIENTED_EDGE ( 'NONE', *, *, #29216, .T. ) ;
#27056=ORIENTED_EDGE ( 'NONE', *, *, #4736, .F. ) ;
#27062=VECTOR ( 'NONE', #39422, 1000.000000000000000 ) ;
#27065=LINE ( 'NONE', #33745, #16666 ) ;
#27072=ORIENTED_EDGE ( 'NONE', *, *, #60505, .T. ) ;
#27077=VERTEX_POINT ( 'NONE', #45386 ) ;
#27079=CARTESIAN_POINT ( 'NONE',  ( -9.390476262117259054, 1.466476262117183627, 54.00000000000000711 ) ) ;
#27083=DIRECTION ( 'NONE',  ( -0.000000000000000000, -0.000000000000000000, -1.000000000000000000 ) ) ;
#27086=CIRCLE ( 'NONE', #29182, 1.224999999999997868 ) ;
#27088=ADVANCED_FACE ( 'NONE', ( #12852 ), #34417, .F. ) ;
#27090=EDGE_CURVE ( 'NONE', #47795, #55063, #65916, .T. ) ;
#27091=ORIENTED_EDGE ( 'NONE', *, *, #20637, .F. ) ;
#27096=CARTESIAN_POINT ( 'NONE',  ( 9.912023737882815766, -6.832023737882823688, 54.00000000000000711 ) ) ;
#27099=LINE ( 'NONE', #10831, #34334 ) ;
#27110=EDGE_LOOP ( 'NONE', ( #20931, #27293, #32452, #28777 ) ) ;
#27113=VERTEX_POINT ( 'NONE', #58481 ) ;
#27115=CARTESIAN_POINT ( 'NONE',  ( -5.242976262117259978, 5.242976262117182706, 54.00000000000000711 ) ) ;
#27133=ORIENTED_EDGE ( 'NONE', *, *, #22521, .T. ) ;
#27135=DIRECTION ( 'NONE',  ( -0.000000000000000000, 3.673940397442059868E-16, -1.000000000000000000 ) ) ;
#27146=CARTESIAN_POINT ( 'NONE',  ( -8.697938382363098242, -2.420780051175094094, 26.00000000000000711 ) ) ;
#27150=ORIENTED_EDGE ( 'NONE', *, *, #52170, .T. ) ;
#27154=VECTOR ( 'NONE', #26498, 1000.000000000000000 ) ;
#27179=DIRECTION ( 'NONE',  ( -1.000000000000000000, 1.610765207321970913E-14, 1.836970198721059516E-16 ) ) ;
#27182=CARTESIAN_POINT ( 'NONE',  ( -9.547976262117222390, -2.369523737882729186, 54.00000000000000711 ) ) ;
#27187=EDGE_CURVE ( 'NONE', #56499, #15565, #8609, .T. ) ;
#27194=DIRECTION ( 'NONE',  ( -1.000000000000000000, 0.000000000000000000, 0.000000000000000000 ) ) ;
#27198=CYLINDRICAL_SURFACE ( 'NONE', #26443, 0.1749999999999980738 ) ;
#27201=VECTOR ( 'NONE', #18527, 1000.000000000000000 ) ;
#27213=EDGE_CURVE ( 'NONE', #62873, #56266, #22108, .T. ) ;
#27218=VERTEX_POINT ( 'NONE', #19925 ) ;
#27224=CARTESIAN_POINT ( 'NONE',  ( 9.562023737882759278, 2.355476262117158104, 26.00000000000000711 ) ) ;
#27226=CARTESIAN_POINT ( 'NONE',  ( -7.517976262117294084, -6.665817930929260449, 54.00000000000000711 ) ) ;
#27227=ORIENTED_EDGE ( 'NONE', *, *, #40773, .F. ) ;
#27230=DIRECTION ( 'NONE',  ( 0.7071067811865527908, 0.7071067811865422437, 2.597868168706460875E-16 ) ) ;
#27243=DIRECTION ( 'NONE',  ( -0.8660254037844358210, 0.5000000000000049960, 2.509347957447882735E-16 ) ) ;
#27250=LINE ( 'NONE', #26905, #39529 ) ;
#27273=VECTOR ( 'NONE', #50237, 1000.000000000000000 ) ;
#27277=CARTESIAN_POINT ( 'NONE',  ( -6.822336235477446387, 4.135079735113101229, 54.00000000000000711 ) ) ;
#27280=DIRECTION ( 'NONE',  ( -0.6414496315691494699, -0.7671651518153064231, -0.000000000000000000 ) ) ;
#27284=DIRECTION ( 'NONE',  ( -0.7671651518153006499, -0.6414496315691565753, 0.000000000000000000 ) ) ;
#27286=CARTESIAN_POINT ( 'NONE',  ( 3.157023737882797665, 4.031976262117209053, 54.00000000000000711 ) ) ;
#27293=ORIENTED_EDGE ( 'NONE', *, *, #20059, .F. ) ;
#27302=CARTESIAN_POINT ( 'NONE',  ( -0.9414762621172249046, 9.915476262117151052, 26.00000000000000711 ) ) ;
#27312=DIRECTION ( 'NONE',  ( -0.000000000000000000, -0.000000000000000000, -1.000000000000000000 ) ) ;
#27318=DIRECTION ( 'NONE',  ( -0.000000000000000000, -0.000000000000000000, -1.000000000000000000 ) ) ;
#27324=ORIENTED_EDGE ( 'NONE', *, *, #46603, .F. ) ;
#27331=EDGE_CURVE ( 'NONE', #12520, #47907, #26283, .T. ) ;
#27339=ORIENTED_EDGE ( 'NONE', *, *, #69272, .F. ) ;
#27343=ORIENTED_EDGE ( 'NONE', *, *, #28619, .T. ) ;
#27357=CARTESIAN_POINT ( 'NONE',  ( 3.857023737882779635, -10.31452373788280141, 26.00000000000000000 ) ) ;
#27360=CARTESIAN_POINT ( 'NONE',  ( -5.242976262117280406, -5.257023737882805747, 54.00000000000000711 ) ) ;
#27368=DIRECTION ( 'NONE',  ( -1.000000000000000000, 0.000000000000000000, 0.000000000000000000 ) ) ;
#27374=ORIENTED_EDGE ( 'NONE', *, *, #38535, .T. ) ;
#27383=CARTESIAN_POINT ( 'NONE',  ( 8.144523737882812142, 8.821682069070710952, 54.00000000000000711 ) ) ;
#27397=EDGE_CURVE ( 'NONE', #17943, #67681, #29389, .T. ) ;
#27400=VERTEX_POINT ( 'NONE', #49582 ) ;
#27401=CARTESIAN_POINT ( 'NONE',  ( -2.989207322240185594, 6.858227778582772771, 26.00000000000000711 ) ) ;
#27406=CARTESIAN_POINT ( 'NONE',  ( 8.835729544836338434, -2.369523737882826886, 54.00000000000000711 ) ) ;
#27409=EDGE_CURVE ( 'NONE', #15324, #59398, #66189, .T. ) ;
#27412=CARTESIAN_POINT ( 'NONE',  ( -8.566576262117358453, -9.703773737882738004, 54.00000000000000711 ) ) ;
#27421=VERTEX_POINT ( 'NONE', #28350 ) ;
#27425=DIRECTION ( 'NONE',  ( 0.000000000000000000, 1.000000000000000000, 0.000000000000000000 ) ) ;
#27428=DIRECTION ( 'NONE',  ( 1.000000000000000000, -0.000000000000000000, 0.000000000000000000 ) ) ;
#27429=CARTESIAN_POINT ( 'NONE',  ( 6.501044194225490180, -2.632023737882825287, 54.00000000000000711 ) ) ;
#27436=CARTESIAN_POINT ( 'NONE',  ( 8.612468434717182930, 1.466476262117163865, 54.00000000000000711 ) ) ;
#27439=PLANE ( 'NONE',  #41739 ) ;
#27440=CARTESIAN_POINT ( 'NONE',  ( 9.703773737882810835, 8.916576262117189344, 26.00000000000000711 ) ) ;
#27443=ADVANCED_FACE ( 'NONE', ( #23744 ), #7819, .F. ) ;
#27459=DIRECTION ( 'NONE',  ( -1.000000000000000000, 0.000000000000000000, 0.000000000000000000 ) ) ;
#27467=AXIS2_PLACEMENT_3D ( 'NONE', #61054, #18269, #12265 ) ;
#27468=VERTEX_POINT ( 'NONE', #44600 ) ;
#27470=ORIENTED_EDGE ( 'NONE', *, *, #46084, .F. ) ;
#27475=ORIENTED_EDGE ( 'NONE', *, *, #7650, .T. ) ;
#27483=VECTOR ( 'NONE', #69234, 1000.000000000000000 ) ;
#27488=CARTESIAN_POINT ( 'NONE',  ( -2.406732575409671337, -8.711985858128709737, 54.00000000000000711 ) ) ;
#27490=ORIENTED_EDGE ( 'NONE', *, *, #14800, .T. ) ;
#27492=ORIENTED_EDGE ( 'NONE', *, *, #13965, .T. ) ;
#27495=VERTEX_POINT ( 'NONE', #57669 ) ;
#27496=CARTESIAN_POINT ( 'NONE',  ( -9.390476262117209316, -1.480523737882732060, 54.00000000000000711 ) ) ;
#27497=DIRECTION ( 'NONE',  ( 0.7071067811865474617, -0.7071067811865474617, 0.000000000000000000 ) ) ;
#27505=FACE_OUTER_BOUND ( 'NONE', #55791, .T. ) ;
#27506=CARTESIAN_POINT ( 'NONE',  ( 3.677663764522620671, 4.135079735113112775, 54.00000000000000711 ) ) ;
#27516=DIRECTION ( 'NONE',  ( -0.7071067811865401342, 0.7071067811865550112, 1.355854680848613865E-30 ) ) ;
#27530=ORIENTED_EDGE ( 'NONE', *, *, #19469, .F. ) ;
#27536=DIRECTION ( 'NONE',  ( -0.8660254037844358210, 0.5000000000000049960, 2.509347957447882735E-16 ) ) ;
#27540=ORIENTED_EDGE ( 'NONE', *, *, #21550, .T. ) ;
#27546=CYLINDRICAL_SURFACE ( 'NONE', #29898, 0.5249999999999994671 ) ;
#27548=ORIENTED_EDGE ( 'NONE', *, *, #12459, .T. ) ;
#27560=CARTESIAN_POINT ( 'NONE',  ( 5.257023737882801306, 5.242976262117200470, 54.00000000000000711 ) ) ;
#27564=VECTOR ( 'NONE', #68202, 1000.000000000000000 ) ;
#27580=CARTESIAN_POINT ( 'NONE',  ( 4.720772854004774643, -6.358413763958961518, 26.00000000000000711 ) ) ;
#27590=CARTESIAN_POINT ( 'NONE',  ( -6.350872789121327244, 3.663616288756986084, 54.00000000000000711 ) ) ;
#27591=VERTEX_POINT ( 'NONE', #14184 ) ;
#27595=AXIS2_PLACEMENT_3D ( 'NONE', #23599, #44817, #34198 ) ;
#27597=DIRECTION ( 'NONE',  ( -0.000000000000000000, 3.673940397442059868E-16, -1.000000000000000000 ) ) ;
#27601=DIRECTION ( 'NONE',  ( 1.836970198721029934E-16, 1.836970198721010706E-16, -1.000000000000000000 ) ) ;
#27604=CARTESIAN_POINT ( 'NONE',  ( -10.03972626211722918, 9.689726262117183353, 54.00000000000000711 ) ) ;
#27605=ORIENTED_EDGE ( 'NONE', *, *, #3313, .T. ) ;
#27606=VECTOR ( 'NONE', #17174, 1000.000000000000000 ) ;
#27607=VECTOR ( 'NONE', #62332, 1000.000000000000000 ) ;
#27623=LINE ( 'NONE', #42498, #22565 ) ;
#27630=EDGE_CURVE ( 'NONE', #45832, #6981, #65550, .T. ) ;
#27660=CARTESIAN_POINT ( 'NONE',  ( 6.849523737882814878, 10.49297626211720136, 26.00000000000000711 ) ) ;
#27663=VECTOR ( 'NONE', #17289, 1000.000000000000000 ) ;
#27665=LINE ( 'NONE', #43577, #30906 ) ;
#27670=VECTOR ( 'NONE', #27318, 1000.000000000000000 ) ;
#27674=ADVANCED_FACE ( 'NONE', ( #64722 ), #49155, .F. ) ;
#27677=VECTOR ( 'NONE', #11747, 1000.000000000000000 ) ;
#27689=LINE ( 'NONE', #49267, #59323 ) ;
#27708=EDGE_CURVE ( 'NONE', #44931, #65973, #27250, .T. ) ;
#27709=ORIENTED_EDGE ( 'NONE', *, *, #36256, .T. ) ;
#27711=LINE ( 'NONE', #65209, #1473 ) ;
#27717=DIRECTION ( 'NONE',  ( -0.7071067811865401342, 0.7071067811865550112, 1.367410260514937456E-30 ) ) ;
#27723=LINE ( 'NONE', #48948, #20443 ) ;
#27728=FACE_OUTER_BOUND ( 'NONE', #7792, .T. ) ;
#27729=VERTEX_POINT ( 'NONE', #54123 ) ;
#27732=CARTESIAN_POINT ( 'NONE',  ( 6.832023737882818359, -9.912023737882819319, 54.00000000000000711 ) ) ;
#27733=EDGE_LOOP ( 'NONE', ( #20693, #24819, #65274, #23608 ) ) ;
#27738=CYLINDRICAL_SURFACE ( 'NONE', #11742, 0.1749999999999998224 ) ;
#27743=DIRECTION ( 'NONE',  ( -0.000000000000000000, -0.000000000000000000, -1.000000000000000000 ) ) ;
#27745=VECTOR ( 'NONE', #43805, 1000.000000000000227 ) ;
#27757=VECTOR ( 'NONE', #38399, 1000.000000000000000 ) ;
#27765=VECTOR ( 'NONE', #5037, 1000.000000000000114 ) ;
#27768=AXIS2_PLACEMENT_3D ( 'NONE', #38122, #59673, #65334 ) ;
#27778=DIRECTION ( 'NONE',  ( 1.836970198721029934E-16, 1.836970198721010706E-16, -1.000000000000000000 ) ) ;
#27779=CARTESIAN_POINT ( 'NONE',  ( 10.50702373788281996, -3.664523737882826815, 54.00000000000000711 ) ) ;
#27783=DIRECTION ( 'NONE',  ( 0.000000000000000000, -1.000000000000000000, 0.000000000000000000 ) ) ;
#27787=VECTOR ( 'NONE', #6203, 1000.000000000000000 ) ;
#27790=DIRECTION ( 'NONE',  ( 1.836970198721029934E-16, 1.836970198721010706E-16, -1.000000000000000000 ) ) ;
#27792=CARTESIAN_POINT ( 'NONE',  ( -5.538810540050059572, -7.357023737882796510, 26.00000000000000711 ) ) ;
#27793=CARTESIAN_POINT ( 'NONE',  ( -8.916576262117258622, 9.689726262117185129, 54.00000000000000711 ) ) ;
#27795=EDGE_CURVE ( 'NONE', #38364, #19298, #28963, .T. ) ;
#27803=ORIENTED_EDGE ( 'NONE', *, *, #48435, .F. ) ;
#27804=AXIS2_PLACEMENT_3D ( 'NONE', #55530, #41251, #17698 ) ;
#27807=ORIENTED_EDGE ( 'NONE', *, *, #34234, .T. ) ;
#27808=EDGE_CURVE ( 'NONE', #7626, #65138, #39562, .T. ) ;
#27810=CARTESIAN_POINT ( 'NONE',  ( 10.31452373788281562, -6.657023737882825642, 54.00000000000000711 ) ) ;
#27813=AXIS2_PLACEMENT_3D ( 'NONE', #14955, #44746, #61009 ) ;
#27817=AXIS2_PLACEMENT_3D ( 'NONE', #3401, #13648, #56782 ) ;
#27820=EDGE_LOOP ( 'NONE', ( #59735, #32868, #37501, #30445 ) ) ;
#27822=ORIENTED_EDGE ( 'NONE', *, *, #68278, .F. ) ;
#27825=DIRECTION ( 'NONE',  ( -0.000000000000000000, -0.000000000000000000, -1.000000000000000000 ) ) ;
#27849=AXIS2_PLACEMENT_3D ( 'NONE', #39921, #61140, #12701 ) ;
#27853=AXIS2_PLACEMENT_3D ( 'NONE', #61878, #46304, #35328 ) ;
#27864=CARTESIAN_POINT ( 'NONE',  ( 5.257023737882803083, 7.172176262117205603, 26.00000000000000711 ) ) ;
#27867=ORIENTED_EDGE ( 'NONE', *, *, #24149, .F. ) ;
#27872=VECTOR ( 'NONE', #13845, 1000.000000000000000 ) ;
#27874=DIRECTION ( 'NONE',  ( -0.5000000000000004441, 0.8660254037844383745, 3.181725716174720005E-16 ) ) ;
#27875=DIRECTION ( 'NONE',  ( 0.000000000000000000, 0.000000000000000000, 1.000000000000000000 ) ) ;
#27878=CARTESIAN_POINT ( 'NONE',  ( 2.369523737882817116, 9.547976262117204627, 54.00000000000000711 ) ) ;
#27881=DIRECTION ( 'NONE',  ( -0.6414496315691473605, -0.7671651518153083105, -2.309356642089130002E-17 ) ) ;
#27882=DIRECTION ( 'NONE',  ( -1.836970198721029934E-16, -1.836970198721010706E-16, 1.000000000000000000 ) ) ;
#27883=CARTESIAN_POINT ( 'NONE',  ( -9.390476262117200434, -0.9555237378827314831, 54.00000000000000711 ) ) ;
#27890=EDGE_CURVE ( 'NONE', #28088, #16593, #45565, .T. ) ;
#27891=DIRECTION ( 'NONE',  ( -0.000000000000000000, 3.673940397442059868E-16, -1.000000000000000000 ) ) ;
#27895=CYLINDRICAL_SURFACE ( 'NONE', #20129, 0.1749999999999998224 ) ;
#27899=AXIS2_PLACEMENT_3D ( 'NONE', #29584, #13328, #2374 ) ;
#27902=EDGE_CURVE ( 'NONE', #40018, #42074, #8080, .T. ) ;
#27913=CARTESIAN_POINT ( 'NONE',  ( 6.832023737882818359, -9.737023737882811503, 26.00000000000000000 ) ) ;
#27914=VECTOR ( 'NONE', #52930, 1000.000000000000000 ) ;
#27916=LINE ( 'NONE', #1049, #5075 ) ;
#27922=DIRECTION ( 'NONE',  ( 0.6414496315691484707, -0.7671651518153074223, 0.000000000000000000 ) ) ;
#27927=DIRECTION ( 'NONE',  ( -1.000000000000000000, 0.000000000000000000, 0.000000000000000000 ) ) ;
#27929=VERTEX_POINT ( 'NONE', #19054 ) ;
#27937=CIRCLE ( 'NONE', #36994, 1.929199999999997139 ) ;
#27943=EDGE_CURVE ( 'NONE', #45109, #114, #57670, .T. ) ;
#27960=DIRECTION ( 'NONE',  ( 1.836970198721029934E-16, -1.836970198721036344E-16, 1.000000000000000000 ) ) ;
#27965=ADVANCED_FACE ( 'NONE', ( #13396 ), #61845, .F. ) ;
#27970=DIRECTION ( 'NONE',  ( 0.5000000000000068834, 0.8660254037844345998, 6.723777587268309839E-17 ) ) ;
#27978=EDGE_CURVE ( 'NONE', #10363, #21898, #57237, .T. ) ;
#27984=DIRECTION ( 'NONE',  ( -0.000000000000000000, 3.673940397442059868E-16, -1.000000000000000000 ) ) ;
#27997=DIRECTION ( 'NONE',  ( -1.000000000000000000, 0.000000000000000000, 0.000000000000000000 ) ) ;
#28007=VECTOR ( 'NONE', #60396, 1000.000000000000000 ) ;
#28010=EDGE_CURVE ( 'NONE', #48863, #50286, #10285, .T. ) ;
#28016=CARTESIAN_POINT ( 'NONE',  ( -9.897976262117287760, -6.832023737882751746, 26.00000000000000000 ) ) ;
#28018=ADVANCED_FACE ( 'NONE', ( #25413 ), #46974, .F. ) ;
#28024=AXIS2_PLACEMENT_3D ( 'NONE', #5178, #27778, #930 ) ;
#28030=PLANE ( 'NONE',  #28721 ) ;
#28038=CARTESIAN_POINT ( 'NONE',  ( -4.135079735113167843, 6.822336235477362010, 26.00000000000000711 ) ) ;
#28045=FACE_OUTER_BOUND ( 'NONE', #42455, .T. ) ;
#28047=ADVANCED_FACE ( 'NONE', ( #53690 ), #37084, .T. ) ;
#28048=VERTEX_POINT ( 'NONE', #4898 ) ;
#28057=EDGE_CURVE ( 'NONE', #50773, #48157, #11829, .T. ) ;
#28061=ADVANCED_FACE ( 'NONE', ( #22800 ), #58985, .F. ) ;
#28062=VECTOR ( 'NONE', #550, 1000.000000000000000 ) ;
#28065=VERTEX_POINT ( 'NONE', #917 ) ;
#28070=VERTEX_POINT ( 'NONE', #42022 ) ;
#28071=DIRECTION ( 'NONE',  ( -0.5000000000000129896, -0.8660254037844311581, -2.509347957447868930E-16 ) ) ;
#28072=ORIENTED_EDGE ( 'NONE', *, *, #25632, .F. ) ;
#28077=DIRECTION ( 'NONE',  ( -1.000000000000000000, 0.000000000000000000, 0.000000000000000000 ) ) ;
#28086=DIRECTION ( 'NONE',  ( 1.836970198721029934E-16, 1.836970198721010706E-16, -1.000000000000000000 ) ) ;
#28088=VERTEX_POINT ( 'NONE', #15853 ) ;
#28097=ORIENTED_EDGE ( 'NONE', *, *, #8756, .T. ) ;
#28102=EDGE_CURVE ( 'NONE', #9312, #2345, #62361, .T. ) ;
#28107=ORIENTED_EDGE ( 'NONE', *, *, #20801, .T. ) ;
#28108=AXIS2_PLACEMENT_3D ( 'NONE', #56029, #66630, #18183 ) ;
#28110=CARTESIAN_POINT ( 'NONE',  ( -8.916576262117345664, -8.580623737882765667, 54.00000000000000711 ) ) ;
#28114=VERTEX_POINT ( 'NONE', #18893 ) ;
#28115=PLANE ( 'NONE',  #54065 ) ;
#28116=VECTOR ( 'NONE', #44119, 999.9999999999998863 ) ;
#28130=DIRECTION ( 'NONE',  ( -8.540177112501197482E-15, -1.000000000000000000, -3.673940397442059868E-16 ) ) ;
#28136=EDGE_LOOP ( 'NONE', ( #68774, #61604, #43915, #36397 ) ) ;
#28159=DIRECTION ( 'NONE',  ( 2.478176394252584099E-15, 1.000000000000000000, 0.000000000000000000 ) ) ;
#28161=DIRECTION ( 'NONE',  ( -1.062075597536822467E-14, -1.000000000000000000, 0.000000000000000000 ) ) ;
#28168=VERTEX_POINT ( 'NONE', #24550 ) ;
#28172=DIRECTION ( 'NONE',  ( -0.7071067811865451302, 0.7071067811865500152, 0.000000000000000000 ) ) ;
#28188=EDGE_CURVE ( 'NONE', #5949, #19358, #22696, .T. ) ;
#28191=AXIS2_PLACEMENT_3D ( 'NONE', #12736, #66842, #35348 ) ;
#28196=ORIENTED_EDGE ( 'NONE', *, *, #21040, .F. ) ;
#28209=AXIS2_PLACEMENT_3D ( 'NONE', #46742, #40745, #57707 ) ;
#28236=CARTESIAN_POINT ( 'NONE',  ( 4.720772854004774643, -6.358413763958971288, 54.00000000000000711 ) ) ;
#28240=CARTESIAN_POINT ( 'NONE',  ( 8.241237374594303944, -1.634292677759888068, 54.00000000000000711 ) ) ;
#28241=CARTESIAN_POINT ( 'NONE',  ( 2.544523737882812053, 9.547976262117211732, 26.00000000000000711 ) ) ;
#28243=LINE ( 'NONE', #33884, #30994 ) ;
#28261=ORIENTED_EDGE ( 'NONE', *, *, #60476, .T. ) ;
#28267=DIRECTION ( 'NONE',  ( -1.836970198721029934E-16, 1.836970198721036590E-16, -1.000000000000000000 ) ) ;
#28268=DIRECTION ( 'NONE',  ( 0.000000000000000000, -1.000000000000000000, 0.000000000000000000 ) ) ;
#28278=DIRECTION ( 'NONE',  ( -1.836970198721029934E-16, -1.836970198721010706E-16, 1.000000000000000000 ) ) ;
#28283=CARTESIAN_POINT ( 'NONE',  ( 4.961189459950039904, -7.357023737882821379, 54.00000000000000711 ) ) ;
#28284=PLANE ( 'NONE',  #64427 ) ;
#28287=CARTESIAN_POINT ( 'NONE',  ( 9.404523737882753309, 1.466476262117160312, 26.00000000000000711 ) ) ;
#28291=ORIENTED_EDGE ( 'NONE', *, *, #67802, .F. ) ;
#28298=DIRECTION ( 'NONE',  ( 1.836970198721029934E-16, -1.836970198721036344E-16, 1.000000000000000000 ) ) ;
#28309=ORIENTED_EDGE ( 'NONE', *, *, #23393, .F. ) ;
#28314=DIRECTION ( 'NONE',  ( 1.000000000000000000, -3.491481338843133750E-15, -1.836970198721036590E-16 ) ) ;
#28330=ORIENTED_EDGE ( 'NONE', *, *, #61218, .T. ) ;
#28339=PLANE ( 'NONE',  #29688 ) ;
#28341=ORIENTED_EDGE ( 'NONE', *, *, #64372, .T. ) ;
#28349=CARTESIAN_POINT ( 'NONE',  ( 3.857023737882817827, 10.30047626211720413, 54.00000000000000711 ) ) ;
#28350=CARTESIAN_POINT ( 'NONE',  ( 7.357023737882817827, -5.552858015815577808, 26.00000000000000711 ) ) ;
#28351=ORIENTED_EDGE ( 'NONE', *, *, #22135, .F. ) ;
#28361=FACE_OUTER_BOUND ( 'NONE', #41046, .T. ) ;
#28362=DIRECTION ( 'NONE',  ( 0.000000000000000000, 0.000000000000000000, 1.000000000000000000 ) ) ;
#28367=CARTESIAN_POINT ( 'NONE',  ( -6.817976262117261044, 9.722976262117182245, 54.00000000000000711 ) ) ;
#28373=ORIENTED_EDGE ( 'NONE', *, *, #65943, .F. ) ;
#28375=DIRECTION ( 'NONE',  ( 1.000000000000000000, 0.000000000000000000, 0.000000000000000000 ) ) ;
#28383=DIRECTION ( 'NONE',  ( 1.000000000000000000, -7.304098846218132892E-15, -2.683482381803073952E-30 ) ) ;
#28391=EDGE_LOOP ( 'NONE', ( #27072, #33026, #69957, #52102 ) ) ;
#28392=DIRECTION ( 'NONE',  ( -3.491481338843133355E-15, -1.000000000000000000, -1.836970198721029934E-16 ) ) ;
#28394=VECTOR ( 'NONE', #34301, 1000.000000000000000 ) ;
#28396=ORIENTED_EDGE ( 'NONE', *, *, #32117, .F. ) ;
#28404=AXIS2_PLACEMENT_3D ( 'NONE', #16671, #9975, #37195 ) ;
#28405=DIRECTION ( 'NONE',  ( 1.047444401652940007E-14, 1.000000000000000000, 0.000000000000000000 ) ) ;
#28408=ORIENTED_EDGE ( 'NONE', *, *, #55649, .T. ) ;
#28409=ORIENTED_EDGE ( 'NONE', *, *, #64737, .F. ) ;
#28411=EDGE_CURVE ( 'NONE', #29645, #37690, #4397, .T. ) ;
#28415=LINE ( 'NONE', #13203, #49594 ) ;
#28417=DIRECTION ( 'NONE',  ( 1.836970198721029934E-16, 1.836970198721010706E-16, -1.000000000000000000 ) ) ;
#28418=ORIENTED_EDGE ( 'NONE', *, *, #64919, .T. ) ;
#28419=ORIENTED_EDGE ( 'NONE', *, *, #31386, .F. ) ;
#28421=ORIENTED_EDGE ( 'NONE', *, *, #47053, .T. ) ;
#28427=ORIENTED_EDGE ( 'NONE', *, *, #3176, .F. ) ;
#28433=PRODUCT_DEFINITION_SHAPE ( 'NONE', 'NONE',  #34822 ) ;
#28438=VERTEX_POINT ( 'NONE', #49259 ) ;
#28440=VECTOR ( 'NONE', #14765, 1000.000000000000000 ) ;
#28448=LINE ( 'NONE', #1576, #12845 ) ;
#28450=VERTEX_POINT ( 'NONE', #64482 ) ;
#28454=DIRECTION ( 'NONE',  ( -1.047444401652940007E-14, -1.000000000000000000, 0.000000000000000000 ) ) ;
#28458=DIRECTION ( 'NONE',  ( 1.836970198721029934E-16, 1.836970198721010706E-16, -1.000000000000000000 ) ) ;
#28460=DIRECTION ( 'NONE',  ( -1.000000000000000000, 0.000000000000000000, 0.000000000000000000 ) ) ;
#28462=CARTESIAN_POINT ( 'NONE',  ( 9.703773737882785966, -8.580623737882856261, 54.00000000000000711 ) ) ;
#28477=VERTEX_POINT ( 'NONE', #48220 ) ;
#28478=EDGE_CURVE ( 'NONE', #26351, #41781, #38548, .T. ) ;
#28491=ORIENTED_EDGE ( 'NONE', *, *, #58145, .T. ) ;
#28497=AXIS2_PLACEMENT_3D ( 'NONE', #46845, #25286, #9731 ) ;
#28506=VECTOR ( 'NONE', #3578, 1000.000000000000000 ) ;
#28508=EDGE_CURVE ( 'NONE', #7626, #4514, #64550, .T. ) ;
#28511=CARTESIAN_POINT ( 'NONE',  ( -8.079219948824906794, 8.697938382363059162, 26.00000000000000711 ) ) ;
#28513=DIRECTION ( 'NONE',  ( -1.000000000000000000, 8.540177112501197482E-15, 3.137610169492823463E-30 ) ) ;
#28520=VERTEX_POINT ( 'NONE', #32299 ) ;
#28527=EDGE_CURVE ( 'NONE', #10161, #29039, #2529, .T. ) ;
#28532=ORIENTED_EDGE ( 'NONE', *, *, #25327, .T. ) ;
#28533=VECTOR ( 'NONE', #46688, 1000.000000000000000 ) ;
#28535=FACE_OUTER_BOUND ( 'NONE', #58567, .T. ) ;
#28544=LINE ( 'NONE', #59356, #20243 ) ;
#28545=PLANE ( 'NONE',  #3643 ) ;
#28548=AXIS2_PLACEMENT_3D ( 'NONE', #51886, #57187, #45513 ) ;
#28565=CARTESIAN_POINT ( 'NONE',  ( -3.667976262117227382, 9.897976262117168744, 54.00000000000000711 ) ) ;
#28566=ORIENTED_EDGE ( 'NONE', *, *, #52154, .F. ) ;
#28567=EDGE_CURVE ( 'NONE', #46469, #46340, #8180, .T. ) ;
#28572=DIRECTION ( 'NONE',  ( 1.000000000000000000, 0.000000000000000000, 0.000000000000000000 ) ) ;
#28573=FACE_OUTER_BOUND ( 'NONE', #34024, .T. ) ;
#28583=LINE ( 'NONE', #28932, #32469 ) ;
#28587=DIRECTION ( 'NONE',  ( -1.000000000000000000, 0.000000000000000000, 0.000000000000000000 ) ) ;
#28592=VERTEX_POINT ( 'NONE', #45308 ) ;
#28593=ORIENTED_EDGE ( 'NONE', *, *, #14971, .T. ) ;
#28619=EDGE_CURVE ( 'NONE', #66569, #13296, #12431, .T. ) ;
#28620=VERTEX_POINT ( 'NONE', #56631 ) ;
#28627=DIRECTION ( 'NONE',  ( 1.000000000000000000, 0.000000000000000000, 0.000000000000000000 ) ) ;
#28629=CARTESIAN_POINT ( 'NONE',  ( -3.663616288757086004, -4.149127210878724270, 26.00000000000000711 ) ) ;
#28631=DIRECTION ( 'NONE',  ( -1.000000000000000000, 0.000000000000000000, 0.000000000000000000 ) ) ;
#28634=FACE_OUTER_BOUND ( 'NONE', #37392, .T. ) ;
#28642=FACE_BOUND ( 'NONE', #39114, .T. ) ;
#28657=EDGE_CURVE ( 'NONE', #55692, #51462, #39998, .T. ) ;
#28670=DIRECTION ( 'NONE',  ( -1.836970198721029934E-16, -1.836970198721010706E-16, 1.000000000000000000 ) ) ;
#28678=ORIENTED_EDGE ( 'NONE', *, *, #47042, .T. ) ;
#28683=CARTESIAN_POINT ( 'NONE',  ( -2.530476262117229425, 9.547976262117158441, 26.00000000000000711 ) ) ;
#28686=ORIENTED_EDGE ( 'NONE', *, *, #2593, .T. ) ;
#28696=VECTOR ( 'NONE', #50813, 1000.000000000000114 ) ;
#28698=LINE ( 'NONE', #61560, #69658 ) ;
#28703=EDGE_CURVE ( 'NONE', #8535, #46756, #43133, .T. ) ;
#28721=AXIS2_PLACEMENT_3D ( 'NONE', #66874, #50628, #2188 ) ;
#28722=CARTESIAN_POINT ( 'NONE',  ( -5.242976262117280406, -5.257023737882805747, 54.00000000000000711 ) ) ;
#28723=AXIS2_PLACEMENT_3D ( 'NONE', #36077, #30076, #20869 ) ;
#28725=VERTEX_POINT ( 'NONE', #9960 ) ;
#28731=LINE ( 'NONE', #49951, #18053 ) ;
#28751=DIRECTION ( 'NONE',  ( -1.000000000000000000, -1.671920889371702854E-15, 0.000000000000000000 ) ) ;
#28754=VECTOR ( 'NONE', #57632, 1000.000000000000000 ) ;
#28756=EDGE_CURVE ( 'NONE', #57627, #25429, #31528, .T. ) ;
#28762=ADVANCED_FACE ( 'NONE', ( #41414 ), #68293, .F. ) ;
#28767=ORIENTED_EDGE ( 'NONE', *, *, #44448, .F. ) ;
#28771=ORIENTED_EDGE ( 'NONE', *, *, #69401, .F. ) ;
#28777=ORIENTED_EDGE ( 'NONE', *, *, #30226, .T. ) ;
#28780=CARTESIAN_POINT ( 'NONE',  ( 2.005523737882808355, 8.598420958951638937, 26.00000000000000711 ) ) ;
#28785=LINE ( 'NONE', #56024, #32314 ) ;
#28789=DIRECTION ( 'NONE',  ( -0.8660254037844510311, -0.4999999999999786282, 0.000000000000000000 ) ) ;
#28795=CARTESIAN_POINT ( 'NONE',  ( 6.849523737882817542, -10.50702373788282529, 54.00000000000000711 ) ) ;
#28797=EDGE_CURVE ( 'NONE', #41567, #2486, #58030, .T. ) ;
#28800=EDGE_LOOP ( 'NONE', ( #28678, #14874, #37565, #24944 ) ) ;
#28814=FACE_OUTER_BOUND ( 'NONE', #23381, .T. ) ;
#28816=EDGE_CURVE ( 'NONE', #63729, #59026, #19147, .T. ) ;
#28843=EDGE_LOOP ( 'NONE', ( #18417, #34125, #38422, #12249 ) ) ;
#28844=ORIENTED_EDGE ( 'NONE', *, *, #15039, .T. ) ;
#28847=CIRCLE ( 'NONE', #43611, 0.1749999999999998224 ) ;
#28851=ORIENTED_EDGE ( 'NONE', *, *, #10801, .F. ) ;
#28871=CARTESIAN_POINT ( 'NONE',  ( -6.822336235477441946, -4.149127210878692296, 26.00000000000000711 ) ) ;
#28875=PLANE ( 'NONE',  #47912 ) ;
#28876=LINE ( 'NONE', #50105, #64633 ) ;
#28880=VECTOR ( 'NONE', #5112, 1000.000000000000000 ) ;
#28886=DIRECTION ( 'NONE',  ( 1.836970198721029934E-16, 1.836970198721010706E-16, -1.000000000000000000 ) ) ;
#28893=EDGE_CURVE ( 'NONE', #86, #30798, #43159, .T. ) ;
#28901=EDGE_CURVE ( 'NONE', #68940, #11281, #64058, .T. ) ;
#28903=CARTESIAN_POINT ( 'NONE',  ( -3.650476262117223314, 10.30047626211716683, 54.00000000000000711 ) ) ;
#28906=DIRECTION ( 'NONE',  ( 0.7071067811865474617, 0.7071067811865474617, 0.000000000000000000 ) ) ;
#28907=AXIS2_PLACEMENT_3D ( 'NONE', #51762, #12854, #67669 ) ;
#28919=PLANE ( 'NONE',  #22459 ) ;
#28925=CARTESIAN_POINT ( 'NONE',  ( -4.141586236041100655, 4.706725378239165813, 54.00000000000000711 ) ) ;
#28927=VERTEX_POINT ( 'NONE', #383 ) ;
#28929=EDGE_CURVE ( 'NONE', #6044, #56509, #14881, .T. ) ;
#28932=CARTESIAN_POINT ( 'NONE',  ( -9.390476262117259054, 1.466476262117183182, 26.00000000000000711 ) ) ;
#28936=DIRECTION ( 'NONE',  ( 0.000000000000000000, -3.673940397442059868E-16, 1.000000000000000000 ) ) ;
#28940=FACE_OUTER_BOUND ( 'NONE', #55876, .T. ) ;
#28946=CIRCLE ( 'NONE', #42542, 0.1749999999999989342 ) ;
#28948=EDGE_LOOP ( 'NONE', ( #56256, #47201, #46419, #5012 ) ) ;
#28951=VECTOR ( 'NONE', #14457, 1000.000000000000000 ) ;
#28963=LINE ( 'NONE', #45215, #12420 ) ;
#28966=CIRCLE ( 'NONE', #36932, 0.1749999999999998224 ) ;
#28969=LINE ( 'NONE', #39911, #8084 ) ;
#28972=EDGE_LOOP ( 'NONE', ( #36939, #34860, #25834, #61465 ) ) ;
#28973=EDGE_CURVE ( 'NONE', #4514, #48863, #28974, .T. ) ;
#28974=LINE ( 'NONE', #61481, #65691 ) ;
#28983=DIRECTION ( 'NONE',  ( 1.836970198721029934E-16, 1.836970198721010706E-16, -1.000000000000000000 ) ) ;
#28985=ORIENTED_EDGE ( 'NONE', *, *, #28994, .T. ) ;
#28986=DIRECTION ( 'NONE',  ( -0.000000000000000000, 3.673940397442059868E-16, -1.000000000000000000 ) ) ;
#28991=LINE ( 'NONE', #45242, #60250 ) ;
#28994=EDGE_CURVE ( 'NONE', #9220, #44308, #54822, .T. ) ;
#28995=LINE ( 'NONE', #33945, #30066 ) ;
#28997=AXIS2_PLACEMENT_3D ( 'NONE', #12267, #18625, #34180 ) ;
#29003=ORIENTED_EDGE ( 'NONE', *, *, #10623, .F. ) ;
#29018=ADVANCED_FACE ( 'NONE', ( #24013 ), #22638, .F. ) ;
#29025=DIRECTION ( 'NONE',  ( 0.7071067811865474617, 0.7071067811865474617, 0.000000000000000000 ) ) ;
#29034=VERTEX_POINT ( 'NONE', #44189 ) ;
#29036=CARTESIAN_POINT ( 'NONE',  ( 7.357023737882817827, -3.848229544836346605, 54.00000000000000711 ) ) ;
#29039=VERTEX_POINT ( 'NONE', #12345 ) ;
#29044=CIRCLE ( 'NONE', #68588, 0.3499999999999996447 ) ;
#29052=VECTOR ( 'NONE', #26370, 1000.000000000000000 ) ;
#29055=ORIENTED_EDGE ( 'NONE', *, *, #5524, .F. ) ;
#29067=DIRECTION ( 'NONE',  ( -0.000000000000000000, -0.000000000000000000, -1.000000000000000000 ) ) ;
#29068=EDGE_CURVE ( 'NONE', #8035, #3393, #34263, .T. ) ;
#29069=EDGE_CURVE ( 'NONE', #42896, #22077, #45225, .T. ) ;
#29073=DIRECTION ( 'NONE',  ( -0.000000000000000000, 3.673940397442059868E-16, -1.000000000000000000 ) ) ;
#29079=CARTESIAN_POINT ( 'NONE',  ( -5.538810540050023157, 7.342976262117183239, 26.00000000000000711 ) ) ;
#29084=CYLINDRICAL_SURFACE ( 'NONE', #21188, 0.5249999999999999112 ) ;
#29085=DIRECTION ( 'NONE',  ( -0.000000000000000000, 3.673940397442059868E-16, -1.000000000000000000 ) ) ;
#29090=VECTOR ( 'NONE', #34025, 1000.000000000000000 ) ;
#29096=DIRECTION ( 'NONE',  ( 9.973078850062115052E-15, 1.000000000000000000, 1.836970198721028948E-16 ) ) ;
#29099=ORIENTED_EDGE ( 'NONE', *, *, #47160, .T. ) ;
#29100=DIRECTION ( 'NONE',  ( 0.7071067811865602293, 0.7071067811865348052, 2.597868168706465806E-16 ) ) ;
#29101=ORIENTED_EDGE ( 'NONE', *, *, #29374, .F. ) ;
#29106=LINE ( 'NONE', #25203, #12270 ) ;
#29117=VERTEX_POINT ( 'NONE', #52664 ) ;
#29120=DIRECTION ( 'NONE',  ( -0.7071067811865474617, -0.7071067811865474617, -2.597868168706479611E-16 ) ) ;
#29126=VERTEX_POINT ( 'NONE', #67857 ) ;
#29127=CARTESIAN_POINT ( 'NONE',  ( -6.467976262117258734, 5.242976262117182706, 26.00000000000000711 ) ) ;
#29130=ORIENTED_EDGE ( 'NONE', *, *, #51813, .F. ) ;
#29133=DIRECTION ( 'NONE',  ( -0.000000000000000000, -0.000000000000000000, -1.000000000000000000 ) ) ;
#29145=EDGE_CURVE ( 'NONE', #55686, #16950, #40974, .T. ) ;
#29153=FACE_OUTER_BOUND ( 'NONE', #27820, .T. ) ;
#29156=CARTESIAN_POINT ( 'NONE',  ( -6.486996718459908884, -3.157023737882779013, 26.00000000000000711 ) ) ;
#29157=EDGE_LOOP ( 'NONE', ( #66487, #30727, #49199, #45621 ) ) ;
#29160=FACE_OUTER_BOUND ( 'NONE', #14769, .T. ) ;
#29163=CARTESIAN_POINT ( 'NONE',  ( 10.31452373788281562, -6.849523737882814878, 26.00000000000000000 ) ) ;
#29164=PLANE ( 'NONE',  #60238 ) ;
#29170=DIRECTION ( 'NONE',  ( -1.836970198721029934E-16, 1.836970198721036590E-16, -1.000000000000000000 ) ) ;
#29178=ORIENTED_EDGE ( 'NONE', *, *, #46630, .T. ) ;
#29182=AXIS2_PLACEMENT_3D ( 'NONE', #32775, #38099, #28161 ) ;
#29192=VERTEX_POINT ( 'NONE', #68912 ) ;
#29204=CIRCLE ( 'NONE', #39406, 0.3499999999999996447 ) ;
#29212=ADVANCED_FACE ( 'NONE', ( #62906 ), #51951, .F. ) ;
#29213=DIRECTION ( 'NONE',  ( 1.000000000000000000, 0.000000000000000000, 0.000000000000000000 ) ) ;
#29216=EDGE_CURVE ( 'NONE', #46451, #51473, #20122, .T. ) ;
#29227=ORIENTED_EDGE ( 'NONE', *, *, #55078, .T. ) ;
#29233=CARTESIAN_POINT ( 'NONE',  ( -8.697938382363185283, -8.093267424590415260, 54.00000000000000711 ) ) ;
#29234=CARTESIAN_POINT ( 'NONE',  ( -8.916576262117260399, 8.566576262117216345, 54.00000000000000711 ) ) ;
#29235=CARTESIAN_POINT ( 'NONE',  ( 6.836383711243005479, -6.364920264886896994, 26.00000000000000711 ) ) ;
#29236=VECTOR ( 'NONE', #18100, 1000.000000000000000 ) ;
#29238=ORIENTED_EDGE ( 'NONE', *, *, #52986, .T. ) ;
#29241=VERTEX_POINT ( 'NONE', #56885 ) ;
#29259=DIRECTION ( 'NONE',  ( 1.088659024508174415E-14, 1.000000000000000000, 1.836970198721030674E-16 ) ) ;
#29263=ORIENTED_EDGE ( 'NONE', *, *, #65300, .F. ) ;
#29269=EDGE_LOOP ( 'NONE', ( #2060, #38184, #47303, #48262 ) ) ;
#29272=LINE ( 'NONE', #24691, #40099 ) ;
#29274=LINE ( 'NONE', #50849, #64748 ) ;
#29275=ORIENTED_EDGE ( 'NONE', *, *, #45909, .T. ) ;
#29280=AXIS2_PLACEMENT_3D ( 'NONE', #46145, #8309, #8673 ) ;
#29286=ADVANCED_FACE ( 'NONE', ( #5267 ), #53011, .F. ) ;
#29291=CARTESIAN_POINT ( 'NONE',  ( -3.842976262117324016, -9.912023737882812213, 26.00000000000000000 ) ) ;
#29293=ADVANCED_FACE ( 'NONE', ( #36736 ), #15173, .F. ) ;
#29295=ORIENTED_EDGE ( 'NONE', *, *, #10560, .T. ) ;
#29298=DIRECTION ( 'NONE',  ( -1.000000000000000000, 3.491481338843133355E-15, 1.836970198721036344E-16 ) ) ;
#29304=EDGE_CURVE ( 'NONE', #52054, #63857, #15866, .T. ) ;
#29307=DIRECTION ( 'NONE',  ( -1.073876437509453175E-14, -1.000000000000000000, 0.000000000000000000 ) ) ;
#29310=CARTESIAN_POINT ( 'NONE',  ( 3.848229544836330174, 7.517976262117205266, 54.00000000000000711 ) ) ;
#29312=DIRECTION ( 'NONE',  ( -9.050731179009442381E-15, -1.000000000000000000, 0.000000000000000000 ) ) ;
#29313=DIRECTION ( 'NONE',  ( 1.000000000000000000, -1.203165845134433084E-14, -1.836970198721051874E-16 ) ) ;
#29316=EDGE_CURVE ( 'NONE', #17328, #32965, #45385, .T. ) ;
#29317=VERTEX_POINT ( 'NONE', #37094 ) ;
#29322=CARTESIAN_POINT ( 'NONE',  ( 10.50702373788281285, 9.781776262117176657, 26.00000000000000711 ) ) ;
#29329=CARTESIAN_POINT ( 'NONE',  ( 8.144523737882815695, 9.547976262117185087, 54.00000000000000711 ) ) ;
#29332=DIRECTION ( 'NONE',  ( -1.047444401652940007E-14, -1.000000000000000000, -1.836970198721029934E-16 ) ) ;
#29341=PLANE ( 'NONE',  #49566 ) ;
#29347=EDGE_CURVE ( 'NONE', #35347, #39629, #10552, .T. ) ;
#29351=ORIENTED_EDGE ( 'NONE', *, *, #47815, .T. ) ;
#29357=LINE ( 'NONE', #7447, #66550 ) ;
#29363=LINE ( 'NONE', #18397, #39061 ) ;
#29366=LINE ( 'NONE', #50937, #50175 ) ;
#29368=ORIENTED_EDGE ( 'NONE', *, *, #64844, .F. ) ;
#29369=EDGE_CURVE ( 'NONE', #6930, #45407, #44442, .T. ) ;
#29371=ORIENTED_EDGE ( 'NONE', *, *, #15423, .T. ) ;
#29372=ORIENTED_EDGE ( 'NONE', *, *, #57417, .T. ) ;
#29373=VERTEX_POINT ( 'NONE', #17924 ) ;
#29374=EDGE_CURVE ( 'NONE', #4410, #6935, #55428, .T. ) ;
#29385=EDGE_CURVE ( 'NONE', #11645, #6322, #28876, .T. ) ;
#29389=LINE ( 'NONE', #12089, #19869 ) ;
#29394=DIRECTION ( 'NONE',  ( -0.000000000000000000, -0.000000000000000000, -1.000000000000000000 ) ) ;
#29405=AXIS2_PLACEMENT_3D ( 'NONE', #64941, #54681, #39099 ) ;
#29406=LINE ( 'NONE', #68296, #40683 ) ;
#29409=EDGE_CURVE ( 'NONE', #5287, #56170, #12261, .T. ) ;
#29410=VERTEX_POINT ( 'NONE', #39490 ) ;
#29415=DIRECTION ( 'NONE',  ( 0.000000000000000000, 3.673940397442059868E-16, -1.000000000000000000 ) ) ;
#29416=DIRECTION ( 'NONE',  ( -1.000000000000000000, 1.047444401652940007E-14, -1.836970198721010706E-16 ) ) ;
#29417=DIRECTION ( 'NONE',  ( -1.062075597536821205E-14, -1.000000000000000000, 0.000000000000000000 ) ) ;
#29426=PLANE ( 'NONE',  #52411 ) ;
#29432=CARTESIAN_POINT ( 'NONE',  ( -7.342976262117259623, 4.947141984184421304, 54.00000000000000711 ) ) ;
#29436=CARTESIAN_POINT ( 'NONE',  ( 10.31452373788281562, -6.657023737882825642, 54.00000000000000711 ) ) ;
#29440=VECTOR ( 'NONE', #2440, 1000.000000000000000 ) ;
#29442=ORIENTED_EDGE ( 'NONE', *, *, #19126, .T. ) ;
#29450=DIRECTION ( 'NONE',  ( 1.836970198721029934E-16, 1.836970198721010706E-16, -1.000000000000000000 ) ) ;
#29452=VECTOR ( 'NONE', #2817, 1000.000000000000000 ) ;
#29466=ADVANCED_FACE ( 'NONE', ( #28535 ), #1660, .F. ) ;
#29471=ORIENTED_EDGE ( 'NONE', *, *, #27090, .F. ) ;
#29473=EDGE_LOOP ( 'NONE', ( #14420, #40568, #74, #13170 ) ) ;
#29474=AXIS2_PLACEMENT_3D ( 'NONE', #9345, #57778, #30217 ) ;
#29496=DIRECTION ( 'NONE',  ( -1.836970198721029934E-16, 1.836970198721036590E-16, -1.000000000000000000 ) ) ;
#29498=CARTESIAN_POINT ( 'NONE',  ( 6.849523737882817542, -10.31452373788281207, 26.00000000000000000 ) ) ;
#29502=EDGE_CURVE ( 'NONE', #29645, #4880, #36294, .T. ) ;
#29508=EDGE_CURVE ( 'NONE', #25597, #32858, #29931, .T. ) ;
#29511=CARTESIAN_POINT ( 'NONE',  ( -6.486996718459931088, 3.142976262117182173, 26.00000000000000711 ) ) ;
#29523=DIRECTION ( 'NONE',  ( 4.121462285523435444E-16, 1.000000000000000000, 0.000000000000000000 ) ) ;
#29526=DIRECTION ( 'NONE',  ( 0.000000000000000000, 1.000000000000000000, 0.000000000000000000 ) ) ;
#29531=EDGE_CURVE ( 'NONE', #66948, #19393, #19325, .T. ) ;
#29534=VERTEX_POINT ( 'NONE', #30297 ) ;
#29536=VERTEX_POINT ( 'NONE', #30641 ) ;
#29544=LINE ( 'NONE', #55387, #8307 ) ;
#29545=LINE ( 'NONE', #51114, #7731 ) ;
#29554=ORIENTED_EDGE ( 'NONE', *, *, #25922, .F. ) ;
#29555=VECTOR ( 'NONE', #56409, 1000.000000000000000 ) ;
#29559=ORIENTED_EDGE ( 'NONE', *, *, #33224, .F. ) ;
#29560=PLANE ( 'NONE',  #36818 ) ;
#29568=CARTESIAN_POINT ( 'NONE',  ( -8.130476262117259267, 9.547976262117177981, 26.00000000000000711 ) ) ;
#29570=DIRECTION ( 'NONE',  ( 1.836970198721029934E-16, 1.836970198721010706E-16, -1.000000000000000000 ) ) ;
#29584=CARTESIAN_POINT ( 'NONE',  ( 10.50702373788280752, 6.835476262117182067, 54.00000000000000711 ) ) ;
#29592=DIRECTION ( 'NONE',  ( -1.000000000000000000, 0.000000000000000000, 0.000000000000000000 ) ) ;
#29594=DIRECTION ( 'NONE',  ( 1.836970198721029934E-16, 1.836970198721010706E-16, -1.000000000000000000 ) ) ;
#29600=LINE ( 'NONE', #45873, #18592 ) ;
#29618=ORIENTED_EDGE ( 'NONE', *, *, #44879, .T. ) ;
#29621=CARTESIAN_POINT ( 'NONE',  ( -7.605476262117257136, 9.722976262117180468, 54.00000000000000711 ) ) ;
#29625=EDGE_CURVE ( 'NONE', #25422, #10709, #46894, .T. ) ;
#29627=DIRECTION ( 'NONE',  ( 1.836970198721029934E-16, 1.836970198721010706E-16, -1.000000000000000000 ) ) ;
#29628=LINE ( 'NONE', #23979, #62641 ) ;
#29642=EDGE_LOOP ( 'NONE', ( #12466, #35189, #59695, #38591 ) ) ;
#29645=VERTEX_POINT ( 'NONE', #10127 ) ;
#29646=ORIENTED_EDGE ( 'NONE', *, *, #59378, .T. ) ;
#29647=CARTESIAN_POINT ( 'NONE',  ( -9.547976262117256141, 7.955476262117183062, 54.00000000000000711 ) ) ;
#29656=FACE_OUTER_BOUND ( 'NONE', #16152, .T. ) ;
#29658=ORIENTED_EDGE ( 'NONE', *, *, #66621, .F. ) ;
#29662=CARTESIAN_POINT ( 'NONE',  ( -8.566576262117358453, -9.703773737882738004, 54.00000000000000711 ) ) ;
#29663=AXIS2_PLACEMENT_3D ( 'NONE', #63682, #15238, #24792 ) ;
#29666=PLANE ( 'NONE',  #3435 ) ;
#29684=VERTEX_POINT ( 'NONE', #27079 ) ;
#29688=AXIS2_PLACEMENT_3D ( 'NONE', #55569, #7111, #12755 ) ;
#29703=FACE_OUTER_BOUND ( 'NONE', #31665, .T. ) ;
#29704=ORIENTED_EDGE ( 'NONE', *, *, #44932, .T. ) ;
#29725=AXIS2_PLACEMENT_3D ( 'NONE', #932, #15779, #16126 ) ;
#29736=ORIENTED_EDGE ( 'NONE', *, *, #33545, .F. ) ;
#29761=VECTOR ( 'NONE', #63127, 1000.000000000000000 ) ;
#29781=ORIENTED_EDGE ( 'NONE', *, *, #17259, .F. ) ;
#29789=ADVANCED_FACE ( 'NONE', ( #39755 ), #5867, .F. ) ;
#29803=CARTESIAN_POINT ( 'NONE',  ( -5.242976262117259978, 5.242976262117182706, 26.00000000000000711 ) ) ;
#29808=ORIENTED_EDGE ( 'NONE', *, *, #13275, .F. ) ;
#29811=EDGE_CURVE ( 'NONE', #50286, #20807, #1254, .T. ) ;
#29812=PLANE ( 'NONE',  #29815 ) ;
#29815=AXIS2_PLACEMENT_3D ( 'NONE', #63403, #53161, #68715 ) ;
#29823=ORIENTED_EDGE ( 'NONE', *, *, #30706, .T. ) ;
#29825=ORIENTED_EDGE ( 'NONE', *, *, #61458, .F. ) ;
#29835=PLANE ( 'NONE',  #66204 ) ;
#29837=ORIENTED_EDGE ( 'NONE', *, *, #13894, .F. ) ;
#29844=DIRECTION ( 'NONE',  ( 0.000000000000000000, -1.000000000000000000, -3.673940397442059868E-16 ) ) ;
#29848=VERTEX_POINT ( 'NONE', #60641 ) ;
#29849=VECTOR ( 'NONE', #25110, 1000.000000000000000 ) ;
#29850=PLANE ( 'NONE',  #49423 ) ;
#29851=EDGE_CURVE ( 'NONE', #61234, #18742, #12192, .T. ) ;
#29857=ORIENTED_EDGE ( 'NONE', *, *, #60280, .T. ) ;
#29869=VECTOR ( 'NONE', #64429, 1000.000000000000000 ) ;
#29883=LINE ( 'NONE', #55711, #49644 ) ;
#29886=AXIS2_PLACEMENT_3D ( 'NONE', #55136, #17634, #56172 ) ;
#29893=DIRECTION ( 'NONE',  ( -0.7671651518153105309, 0.6414496315691445849, 0.000000000000000000 ) ) ;
#29894=DIRECTION ( 'NONE',  ( -4.956352788505168198E-15, -1.000000000000000000, 0.000000000000000000 ) ) ;
#29898=AXIS2_PLACEMENT_3D ( 'NONE', #49115, #22929, #23275 ) ;
#29906=ORIENTED_EDGE ( 'NONE', *, *, #47501, .F. ) ;
#29911=VECTOR ( 'NONE', #42825, 1000.000000000000000 ) ;
#29915=ORIENTED_EDGE ( 'NONE', *, *, #28994, .F. ) ;
#29918=LINE ( 'NONE', #51498, #33755 ) ;
#29931=LINE ( 'NONE', #35220, #49981 ) ;
#29939=EDGE_CURVE ( 'NONE', #21386, #34404, #11615, .T. ) ;
#29947=EDGE_LOOP ( 'NONE', ( #55432, #62337, #294, #18659 ) ) ;
#29948=DIRECTION ( 'NONE',  ( -0.000000000000000000, -0.000000000000000000, -1.000000000000000000 ) ) ;
#29965=DIRECTION ( 'NONE',  ( -0.000000000000000000, 3.673940397442059868E-16, -1.000000000000000000 ) ) ;
#29966=VERTEX_POINT ( 'NONE', #8279 ) ;
#29971=AXIS2_PLACEMENT_3D ( 'NONE', #54035, #64625, #16185 ) ;
#29974=ORIENTED_EDGE ( 'NONE', *, *, #10796, .F. ) ;
#29978=CARTESIAN_POINT ( 'NONE',  ( -6.822336235477446387, 6.350872789121265072, 26.00000000000000711 ) ) ;
#29979=CARTESIAN_POINT ( 'NONE',  ( -8.697938382363179954, -8.093267424590409931, 26.00000000000000000 ) ) ;
#29988=CARTESIAN_POINT ( 'NONE',  ( -8.079219948824956532, -8.711985858128644011, 26.00000000000000000 ) ) ;
#29996=DIRECTION ( 'NONE',  ( -1.836970198721029934E-16, 1.836970198721036590E-16, -1.000000000000000000 ) ) ;
#30003=PLANE ( 'NONE',  #7446 ) ;
#30007=CARTESIAN_POINT ( 'NONE',  ( 1.634292677759874746, 8.227189898828697778, 54.00000000000000711 ) ) ;
#30037=EDGE_CURVE ( 'NONE', #22259, #18238, #38953, .T. ) ;
#30041=ORIENTED_EDGE ( 'NONE', *, *, #54161, .T. ) ;
#30046=PLANE ( 'NONE',  #61898 ) ;
#30048=ADVANCED_FACE ( 'NONE', ( #1468 ), #28339, .F. ) ;
#30057=AXIS2_PLACEMENT_3D ( 'NONE', #41627, #57886, #20757 ) ;
#30062=ORIENTED_EDGE ( 'NONE', *, *, #11357, .T. ) ;
#30066=VECTOR ( 'NONE', #29332, 1000.000000000000000 ) ;
#30076=DIRECTION ( 'NONE',  ( 0.000000000000000000, -3.673940397442059868E-16, 1.000000000000000000 ) ) ;
#30078=ORIENTED_EDGE ( 'NONE', *, *, #10475, .F. ) ;
#30081=VERTEX_POINT ( 'NONE', #50256 ) ;
#30083=EDGE_CURVE ( 'NONE', #167, #37419, #18421, .T. ) ;
#30087=CARTESIAN_POINT ( 'NONE',  ( -6.344366288193410419, 5.779227145995219139, 26.00000000000000711 ) ) ;
#30088=ORIENTED_EDGE ( 'NONE', *, *, #43547, .F. ) ;
#30089=ORIENTED_EDGE ( 'NONE', *, *, #59243, .F. ) ;
#30099=DIRECTION ( 'NONE',  ( 0.000000000000000000, -1.000000000000000000, 0.000000000000000000 ) ) ;
#30109=CARTESIAN_POINT ( 'NONE',  ( -9.722976262117239088, 7.290476262117218553, 26.00000000000000711 ) ) ;
#30112=DIRECTION ( 'NONE',  ( -1.349135440953254490E-14, -1.000000000000000000, 0.000000000000000000 ) ) ;
#30113=ORIENTED_EDGE ( 'NONE', *, *, #68823, .T. ) ;
#30127=DIRECTION ( 'NONE',  ( -0.000000000000000000, -0.000000000000000000, -1.000000000000000000 ) ) ;
#30128=EDGE_CURVE ( 'NONE', #2608, #43786, #390, .T. ) ;
#30147=LINE ( 'NONE', #19528, #37713 ) ;
#30153=EDGE_LOOP ( 'NONE', ( #8134, #52366, #15306, #47192 ) ) ;
#30159=VECTOR ( 'NONE', #66988, 1000.000000000000000 ) ;
#30161=DIRECTION ( 'NONE',  ( -0.6414496315691484707, 0.7671651518153074223, 2.309356642088893343E-17 ) ) ;
#30163=ORIENTED_EDGE ( 'NONE', *, *, #5385, .T. ) ;
#30166=CIRCLE ( 'NONE', #50496, 0.1749999999999998224 ) ;
#30172=EDGE_CURVE ( 'NONE', #49071, #55278, #22367, .T. ) ;
#30177=ORIENTED_EDGE ( 'NONE', *, *, #53413, .F. ) ;
#30179=CARTESIAN_POINT ( 'NONE',  ( -1.466476262117323737, -9.404523737882843903, 54.00000000000000711 ) ) ;
#30188=DIRECTION ( 'NONE',  ( 1.000000000000000000, -1.952517519553884087E-14, 1.836970198720994435E-16 ) ) ;
#30199=ORIENTED_EDGE ( 'NONE', *, *, #6130, .F. ) ;
#30200=CARTESIAN_POINT ( 'NONE',  ( -7.342976262117269393, -4.961189459949999936, 26.00000000000000711 ) ) ;
#30214=ORIENTED_EDGE ( 'NONE', *, *, #39908, .F. ) ;
#30217=DIRECTION ( 'NONE',  ( -1.000000000000000000, 8.728482790395504563E-15, 0.000000000000000000 ) ) ;
#30218=CARTESIAN_POINT ( 'NONE',  ( -6.835476262117334834, -10.50702373788278798, 54.00000000000000711 ) ) ;
#30226=EDGE_CURVE ( 'NONE', #21406, #46314, #68888, .T. ) ;
#30233=DIRECTION ( 'NONE',  ( 3.491481338843133355E-15, 1.000000000000000000, 1.836970198721029934E-16 ) ) ;
#30234=VECTOR ( 'NONE', #60206, 1000.000000000000000 ) ;
#30244=VERTEX_POINT ( 'NONE', #31420 ) ;
#30254=EDGE_CURVE ( 'NONE', #3304, #50773, #57572, .T. ) ;
#30256=ORIENTED_EDGE ( 'NONE', *, *, #40676, .T. ) ;
#30259=ADVANCED_FACE ( 'NONE', ( #9138 ), #4883, .F. ) ;
#30269=EDGE_CURVE ( 'NONE', #63123, #49409, #9848, .T. ) ;
#30275=EDGE_CURVE ( 'NONE', #31134, #8535, #53335, .T. ) ;
#30280=CARTESIAN_POINT ( 'NONE',  ( 10.31452373788281562, -3.857023737882814718, 26.00000000000000711 ) ) ;
#30281=ORIENTED_EDGE ( 'NONE', *, *, #15619, .F. ) ;
#30282=ORIENTED_EDGE ( 'NONE', *, *, #32431, .F. ) ;
#30283=VECTOR ( 'NONE', #1390, 1000.000000000000000 ) ;
#30290=PLANE ( 'NONE',  #4032 ) ;
#30294=ORIENTED_EDGE ( 'NONE', *, *, #11518, .T. ) ;
#30297=CARTESIAN_POINT ( 'NONE',  ( 0.9555237378828180805, 9.915476262117216777, 54.00000000000000711 ) ) ;
#30299=LINE ( 'NONE', #13676, #59067 ) ;
#30309=CARTESIAN_POINT ( 'NONE',  ( -7.394232575409651176, -6.789561617636906909, 54.00000000000000711 ) ) ;
#30317=DIRECTION ( 'NONE',  ( 1.836970198721029934E-16, 1.836970198721010706E-16, -1.000000000000000000 ) ) ;
#30321=LINE ( 'NONE', #9100, #43203 ) ;
#30325=ORIENTED_EDGE ( 'NONE', *, *, #5685, .T. ) ;
#30331=ORIENTED_EDGE ( 'NONE', *, *, #7850, .T. ) ;
#30337=DIRECTION ( 'NONE',  ( 1.000000000000000000, 0.000000000000000000, 0.000000000000000000 ) ) ;
#30340=ORIENTED_EDGE ( 'NONE', *, *, #30643, .F. ) ;
#30358=EDGE_CURVE ( 'NONE', #46340, #47169, #49414, .T. ) ;
#30359=CARTESIAN_POINT ( 'NONE',  ( -3.710438382363119736, 7.394232575409525943, 54.00000000000000711 ) ) ;
#30361=VERTEX_POINT ( 'NONE', #17560 ) ;
#30364=AXIS2_PLACEMENT_3D ( 'NONE', #5495, #27048, #6174 ) ;
#30366=CARTESIAN_POINT ( 'NONE',  ( 5.257023737882801306, 5.242976262117200470, 54.00000000000000711 ) ) ;
#30371=FACE_OUTER_BOUND ( 'NONE', #29157, .T. ) ;
#30381=VECTOR ( 'NONE', #57277, 1000.000000000000000 ) ;
#30389=CARTESIAN_POINT ( 'NONE',  ( -6.486996718459931088, 3.142976262117183062, 54.00000000000000711 ) ) ;
#30398=DIRECTION ( 'NONE',  ( 0.7071067811865550112, 0.7071067811865401342, 2.597868168706467285E-16 ) ) ;
#30401=ORIENTED_EDGE ( 'NONE', *, *, #3047, .F. ) ;
#30402=CARTESIAN_POINT ( 'NONE',  ( 9.562023737882814345, -7.969523737882825642, 54.00000000000000711 ) ) ;
#30411=DIRECTION ( 'NONE',  ( -0.000000000000000000, 3.673940397442059868E-16, -1.000000000000000000 ) ) ;
#30414=CARTESIAN_POINT ( 'NONE',  ( 9.703773737882814387, 8.566576262117184370, 54.00000000000000711 ) ) ;
#30420=VECTOR ( 'NONE', #19454, 1000.000000000000000 ) ;
#30425=DIRECTION ( 'NONE',  ( -1.000000000000000000, 0.000000000000000000, 0.000000000000000000 ) ) ;
#30427=ORIENTED_EDGE ( 'NONE', *, *, #7271, .T. ) ;
#30429=DIRECTION ( 'NONE',  ( 0.000000000000000000, 0.000000000000000000, 1.000000000000000000 ) ) ;
#30431=DIRECTION ( 'NONE',  ( 0.000000000000000000, -0.000000000000000000, 1.000000000000000000 ) ) ;
#30433=CARTESIAN_POINT ( 'NONE',  ( -6.651770455163739548, 7.342976262117183239, 26.00000000000000711 ) ) ;
#30434=ORIENTED_EDGE ( 'NONE', *, *, #11903, .T. ) ;
#30444=EDGE_LOOP ( 'NONE', ( #53914, #4027, #54289, #55655 ) ) ;
#30445=ORIENTED_EDGE ( 'NONE', *, *, #24363, .T. ) ;
#30447=CARTESIAN_POINT ( 'NONE',  ( -5.242976262117259978, 5.242976262117182706, 54.00000000000000711 ) ) ;
#30455=CARTESIAN_POINT ( 'NONE',  ( 4.961189459950046121, 7.342976262117201003, 54.00000000000000711 ) ) ;
#30465=ORIENTED_EDGE ( 'NONE', *, *, #5588, .T. ) ;
#30477=CARTESIAN_POINT ( 'NONE',  ( -8.130476262117259267, 9.547976262117177981, 54.00000000000000711 ) ) ;
#30482=FACE_OUTER_BOUND ( 'NONE', #51667, .T. ) ;
#30487=ORIENTED_EDGE ( 'NONE', *, *, #58938, .F. ) ;
#30496=DIRECTION ( 'NONE',  ( 1.836970198721029934E-16, 1.836970198721010706E-16, -1.000000000000000000 ) ) ;
#30510=EDGE_LOOP ( 'NONE', ( #2914, #48824, #46521, #64089 ) ) ;
#30512=ORIENTED_EDGE ( 'NONE', *, *, #33384, .F. ) ;
#30519=DIRECTION ( 'NONE',  ( -1.836970198721029934E-16, 1.836970198721036590E-16, -1.000000000000000000 ) ) ;
#30521=ADVANCED_FACE ( 'NONE', ( #43430 ), #17251, .F. ) ;
#30522=VERTEX_POINT ( 'NONE', #33173 ) ;
#30528=ORIENTED_EDGE ( 'NONE', *, *, #28973, .T. ) ;
#30535=EDGE_CURVE ( 'NONE', #55686, #8868, #9268, .T. ) ;
#30550=VECTOR ( 'NONE', #52452, 1000.000000000000000 ) ;
#30554=ORIENTED_EDGE ( 'NONE', *, *, #30254, .T. ) ;
#30562=DIRECTION ( 'NONE',  ( -1.000000000000000000, 8.728482790395504563E-15, 0.000000000000000000 ) ) ;
#30569=ORIENTED_EDGE ( 'NONE', *, *, #37412, .T. ) ;
#30584=EDGE_CURVE ( 'NONE', #52916, #42765, #48752, .T. ) ;
#30585=DIRECTION ( 'NONE',  ( 1.000000000000000000, 0.000000000000000000, 0.000000000000000000 ) ) ;
#30588=ORIENTED_EDGE ( 'NONE', *, *, #55458, .F. ) ;
#30609=CARTESIAN_POINT ( 'NONE',  ( 3.677663764522614454, -4.149127210878770455, 54.00000000000000711 ) ) ;
#30611=ORIENTED_EDGE ( 'NONE', *, *, #40456, .F. ) ;
#30615=CARTESIAN_POINT ( 'NONE',  ( -9.897976262117248680, -3.682023737882723857, 54.00000000000000711 ) ) ;
#30622=AXIS2_PLACEMENT_3D ( 'NONE', #37951, #5438, #43242 ) ;
#30630=DIRECTION ( 'NONE',  ( -0.000000000000000000, 3.673940397442059868E-16, -1.000000000000000000 ) ) ;
#30632=ORIENTED_EDGE ( 'NONE', *, *, #47918, .F. ) ;
#30641=CARTESIAN_POINT ( 'NONE',  ( 6.364920264886889001, 6.822336235477383326, 54.00000000000000711 ) ) ;
#30643=EDGE_CURVE ( 'NONE', #14855, #42529, #18282, .T. ) ;
#30645=ORIENTED_EDGE ( 'NONE', *, *, #61879, .T. ) ;
#30650=DIRECTION ( 'NONE',  ( 0.000000000000000000, -1.000000000000000000, 0.000000000000000000 ) ) ;
#30652=CARTESIAN_POINT ( 'NONE',  ( -1.466476262117310414, -8.612468434717262866, 26.00000000000000711 ) ) ;
#30653=CARTESIAN_POINT ( 'NONE',  ( -9.897976262117285984, -6.657023737882751924, 26.00000000000000000 ) ) ;
#30664=CARTESIAN_POINT ( 'NONE',  ( 7.357023737882817827, -3.848229544836346605, 54.00000000000000711 ) ) ;
#30665=DIRECTION ( 'NONE',  ( -0.5000000000000004441, 0.8660254037844383745, 3.181725716174720005E-16 ) ) ;
#30669=VERTEX_POINT ( 'NONE', #40204 ) ;
#30685=CARTESIAN_POINT ( 'NONE',  ( 7.532023737882778569, 3.834182069070700916, 26.00000000000000711 ) ) ;
#30688=DIRECTION ( 'NONE',  ( 0.000000000000000000, 0.000000000000000000, 1.000000000000000000 ) ) ;
#30689=EDGE_LOOP ( 'NONE', ( #22735, #39607, #16096, #43390 ) ) ;
#30695=ORIENTED_EDGE ( 'NONE', *, *, #59422, .F. ) ;
#30704=SHAPE_DEFINITION_REPRESENTATION ( #28433, #15926 ) ;
#30706=EDGE_CURVE ( 'NONE', #97, #37440, #11669, .T. ) ;
#30708=ORIENTED_EDGE ( 'NONE', *, *, #15275, .F. ) ;
#30711=CARTESIAN_POINT ( 'NONE',  ( -6.642976262117334940, -10.31452373788278898, 54.00000000000000711 ) ) ;
#30713=EDGE_LOOP ( 'NONE', ( #10340, #57073, #41244, #36903 ) ) ;
#30719=DIRECTION ( 'NONE',  ( -0.000000000000000000, -0.000000000000000000, -1.000000000000000000 ) ) ;
#30726=LINE ( 'NONE', #62534, #27564 ) ;
#30727=ORIENTED_EDGE ( 'NONE', *, *, #51408, .F. ) ;
#30728=CYLINDRICAL_SURFACE ( 'NONE', #40782, 0.1749999999999998224 ) ;
#30735=PLANE ( 'NONE',  #50400 ) ;
#30738=EDGE_CURVE ( 'NONE', #12110, #58380, #14032, .T. ) ;
#30739=DIRECTION ( 'NONE',  ( -0.7671651518153006499, 0.6414496315691565753, -0.000000000000000000 ) ) ;
#30740=ORIENTED_EDGE ( 'NONE', *, *, #16015, .F. ) ;
#30744=EDGE_CURVE ( 'NONE', #64822, #22435, #18994, .T. ) ;
#30746=CARTESIAN_POINT ( 'NONE',  ( -10.30047626211724499, -3.857023737882708581, 26.00000000000000000 ) ) ;
#30748=DIRECTION ( 'NONE',  ( 1.836970198721029934E-16, 1.836970198721010706E-16, -1.000000000000000000 ) ) ;
#30754=DIRECTION ( 'NONE',  ( 9.912705577010386883E-15, 1.000000000000000000, 0.000000000000000000 ) ) ;
#30762=ORIENTED_EDGE ( 'NONE', *, *, #19041, .T. ) ;
#30770=ORIENTED_EDGE ( 'NONE', *, *, #1366, .T. ) ;
#30771=VECTOR ( 'NONE', #66016, 1000.000000000000000 ) ;
#30772=PLANE ( 'NONE',  #41990 ) ;
#30782=DIRECTION ( 'NONE',  ( 0.000000000000000000, 1.000000000000000000, 3.673940397442059868E-16 ) ) ;
#30794=VECTOR ( 'NONE', #58585, 1000.000000000000000 ) ;
#30795=VECTOR ( 'NONE', #3621, 1000.000000000000000 ) ;
#30798=VERTEX_POINT ( 'NONE', #35958 ) ;
#30810=DIRECTION ( 'NONE',  ( -1.000000000000000000, 1.671920889371702854E-15, 6.142537696789956391E-31 ) ) ;
#30813=DIRECTION ( 'NONE',  ( 0.000000000000000000, 3.673940397442059868E-16, -1.000000000000000000 ) ) ;
#30820=ORIENTED_EDGE ( 'NONE', *, *, #32340, .F. ) ;
#30831=EDGE_CURVE ( 'NONE', #21095, #59900, #26758, .T. ) ;
#30832=ORIENTED_EDGE ( 'NONE', *, *, #11395, .F. ) ;
#30835=ADVANCED_FACE ( 'NONE', ( #37369 ), #57871, .F. ) ;
#30844=DIRECTION ( 'NONE',  ( -0.6414496315691592399, -0.7671651518152985405, 0.000000000000000000 ) ) ;
#30848=CARTESIAN_POINT ( 'NONE',  ( 6.364920264886885448, -3.677663764522628664, 54.00000000000000711 ) ) ;
#30850=AXIS2_PLACEMENT_3D ( 'NONE', #63167, #20729, #62447 ) ;
#30854=ORIENTED_EDGE ( 'NONE', *, *, #63904, .F. ) ;
#30867=VERTEX_POINT ( 'NONE', #69537 ) ;
#30871=DIRECTION ( 'NONE',  ( -1.836970198721029934E-16, 1.836970198721036344E-16, -1.000000000000000000 ) ) ;
#30878=EDGE_CURVE ( 'NONE', #2772, #15483, #22880, .T. ) ;
#30886=ORIENTED_EDGE ( 'NONE', *, *, #56149, .F. ) ;
#30893=LINE ( 'NONE', #36913, #61166 ) ;
#30906=VECTOR ( 'NONE', #58811, 1000.000000000000000 ) ;
#30919=EDGE_CURVE ( 'NONE', #59636, #37440, #10141, .T. ) ;
#30935=APPLICATION_CONTEXT ( 'automotive_design' ) ;
#30947=AXIS2_PLACEMENT_3D ( 'NONE', #53558, #32335, #5115 ) ;
#30954=DIRECTION ( 'NONE',  ( -3.903627567395476653E-15, -1.000000000000000000, -1.836970198721029194E-16 ) ) ;
#30966=ORIENTED_EDGE ( 'NONE', *, *, #7685, .F. ) ;
#30971=DIRECTION ( 'NONE',  ( 1.836970198721029934E-16, 1.836970198721010706E-16, -1.000000000000000000 ) ) ;
#30977=EDGE_CURVE ( 'NONE', #34023, #40740, #22496, .T. ) ;
#30994=VECTOR ( 'NONE', #49813, 1000.000000000000000 ) ;
#31000=CARTESIAN_POINT ( 'NONE',  ( 5.793274621760841292, 6.344366288193348247, 54.00000000000000711 ) ) ;
#31014=CARTESIAN_POINT ( 'NONE',  ( -3.650476262117221093, 10.49297626211717116, 26.00000000000000711 ) ) ;
#31028=ORIENTED_EDGE ( 'NONE', *, *, #20237, .F. ) ;
#31030=ORIENTED_EDGE ( 'NONE', *, *, #66840, .F. ) ;
#31033=ORIENTED_EDGE ( 'NONE', *, *, #8756, .F. ) ;
#31049=EDGE_CURVE ( 'NONE', #28114, #67635, #12206, .T. ) ;
#31060=ORIENTED_EDGE ( 'NONE', *, *, #34493, .F. ) ;
#31077=DIRECTION ( 'NONE',  ( -0.000000000000000000, -0.000000000000000000, -1.000000000000000000 ) ) ;
#31078=VERTEX_POINT ( 'NONE', #1960 ) ;
#31080=CARTESIAN_POINT ( 'NONE',  ( -5.242976262117275077, -5.257023737882800418, 26.00000000000000711 ) ) ;
#31088=CIRCLE ( 'NONE', #5147, 0.1749999999999989342 ) ;
#31107=DIRECTION ( 'NONE',  ( -1.000000000000000000, 1.671920889371702854E-15, 0.000000000000000000 ) ) ;
#31122=ORIENTED_EDGE ( 'NONE', *, *, #21588, .T. ) ;
#31123=ORIENTED_EDGE ( 'NONE', *, *, #28478, .T. ) ;
#31133=ORIENTED_EDGE ( 'NONE', *, *, #27890, .T. ) ;
#31134=VERTEX_POINT ( 'NONE', #12890 ) ;
#31135=DIRECTION ( 'NONE',  ( -0.8660254037844383745, -0.5000000000000004441, -1.836970198721031660E-16 ) ) ;
#31136=CARTESIAN_POINT ( 'NONE',  ( -7.394232575409605879, -3.724485858128642413, 54.00000000000000711 ) ) ;
#31153=AXIS2_PLACEMENT_3D ( 'NONE', #21325, #64466, #60865 ) ;
#31158=VECTOR ( 'NONE', #32719, 1000.000000000000114 ) ;
#31160=CIRCLE ( 'NONE', #19826, 0.3499999999999996447 ) ;
#31164=ORIENTED_EDGE ( 'NONE', *, *, #31182, .T. ) ;
#31172=CARTESIAN_POINT ( 'NONE',  ( 5.257023737882819070, -5.257023737882825287, 54.00000000000000711 ) ) ;
#31173=CYLINDRICAL_SURFACE ( 'NONE', #23847, 0.7112000000000124889 ) ;
#31182=EDGE_CURVE ( 'NONE', #12532, #45380, #42582, .T. ) ;
#31183=PLANE ( 'NONE',  #4620 ) ;
#31185=ORIENTED_EDGE ( 'NONE', *, *, #45027, .F. ) ;
#31187=DIRECTION ( 'NONE',  ( 1.000000000000000000, -8.728482790395504563E-15, -3.206792553201184024E-30 ) ) ;
#31188=ORIENTED_EDGE ( 'NONE', *, *, #29939, .T. ) ;
#31190=FACE_OUTER_BOUND ( 'NONE', #15591, .T. ) ;
#31193=CARTESIAN_POINT ( 'NONE',  ( 10.31452373788281562, -3.857023737882824932, 54.00000000000000711 ) ) ;
#31197=LINE ( 'NONE', #4331, #33887 ) ;
#31200=AXIS2_PLACEMENT_3D ( 'NONE', #23091, #27717, #48943 ) ;
#31214=AXIS2_PLACEMENT_3D ( 'NONE', #69432, #20984, #10384 ) ;
#31217=VECTOR ( 'NONE', #16621, 1000.000000000000000 ) ;
#31224=DIRECTION ( 'NONE',  ( -1.836970198721029934E-16, 1.836970198721036590E-16, -1.000000000000000000 ) ) ;
#31228=CARTESIAN_POINT ( 'NONE',  ( 5.257023737882819070, -5.257023737882825287, 54.00000000000000711 ) ) ;
#31229=LINE ( 'NONE', #37222, #24126 ) ;
#31238=CARTESIAN_POINT ( 'NONE',  ( -7.342976262117259623, 5.538810540049946773, 26.00000000000000711 ) ) ;
#31245=EDGE_CURVE ( 'NONE', #25606, #7476, #69108, .T. ) ;
#31246=CARTESIAN_POINT ( 'NONE',  ( -2.355476262117229158, 9.547976262117156665, 54.00000000000000711 ) ) ;
#31247=ORIENTED_EDGE ( 'NONE', *, *, #26871, .T. ) ;
#31249=VERTEX_POINT ( 'NONE', #46481 ) ;
#31250=EDGE_CURVE ( 'NONE', #45686, #27049, #68056, .T. ) ;
#31252=EDGE_CURVE ( 'NONE', #55063, #7002, #61267, .T. ) ;
#31261=ORIENTED_EDGE ( 'NONE', *, *, #34535, .F. ) ;
#31262=ORIENTED_EDGE ( 'NONE', *, *, #45417, .T. ) ;
#31263=CIRCLE ( 'NONE', #65172, 0.1749999999999980738 ) ;
#31284=LINE ( 'NONE', #25622, #41535 ) ;
#31285=DIRECTION ( 'NONE',  ( -1.356437060717832013E-15, -1.000000000000000000, -1.836970198721033878E-16 ) ) ;
#31286=CARTESIAN_POINT ( 'NONE',  ( -7.394232575409614761, 3.710438382363058896, 54.00000000000000711 ) ) ;
#31294=CARTESIAN_POINT ( 'NONE',  ( -6.642976262117328723, -9.912023737882789121, 54.00000000000000711 ) ) ;
#31301=DIRECTION ( 'NONE',  ( 0.8660254037844311581, -0.5000000000000129896, 6.723777587268175486E-17 ) ) ;
#31302=CARTESIAN_POINT ( 'NONE',  ( 5.257023737882819070, -5.257023737882825287, 54.00000000000000711 ) ) ;
#31307=AXIS2_PLACEMENT_3D ( 'NONE', #8433, #46980, #25781 ) ;
#31309=LINE ( 'NONE', #58157, #14791 ) ;
#31313=AXIS2_PLACEMENT_3D ( 'NONE', #37637, #37287, #47880 ) ;
#31315=LINE ( 'NONE', #69119, #23410 ) ;
#31317=CARTESIAN_POINT ( 'NONE',  ( -8.916576262117361651, -10.05377373788273587, 54.00000000000000711 ) ) ;
#31323=CARTESIAN_POINT ( 'NONE',  ( 3.664523737882781518, -10.31452373788281029, 54.00000000000000711 ) ) ;
#31326=AXIS2_PLACEMENT_3D ( 'NONE', #50784, #3753, #67418 ) ;
#31337=ORIENTED_EDGE ( 'NONE', *, *, #13035, .F. ) ;
#31339=ORIENTED_EDGE ( 'NONE', *, *, #46818, .F. ) ;
#31348=CARTESIAN_POINT ( 'NONE',  ( -2.530476262117228092, 9.722976262117159152, 54.00000000000000711 ) ) ;
#31354=CIRCLE ( 'NONE', #7589, 0.1749999999999989342 ) ;
#31364=CARTESIAN_POINT ( 'NONE',  ( -8.821682069070824639, -8.144523737882760628, 26.00000000000000000 ) ) ;
#31366=CIRCLE ( 'NONE', #12100, 1.224999999999999423 ) ;
#31378=LINE ( 'NONE', #47616, #30794 ) ;
#31386=EDGE_CURVE ( 'NONE', #28477, #64355, #27711, .T. ) ;
#31391=VERTEX_POINT ( 'NONE', #32330 ) ;
#31394=ORIENTED_EDGE ( 'NONE', *, *, #31971, .T. ) ;
#31398=EDGE_CURVE ( 'NONE', #50489, #51462, #11439, .T. ) ;
#31399=CARTESIAN_POINT ( 'NONE',  ( 5.257023737882801306, 5.242976262117200470, 54.00000000000000711 ) ) ;
#31412=CARTESIAN_POINT ( 'NONE',  ( -9.880476262117236175, 7.447976262117216528, 54.00000000000000711 ) ) ;
#31420=CARTESIAN_POINT ( 'NONE',  ( 8.930623737882843471, 8.566576262117187923, 54.00000000000000711 ) ) ;
#31431=EDGE_CURVE ( 'NONE', #27077, #14139, #7117, .T. ) ;
#31437=DIRECTION ( 'NONE',  ( 0.000000000000000000, 1.000000000000000000, 0.000000000000000000 ) ) ;
#31453=DIRECTION ( 'NONE',  ( 1.000000000000000000, -1.671920889371702854E-15, 0.000000000000000000 ) ) ;
#31464=FACE_OUTER_BOUND ( 'NONE', #24623, .T. ) ;
#31487=EDGE_LOOP ( 'NONE', ( #12878, #24244, #54424, #58004, #64030, #65787, #55506, #42282 ) ) ;
#31490=CARTESIAN_POINT ( 'NONE',  ( 10.05377373788278739, -9.703773737882823269, 54.00000000000000711 ) ) ;
#31494=LINE ( 'NONE', #19461, #34357 ) ;
#31502=CYLINDRICAL_SURFACE ( 'NONE', #36696, 0.1749999999999989342 ) ;
#31507=EDGE_CURVE ( 'NONE', #45115, #9110, #13173, .T. ) ;
#31508=AXIS2_PLACEMENT_3D ( 'NONE', #16117, #54649, #62900 ) ;
#31512=ORIENTED_EDGE ( 'NONE', *, *, #7262, .F. ) ;
#31514=DIRECTION ( 'NONE',  ( 9.912705577010319041E-15, 1.000000000000000000, 0.000000000000000000 ) ) ;
#31518=EDGE_CURVE ( 'NONE', #45363, #51724, #24139, .T. ) ;
#31520=CARTESIAN_POINT ( 'NONE',  ( 9.737023737882781305, 3.667976262117152775, 54.00000000000000711 ) ) ;
#31524=FACE_OUTER_BOUND ( 'NONE', #40037, .T. ) ;
#31525=VERTEX_POINT ( 'NONE', #44643 ) ;
#31528=LINE ( 'NONE', #56968, #47626 ) ;
#31530=CARTESIAN_POINT ( 'NONE',  ( 6.364920264886846368, 3.663616288756996298, 26.00000000000000711 ) ) ;
#31531=CARTESIAN_POINT ( 'NONE',  ( 4.046023737882819660, -3.157023737882826087, 54.00000000000000711 ) ) ;
#31532=DIRECTION ( 'NONE',  ( 0.000000000000000000, 0.000000000000000000, -1.000000000000000000 ) ) ;
#31542=PLANE ( 'NONE',  #17346 ) ;
#31543=PLANE ( 'NONE',  #58808 ) ;
#31548=DIRECTION ( 'NONE',  ( 1.000000000000000000, -1.047444401652940007E-14, 0.000000000000000000 ) ) ;
#31556=ORIENTED_EDGE ( 'NONE', *, *, #34937, .F. ) ;
#31561=DIRECTION ( 'NONE',  ( -0.000000000000000000, -0.000000000000000000, -1.000000000000000000 ) ) ;
#31567=ORIENTED_EDGE ( 'NONE', *, *, #30831, .F. ) ;
#31572=EDGE_CURVE ( 'NONE', #24795, #50489, #26246, .T. ) ;
#31581=EDGE_CURVE ( 'NONE', #20102, #20187, #19183, .T. ) ;
#31585=ADVANCED_FACE ( 'NONE', ( #47115 ), #68686, .T. ) ;
#31588=CIRCLE ( 'NONE', #18021, 0.3499999999999996447 ) ;
#31592=CARTESIAN_POINT ( 'NONE',  ( 3.682023737882818448, 9.722976262117203561, 54.00000000000000711 ) ) ;
#31605=CARTESIAN_POINT ( 'NONE',  ( 5.257023737882801306, 5.242976262117200470, 54.00000000000000711 ) ) ;
#31609=ORIENTED_EDGE ( 'NONE', *, *, #5385, .F. ) ;
#31614=CYLINDRICAL_SURFACE ( 'NONE', #31214, 0.1749999999999989342 ) ;
#31620=ORIENTED_EDGE ( 'NONE', *, *, #38452, .T. ) ;
#31634=DIRECTION ( 'NONE',  ( 3.304235192336778667E-15, 1.000000000000000000, 0.000000000000000000 ) ) ;
#31635=CARTESIAN_POINT ( 'NONE',  ( 0.9555237378827876604, -9.404523737882779955, 26.00000000000000000 ) ) ;
#31640=EDGE_LOOP ( 'NONE', ( #20262, #5519, #61643, #64894 ) ) ;
#31641=LINE ( 'NONE', #64511, #62660 ) ;
#31642=DIRECTION ( 'NONE',  ( 0.000000000000000000, -3.673940397442059868E-16, 1.000000000000000000 ) ) ;
#31657=CARTESIAN_POINT ( 'NONE',  ( 2.369523737882786918, -9.562023737882798358, 54.00000000000000711 ) ) ;
#31661=DIRECTION ( 'NONE',  ( -1.000000000000000000, 0.000000000000000000, 0.000000000000000000 ) ) ;
#31664=VECTOR ( 'NONE', #39514, 1000.000000000000000 ) ;
#31665=EDGE_LOOP ( 'NONE', ( #41278, #9210, #3810, #62263 ) ) ;
#31668=AXIS2_PLACEMENT_3D ( 'NONE', #56573, #40660, #62936 ) ;
#31678=ORIENTED_EDGE ( 'NONE', *, *, #29531, .T. ) ;
#31679=ORIENTED_EDGE ( 'NONE', *, *, #36583, .F. ) ;
#31692=CARTESIAN_POINT ( 'NONE',  ( -7.955476262117324282, -9.562023737882771712, 54.00000000000000711 ) ) ;
#31695=AXIS2_PLACEMENT_3D ( 'NONE', #64385, #15938, #37510 ) ;
#31696=ORIENTED_EDGE ( 'NONE', *, *, #34633, .T. ) ;
#31704=CARTESIAN_POINT ( 'NONE',  ( -4.947141984184534991, -7.357023737882802727, 26.00000000000000711 ) ) ;
#31708=FACE_OUTER_BOUND ( 'NONE', #66245, .T. ) ;
#31712=CARTESIAN_POINT ( 'NONE',  ( -2.406732575409589625, 8.697938382363036069, 26.00000000000000711 ) ) ;
#31715=ORIENTED_EDGE ( 'NONE', *, *, #40326, .T. ) ;
#31718=AXIS2_PLACEMENT_3D ( 'NONE', #22978, #44532, #34265 ) ;
#31719=DIRECTION ( 'NONE',  ( -1.000000000000000000, 0.000000000000000000, 0.000000000000000000 ) ) ;
#31720=CARTESIAN_POINT ( 'NONE',  ( -9.722976262117256852, 2.530476262117183683, 54.00000000000000711 ) ) ;
#31726=CARTESIAN_POINT ( 'NONE',  ( 8.241237374594303944, -1.634292677759887846, 54.00000000000000711 ) ) ;
#31730=ORIENTED_EDGE ( 'NONE', *, *, #58713, .F. ) ;
#31733=FACE_OUTER_BOUND ( 'NONE', #38463, .T. ) ;
#31753=AXIS2_PLACEMENT_3D ( 'NONE', #61155, #12711, #50571 ) ;
#31760=AXIS2_PLACEMENT_3D ( 'NONE', #19364, #14770, #8395 ) ;
#31767=PLANE ( 'NONE',  #29971 ) ;
#31771=EDGE_CURVE ( 'NONE', #10965, #15214, #53826, .T. ) ;
#31772=EDGE_CURVE ( 'NONE', #45585, #62156, #11026, .T. ) ;
#31777=EDGE_CURVE ( 'NONE', #45123, #30361, #36512, .T. ) ;
#31779=CARTESIAN_POINT ( 'NONE',  ( -5.538810540050023157, 7.342976262117183239, 26.00000000000000711 ) ) ;
#31786=LINE ( 'NONE', #54650, #56870 ) ;
#31803=CARTESIAN_POINT ( 'NONE',  ( 7.357023737882817827, -6.665817930929295088, 26.00000000000000000 ) ) ;
#31814=LINE ( 'NONE', #47360, #3882 ) ;
#31839=CARTESIAN_POINT ( 'NONE',  ( -3.667976262117330410, -9.912023737882817542, 54.00000000000000711 ) ) ;
#31846=DIRECTION ( 'NONE',  ( 2.478176394252584099E-15, 1.000000000000000000, 0.000000000000000000 ) ) ;
#31860=DIRECTION ( 'NONE',  ( 0.000000000000000000, 1.000000000000000000, 0.000000000000000000 ) ) ;
#31869=CARTESIAN_POINT ( 'NONE',  ( -2.406732575409590069, 8.697938382363036069, 54.00000000000000711 ) ) ;
#31877=DIRECTION ( 'NONE',  ( -1.000000000000000000, -1.570596175624152290E-15, 0.000000000000000000 ) ) ;
#31879=DIRECTION ( 'NONE',  ( -1.000000000000000000, 0.000000000000000000, 0.000000000000000000 ) ) ;
#31884=CARTESIAN_POINT ( 'NONE',  ( -3.667976262117323305, -9.737023737882815055, 26.00000000000000000 ) ) ;
#31886=PLANE ( 'NONE',  #28404 ) ;
#31887=ORIENTED_EDGE ( 'NONE', *, *, #38883, .F. ) ;
#31892=ORIENTED_EDGE ( 'NONE', *, *, #48082, .F. ) ;
#31894=LINE ( 'NONE', #5015, #38206 ) ;
#31896=CYLINDRICAL_SURFACE ( 'NONE', #11591, 0.1749999999999998224 ) ;
#31901=ORIENTED_EDGE ( 'NONE', *, *, #1989, .F. ) ;
#31903=CARTESIAN_POINT ( 'NONE',  ( -9.390476262117209316, -1.480523737882732060, 54.00000000000000711 ) ) ;
#31911=CARTESIAN_POINT ( 'NONE',  ( 3.157023737882792780, 4.031976262117212606, 26.00000000000000711 ) ) ;
#31912=ORIENTED_EDGE ( 'NONE', *, *, #28929, .F. ) ;
#31913=EDGE_CURVE ( 'NONE', #47996, #34611, #33626, .T. ) ;
#31915=DIRECTION ( 'NONE',  ( -0.000000000000000000, 3.673940397442059868E-16, -1.000000000000000000 ) ) ;
#31923=VERTEX_POINT ( 'NONE', #62131 ) ;
#31926=DIRECTION ( 'NONE',  ( -1.000000000000000000, -0.000000000000000000, -0.000000000000000000 ) ) ;
#31929=EDGE_LOOP ( 'NONE', ( #49053, #42564, #18930, #56948 ) ) ;
#31932=LINE ( 'NONE', #59145, #65536 ) ;
#31943=ORIENTED_EDGE ( 'NONE', *, *, #46598, .F. ) ;
#31956=LINE ( 'NONE', #69792, #58722 ) ;
#31971=EDGE_CURVE ( 'NONE', #26273, #49178, #62474, .T. ) ;
#31972=EDGE_CURVE ( 'NONE', #58217, #35004, #3105, .T. ) ;
#31991=CARTESIAN_POINT ( 'NONE',  ( 8.580623737882843827, 9.689726262117162037, 26.00000000000000711 ) ) ;
#31995=EDGE_CURVE ( 'NONE', #57625, #6981, #36676, .T. ) ;
#32002=DIRECTION ( 'NONE',  ( -1.000000000000000000, 1.115702204244423151E-14, 0.000000000000000000 ) ) ;
#32005=FACE_OUTER_BOUND ( 'NONE', #49188, .T. ) ;
#32010=CARTESIAN_POINT ( 'NONE',  ( -5.242976262117280406, -5.257023737882805747, 54.00000000000000711 ) ) ;
#32025=VECTOR ( 'NONE', #37019, 1000.000000000000000 ) ;
#32026=CARTESIAN_POINT ( 'NONE',  ( 8.144523737882817471, -8.835729544836345539, 54.00000000000000711 ) ) ;
#32040=DIRECTION ( 'NONE',  ( 0.000000000000000000, 0.000000000000000000, 1.000000000000000000 ) ) ;
#32042=ORIENTED_EDGE ( 'NONE', *, *, #30083, .T. ) ;
#32050=DIRECTION ( 'NONE',  ( -1.836970198721029934E-16, 1.836970198721036590E-16, -1.000000000000000000 ) ) ;
#32064=CIRCLE ( 'NONE', #61396, 0.1749999999999998224 ) ;
#32066=VECTOR ( 'NONE', #44028, 1000.000000000000000 ) ;
#32067=DIRECTION ( 'NONE',  ( -0.6414496315691592399, 0.7671651518152985405, 2.587583378555132735E-16 ) ) ;
#32073=CARTESIAN_POINT ( 'NONE',  ( -6.467976262117279163, -5.257023737882805747, 54.00000000000000711 ) ) ;
#32076=DIRECTION ( 'NONE',  ( -1.000000000000000000, 9.050731179009442381E-15, 3.325184690495119758E-30 ) ) ;
#32078=ORIENTED_EDGE ( 'NONE', *, *, #69566, .F. ) ;
#32081=VERTEX_POINT ( 'NONE', #37041 ) ;
#32082=CARTESIAN_POINT ( 'NONE',  ( 4.149127210878720717, 6.822336235477395761, 26.00000000000000711 ) ) ;
#32085=LINE ( 'NONE', #26790, #68887 ) ;
#32088=VECTOR ( 'NONE', #57442, 1000.000000000000000 ) ;
#32094=ORIENTED_EDGE ( 'NONE', *, *, #22062, .T. ) ;
#32099=EDGE_CURVE ( 'NONE', #46021, #14139, #43016, .T. ) ;
#32101=VECTOR ( 'NONE', #8373, 1000.000000000000000 ) ;
#32102=VECTOR ( 'NONE', #43657, 1000.000000000000000 ) ;
#32106=ADVANCED_FACE ( 'NONE', ( #31733 ), #37726, .F. ) ;
#32110=EDGE_CURVE ( 'NONE', #42141, #56362, #46923, .T. ) ;
#32113=DIRECTION ( 'NONE',  ( -4.956352788505168198E-15, -1.000000000000000000, 0.000000000000000000 ) ) ;
#32116=CARTESIAN_POINT ( 'NONE',  ( -3.650476262117221093, 10.49297626211717116, 54.00000000000000711 ) ) ;
#32117=EDGE_CURVE ( 'NONE', #28065, #25655, #43365, .T. ) ;
#32132=PLANE ( 'NONE',  #14679 ) ;
#32144=VECTOR ( 'NONE', #20402, 1000.000000000000000 ) ;
#32148=FACE_OUTER_BOUND ( 'NONE', #27733, .T. ) ;
#32156=ORIENTED_EDGE ( 'NONE', *, *, #42870, .T. ) ;
#32162=DIRECTION ( 'NONE',  ( -0.000000000000000000, 3.673940397442059868E-16, -1.000000000000000000 ) ) ;
#32171=LINE ( 'NONE', #31136, #834 ) ;
#32174=AXIS2_PLACEMENT_3D ( 'NONE', #39324, #66196, #1836 ) ;
#32175=VERTEX_POINT ( 'NONE', #6235 ) ;
#32184=VERTEX_POINT ( 'NONE', #55376 ) ;
#32192=ORIENTED_EDGE ( 'NONE', *, *, #28188, .T. ) ;
#32195=LINE ( 'NONE', #53777, #53828 ) ;
#32218=ORIENTED_EDGE ( 'NONE', *, *, #21646, .F. ) ;
#32222=ORIENTED_EDGE ( 'NONE', *, *, #57467, .T. ) ;
#32224=ORIENTED_EDGE ( 'NONE', *, *, #24585, .T. ) ;
#32226=LINE ( 'NONE', #58418, #63455 ) ;
#32228=DIRECTION ( 'NONE',  ( -0.000000000000000000, 3.673940397442059868E-16, -1.000000000000000000 ) ) ;
#32232=LINE ( 'NONE', #11018, #6685 ) ;
#32233=SURFACE_SIDE_STYLE ('',( #42836 ) ) ;
#32238=DIRECTION ( 'NONE',  ( 1.836970198721029934E-16, -1.836970198721036344E-16, 1.000000000000000000 ) ) ;
#32243=VECTOR ( 'NONE', #48673, 1000.000000000000000 ) ;
#32244=DIRECTION ( 'NONE',  ( 1.000000000000000000, 0.000000000000000000, 0.000000000000000000 ) ) ;
#32260=DIRECTION ( 'NONE',  ( -0.000000000000000000, 3.673940397442059868E-16, -1.000000000000000000 ) ) ;
#32261=LINE ( 'NONE', #37924, #51526 ) ;
#32266=EDGE_LOOP ( 'NONE', ( #38832, #69676, #2976, #21940 ) ) ;
#32268=EDGE_CURVE ( 'NONE', #49486, #47595, #38087, .T. ) ;
#32269=PLANE ( 'NONE',  #34446 ) ;
#32270=FACE_OUTER_BOUND ( 'NONE', #17717, .T. ) ;
#32281=VERTEX_POINT ( 'NONE', #33456 ) ;
#32292=FACE_OUTER_BOUND ( 'NONE', #33904, .T. ) ;
#32296=CARTESIAN_POINT ( 'NONE',  ( 10.50702373788278265, 3.650476262117142934, 54.00000000000000711 ) ) ;
#32298=AXIS2_PLACEMENT_3D ( 'NONE', #46146, #34470, #12906 ) ;
#32299=CARTESIAN_POINT ( 'NONE',  ( 4.149127210878726935, -6.836383711243002814, 54.00000000000000711 ) ) ;
#32300=DIRECTION ( 'NONE',  ( 1.836970198721029934E-16, -1.836970198721036344E-16, 1.000000000000000000 ) ) ;
#32301=EDGE_CURVE ( 'NONE', #56758, #9312, #24932, .T. ) ;
#32304=EDGE_CURVE ( 'NONE', #48411, #18604, #53052, .T. ) ;
#32314=VECTOR ( 'NONE', #2984, 1000.000000000000000 ) ;
#32322=VECTOR ( 'NONE', #3443, 1000.000000000000000 ) ;
#32330=CARTESIAN_POINT ( 'NONE',  ( 6.836383711243005479, -6.364920264886896994, 26.00000000000000711 ) ) ;
#32335=DIRECTION ( 'NONE',  ( 0.000000000000000000, 3.673940397442059868E-16, -1.000000000000000000 ) ) ;
#32340=EDGE_CURVE ( 'NONE', #19393, #48826, #29883, .T. ) ;
#32341=DIRECTION ( 'NONE',  ( -1.836970198721029934E-16, 1.836970198721036590E-16, -1.000000000000000000 ) ) ;
#32342=CARTESIAN_POINT ( 'NONE',  ( 8.711985858128686644, 8.079219948824833963, 54.00000000000000711 ) ) ;
#32343=DIRECTION ( 'NONE',  ( 0.000000000000000000, -3.673940397442059868E-16, 1.000000000000000000 ) ) ;
#32350=ORIENTED_EDGE ( 'NONE', *, *, #25632, .T. ) ;
#32355=DIRECTION ( 'NONE',  ( 1.000000000000000000, 0.000000000000000000, 0.000000000000000000 ) ) ;
#32359=EDGE_CURVE ( 'NONE', #62514, #55737, #56753, .T. ) ;
#32364=VECTOR ( 'NONE', #19117, 1000.000000000000000 ) ;
#32366=EDGE_CURVE ( 'NONE', #19510, #14855, #24237, .T. ) ;
#32369=EDGE_CURVE ( 'NONE', #22889, #19590, #34127, .T. ) ;
#32376=ORIENTED_EDGE ( 'NONE', *, *, #53200, .F. ) ;
#32378=LINE ( 'NONE', #39051, #16515 ) ;
#32384=ORIENTED_EDGE ( 'NONE', *, *, #41391, .T. ) ;
#32390=LINE ( 'NONE', #57589, #28062 ) ;
#32394=AXIS2_PLACEMENT_3D ( 'NONE', #62639, #53112, #63712 ) ;
#32401=LINE ( 'NONE', #5525, #69262 ) ;
#32412=VECTOR ( 'NONE', #25164, 1000.000000000000000 ) ;
#32423=LINE ( 'NONE', #33786, #64468 ) ;
#32428=DIRECTION ( 'NONE',  ( -0.000000000000000000, -1.000000000000000000, -0.000000000000000000 ) ) ;
#32429=CYLINDRICAL_SURFACE ( 'NONE', #65062, 1.224999999999998757 ) ;
#32431=EDGE_CURVE ( 'NONE', #49465, #15450, #26686, .T. ) ;
#32432=FACE_OUTER_BOUND ( 'NONE', #9929, .T. ) ;
#32434=EDGE_CURVE ( 'NONE', #48863, #54361, #31315, .T. ) ;
#32439=ORIENTED_EDGE ( 'NONE', *, *, #19469, .T. ) ;
#32442=CARTESIAN_POINT ( 'NONE',  ( 1.480523737882788238, -9.404523737882783507, 26.00000000000000000 ) ) ;
#32447=ORIENTED_EDGE ( 'NONE', *, *, #41863, .T. ) ;
#32450=DIRECTION ( 'NONE',  ( -1.000000000000000000, -5.013651664672856055E-16, -1.841985738954423698E-31 ) ) ;
#32452=ORIENTED_EDGE ( 'NONE', *, *, #25290, .F. ) ;
#32457=AXIS2_PLACEMENT_3D ( 'NONE', #42384, #14112, #63975 ) ;
#32461=ORIENTED_EDGE ( 'NONE', *, *, #1675, .T. ) ;
#32462=AXIS2_PLACEMENT_3D ( 'NONE', #49954, #7162, #1517 ) ;
#32469=VECTOR ( 'NONE', #44842, 1000.000000000000000 ) ;
#32475=VERTEX_POINT ( 'NONE', #21023 ) ;
#32481=VERTEX_POINT ( 'NONE', #63469 ) ;
#32482=ORIENTED_EDGE ( 'NONE', *, *, #34647, .T. ) ;
#32494=DIRECTION ( 'NONE',  ( -1.047444401652940007E-14, -1.000000000000000000, -1.836970198721029934E-16 ) ) ;
#32499=CARTESIAN_POINT ( 'NONE',  ( 7.357023737882797398, 4.947141984184415087, 54.00000000000000711 ) ) ;
#32508=EDGE_CURVE ( 'NONE', #51395, #5174, #15029, .T. ) ;
#32524=CARTESIAN_POINT ( 'NONE',  ( -1.991476262117235274, 8.598420958951582094, 26.00000000000000711 ) ) ;
#32552=LINE ( 'NONE', #54116, #10951 ) ;
#32555=VERTEX_POINT ( 'NONE', #64868 ) ;
#32567=CARTESIAN_POINT ( 'NONE',  ( 2.632023737882809744, -6.501044194225475081, 54.00000000000000711 ) ) ;
#32591=DIRECTION ( 'NONE',  ( -0.7671651518153028704, -0.6414496315691537998, -2.587583378555113506E-16 ) ) ;
#32595=DIRECTION ( 'NONE',  ( -1.000000000000000000, 1.254221251785257731E-14, 1.836970198721053107E-16 ) ) ;
#32604=VERTEX_POINT ( 'NONE', #64522 ) ;
#32609=VECTOR ( 'NONE', #40577, 1000.000000000000000 ) ;
#32616=DIRECTION ( 'NONE',  ( 0.000000000000000000, -1.000000000000000000, 0.000000000000000000 ) ) ;
#32619=CYLINDRICAL_SURFACE ( 'NONE', #57869, 0.1749999999999998224 ) ;
#32631=DIRECTION ( 'NONE',  ( -0.6414496315691484707, 0.7671651518153074223, 2.309356642088893343E-17 ) ) ;
#32636=ORIENTED_EDGE ( 'NONE', *, *, #52764, .F. ) ;
#32641=ORIENTED_EDGE ( 'NONE', *, *, #49996, .F. ) ;
#32642=EDGE_CURVE ( 'NONE', #62873, #167, #43289, .T. ) ;
#32645=CARTESIAN_POINT ( 'NONE',  ( 8.711985858128693749, -2.420780051175180692, 54.00000000000000711 ) ) ;
#32648=ADVANCED_FACE ( 'NONE', ( #17108 ), #54959, .F. ) ;
#32663=FACE_OUTER_BOUND ( 'NONE', #65831, .T. ) ;
#32666=LINE ( 'NONE', #54943, #39500 ) ;
#32669=DIRECTION ( 'NONE',  ( -1.836970198721029934E-16, 1.836970198721036590E-16, -1.000000000000000000 ) ) ;
#32674=CARTESIAN_POINT ( 'NONE',  ( -10.49297626211729551, -6.849523737882748264, 54.00000000000000711 ) ) ;
#32679=EDGE_CURVE ( 'NONE', #36149, #44524, #60234, .T. ) ;
#32684=CYLINDRICAL_SURFACE ( 'NONE', #20640, 0.3499999999999996447 ) ;
#32696=DIRECTION ( 'NONE',  ( -0.000000000000000000, -0.000000000000000000, -1.000000000000000000 ) ) ;
#32703=AXIS2_PLACEMENT_3D ( 'NONE', #23335, #27601, #55173 ) ;
#32711=CARTESIAN_POINT ( 'NONE',  ( -5.779227145995285753, 4.141586236041028712, 54.00000000000000711 ) ) ;
#32719=DIRECTION ( 'NONE',  ( 0.7671651518153105309, 0.6414496315691445849, 2.356647714346206145E-16 ) ) ;
#32721=FACE_BOUND ( 'NONE', #150, .T. ) ;
#32724=CIRCLE ( 'NONE', #2234, 1.929199999999998028 ) ;
#32743=VECTOR ( 'NONE', #20818, 1000.000000000000000 ) ;
#32756=ORIENTED_EDGE ( 'NONE', *, *, #60462, .T. ) ;
#32760=EDGE_CURVE ( 'NONE', #37068, #355, #12822, .T. ) ;
#32762=ORIENTED_EDGE ( 'NONE', *, *, #6285, .T. ) ;
#32764=VECTOR ( 'NONE', #38446, 1000.000000000000000 ) ;
#32768=ORIENTED_EDGE ( 'NONE', *, *, #8612, .T. ) ;
#32770=DIRECTION ( 'NONE',  ( -1.836970198721029934E-16, 1.836970198721036590E-16, -1.000000000000000000 ) ) ;
#32771=EDGE_CURVE ( 'NONE', #22764, #55087, #55980, .T. ) ;
#32773=CARTESIAN_POINT ( 'NONE',  ( 9.404523737882758638, 1.466476262117154983, 54.00000000000000711 ) ) ;
#32775=CARTESIAN_POINT ( 'NONE',  ( -5.242976262117275077, -5.257023737882800418, 26.00000000000000711 ) ) ;
#32809=CARTESIAN_POINT ( 'NONE',  ( -6.835476262117327728, -10.31452373788278187, 26.00000000000000000 ) ) ;
#32815=CARTESIAN_POINT ( 'NONE',  ( 6.665817930929297752, -7.357023737882814274, 26.00000000000000000 ) ) ;
#32821=DIRECTION ( 'NONE',  ( -9.912705577010336396E-15, -1.000000000000000000, 0.000000000000000000 ) ) ;
#32825=VECTOR ( 'NONE', #44420, 1000.000000000000000 ) ;
#32826=DIRECTION ( 'NONE',  ( 1.000000000000000000, 0.000000000000000000, 0.000000000000000000 ) ) ;
#32832=FACE_OUTER_BOUND ( 'NONE', #31640, .T. ) ;
#32835=CARTESIAN_POINT ( 'NONE',  ( 3.677663764522615342, 4.135079735113118993, 26.00000000000000711 ) ) ;
#32838=CARTESIAN_POINT ( 'NONE',  ( 5.257023737882801306, 5.242976262117200470, 54.00000000000000711 ) ) ;
#32839=DIRECTION ( 'NONE',  ( 0.000000000000000000, 1.000000000000000000, 0.000000000000000000 ) ) ;
#32855=CARTESIAN_POINT ( 'NONE',  ( 6.849523737882817542, -10.50702373788281463, 26.00000000000000000 ) ) ;
#32858=VERTEX_POINT ( 'NONE', #63036 ) ;
#32861=EDGE_LOOP ( 'NONE', ( #25458, #51465, #48288, #43974 ) ) ;
#32864=EDGE_CURVE ( 'NONE', #42686, #55973, #41466, .T. ) ;
#32865=DIRECTION ( 'NONE',  ( -0.7071067811865436870, 0.7071067811865514585, 0.000000000000000000 ) ) ;
#32866=DIRECTION ( 'NONE',  ( 2.478176394252584099E-15, 1.000000000000000000, 0.000000000000000000 ) ) ;
#32868=ORIENTED_EDGE ( 'NONE', *, *, #49040, .F. ) ;
#32871=CARTESIAN_POINT ( 'NONE',  ( 7.408280051175172076, -6.789561617636949542, 54.00000000000000711 ) ) ;
#32872=LINE ( 'NONE', #13377, #614 ) ;
#32873=ORIENTED_EDGE ( 'NONE', *, *, #31431, .T. ) ;
#32875=DIRECTION ( 'NONE',  ( 9.912705577010336396E-15, 1.000000000000000000, 0.000000000000000000 ) ) ;
#32879=LINE ( 'NONE', #66078, #30283 ) ;
#32882=ORIENTED_EDGE ( 'NONE', *, *, #16149, .F. ) ;
#32893=VECTOR ( 'NONE', #58394, 1000.000000000000000 ) ;
#32895=DIRECTION ( 'NONE',  ( -0.000000000000000000, -0.000000000000000000, -1.000000000000000000 ) ) ;
#32900=EDGE_CURVE ( 'NONE', #6346, #46451, #31229, .T. ) ;
#32902=CARTESIAN_POINT ( 'NONE',  ( 3.682023737882818892, 9.897976262117202495, 54.00000000000000711 ) ) ;
#32904=CARTESIAN_POINT ( 'NONE',  ( -9.722976262117288826, -6.832023737882753522, 26.00000000000000000 ) ) ;
#32907=DIRECTION ( 'NONE',  ( 0.7671651518153006499, 0.6414496315691565753, 0.000000000000000000 ) ) ;
#32910=DIRECTION ( 'NONE',  ( 1.000000000000000000, -1.260948829465469904E-14, 0.000000000000000000 ) ) ;
#32919=DIRECTION ( 'NONE',  ( 0.000000000000000000, -1.000000000000000000, -3.673940397442059868E-16 ) ) ;
#32932=VERTEX_POINT ( 'NONE', #58446 ) ;
#32955=LINE ( 'NONE', #59485, #65749 ) ;
#32965=VERTEX_POINT ( 'NONE', #22352 ) ;
#32966=EDGE_CURVE ( 'NONE', #20506, #61285, #11710, .T. ) ;
#32969=DIRECTION ( 'NONE',  ( 1.836970198721029934E-16, 1.836970198721010706E-16, -1.000000000000000000 ) ) ;
#32970=DIRECTION ( 'NONE',  ( -1.836970198721029934E-16, 1.836970198721036590E-16, -1.000000000000000000 ) ) ;
#32974=CARTESIAN_POINT ( 'NONE',  ( 2.369523737882793135, -8.835729544836320670, 54.00000000000000711 ) ) ;
#32988=EDGE_CURVE ( 'NONE', #16520, #29410, #38605, .T. ) ;
#32998=LINE ( 'NONE', #22397, #5008 ) ;
#33001=CYLINDRICAL_SURFACE ( 'NONE', #60707, 0.1749999999999998224 ) ;
#33005=ORIENTED_EDGE ( 'NONE', *, *, #32642, .F. ) ;
#33007=ORIENTED_EDGE ( 'NONE', *, *, #37701, .T. ) ;
#33013=DIRECTION ( 'NONE',  ( 1.000000000000000000, -1.920292680692490463E-14, 1.836970198720994435E-16 ) ) ;
#33015=ORIENTED_EDGE ( 'NONE', *, *, #1675, .F. ) ;
#33022=CARTESIAN_POINT ( 'NONE',  ( 10.31452373788281562, -3.664523737882826815, 54.00000000000000711 ) ) ;
#33026=ORIENTED_EDGE ( 'NONE', *, *, #47677, .F. ) ;
#33038=EDGE_LOOP ( 'NONE', ( #34104, #43633, #4252, #61029 ) ) ;
#33047=CARTESIAN_POINT ( 'NONE',  ( 10.31452373788278187, 3.650476262117146042, 54.00000000000000711 ) ) ;
#33058=AXIS2_PLACEMENT_3D ( 'NONE', #7176, #6519, #28751 ) ;
#33063=AXIS2_PLACEMENT_3D ( 'NONE', #66734, #11599, #38827 ) ;
#33075=ORIENTED_EDGE ( 'NONE', *, *, #3051, .T. ) ;
#33078=CARTESIAN_POINT ( 'NONE',  ( -6.835476262117260227, 10.49297626211718359, 26.00000000000000711 ) ) ;
#33081=EDGE_CURVE ( 'NONE', #13295, #3338, #32064, .T. ) ;
#33083=CARTESIAN_POINT ( 'NONE',  ( 10.50702373788280219, 6.835476262117187396, 26.00000000000000711 ) ) ;
#33088=ORIENTED_EDGE ( 'NONE', *, *, #56094, .T. ) ;
#33095=CARTESIAN_POINT ( 'NONE',  ( 9.795823737882804139, 9.781776262117173104, 54.00000000000000711 ) ) ;
#33099=CARTESIAN_POINT ( 'NONE',  ( 3.682023737882786918, -9.737023737882800845, 26.00000000000000000 ) ) ;
#33104=LINE ( 'NONE', #69895, #9739 ) ;
#33128=EDGE_LOOP ( 'NONE', ( #3727, #1584, #15698, #59423 ) ) ;
#33133=VERTEX_POINT ( 'NONE', #66157 ) ;
#33136=ORIENTED_EDGE ( 'NONE', *, *, #44329, .F. ) ;
#33144=AXIS2_PLACEMENT_3D ( 'NONE', #43030, #33470, #28159 ) ;
#33155=AXIS2_PLACEMENT_3D ( 'NONE', #45373, #41124, #57037 ) ;
#33159=VECTOR ( 'NONE', #37434, 1000.000000000000114 ) ;
#33167=CARTESIAN_POINT ( 'NONE',  ( -3.667976262117228714, 9.722976262117169810, 54.00000000000000711 ) ) ;
#33172=DIRECTION ( 'NONE',  ( -1.000000000000000000, 0.000000000000000000, 0.000000000000000000 ) ) ;
#33173=CARTESIAN_POINT ( 'NONE',  ( 9.737023737882765317, 2.530476262117151709, 54.00000000000000711 ) ) ;
#33180=DIRECTION ( 'NONE',  ( -2.135044278125299371E-15, 1.000000000000000000, -0.000000000000000000 ) ) ;
#33181=CYLINDRICAL_SURFACE ( 'NONE', #33250, 0.5250000000000011324 ) ;
#33184=DIRECTION ( 'NONE',  ( -0.7071067811865446862, -0.7071067811865503483, -0.000000000000000000 ) ) ;
#33188=ORIENTED_EDGE ( 'NONE', *, *, #31972, .T. ) ;
#33189=CIRCLE ( 'NONE', #36625, 0.5250000000000003553 ) ;
#33193=LINE ( 'NONE', #33539, #42325 ) ;
#33194=ORIENTED_EDGE ( 'NONE', *, *, #60892, .T. ) ;
#33200=ORIENTED_EDGE ( 'NONE', *, *, #20865, .T. ) ;
#33206=DIRECTION ( 'NONE',  ( -1.836970198721029934E-16, -1.836970198721010706E-16, 1.000000000000000000 ) ) ;
#33212=ORIENTED_EDGE ( 'NONE', *, *, #67721, .T. ) ;
#33216=CARTESIAN_POINT ( 'NONE',  ( 8.580623737882818958, -8.930623737882845248, 26.00000000000000000 ) ) ;
#33217=ORIENTED_EDGE ( 'NONE', *, *, #27090, .T. ) ;
#33224=EDGE_CURVE ( 'NONE', #34394, #58172, #23713, .T. ) ;
#33225=VERTEX_POINT ( 'NONE', #45619 ) ;
#33232=ADVANCED_FACE ( 'NONE', ( #62238 ), #52713, .F. ) ;
#33234=DIRECTION ( 'NONE',  ( -1.836970198721029934E-16, -1.836970198721010706E-16, 1.000000000000000000 ) ) ;
#33241=DIRECTION ( 'NONE',  ( 0.000000000000000000, 3.673940397442059868E-16, -1.000000000000000000 ) ) ;
#33244=ORIENTED_EDGE ( 'NONE', *, *, #47002, .F. ) ;
#33250=AXIS2_PLACEMENT_3D ( 'NONE', #27883, #22579, #17261 ) ;
#33257=CYLINDRICAL_SURFACE ( 'NONE', #32703, 1.224999999999997868 ) ;
#33261=DIRECTION ( 'NONE',  ( 0.000000000000000000, 3.673940397442059868E-16, -1.000000000000000000 ) ) ;
#33268=AXIS2_PLACEMENT_3D ( 'NONE', #47866, #5453, #54575 ) ;
#33291=ORIENTED_EDGE ( 'NONE', *, *, #32110, .T. ) ;
#33307=ORIENTED_EDGE ( 'NONE', *, *, #60427, .T. ) ;
#33309=EDGE_CURVE ( 'NONE', #2756, #21626, #68957, .T. ) ;
#33319=CARTESIAN_POINT ( 'NONE',  ( -9.547976262117256141, 2.530476262117183683, 54.00000000000000711 ) ) ;
#33340=ORIENTED_EDGE ( 'NONE', *, *, #25163, .T. ) ;
#33352=VECTOR ( 'NONE', #63994, 1000.000000000000000 ) ;
#33356=CIRCLE ( 'NONE', #42391, 0.1749999999999989342 ) ;
#33357=CIRCLE ( 'NONE', #608, 0.1749999999999998224 ) ;
#33369=AXIS2_PLACEMENT_3D ( 'NONE', #48017, #63591, #36713 ) ;
#33375=EDGE_CURVE ( 'NONE', #19854, #53029, #36600, .T. ) ;
#33376=CARTESIAN_POINT ( 'NONE',  ( 9.562023737882805463, 8.130476262117184660, 54.00000000000000711 ) ) ;
#33384=EDGE_CURVE ( 'NONE', #13545, #42109, #43467, .T. ) ;
#33397=CIRCLE ( 'NONE', #4084, 1.224999999999999423 ) ;
#33400=ORIENTED_EDGE ( 'NONE', *, *, #65253, .T. ) ;
#33405=AXIS2_PLACEMENT_3D ( 'NONE', #4844, #64248, #47622 ) ;
#33411=AXIS2_PLACEMENT_3D ( 'NONE', #22822, #21787, #28460 ) ;
#33412=VECTOR ( 'NONE', #2516, 1000.000000000000000 ) ;
#33417=DIRECTION ( 'NONE',  ( 1.000000000000000000, -1.261617073437657735E-14, 0.000000000000000000 ) ) ;
#33421=ORIENTED_EDGE ( 'NONE', *, *, #48780, .T. ) ;
#33422=FACE_OUTER_BOUND ( 'NONE', #38455, .T. ) ;
#33423=EDGE_CURVE ( 'NONE', #14823, #961, #65049, .T. ) ;
#33425=CARTESIAN_POINT ( 'NONE',  ( 10.05377373788278739, -9.703773737882823269, 54.00000000000000711 ) ) ;
#33427=EDGE_CURVE ( 'NONE', #65287, #12110, #59222, .T. ) ;
#33429=LINE ( 'NONE', #65603, #64079 ) ;
#33434=CARTESIAN_POINT ( 'NONE',  ( -5.779227145995285753, -4.155633711806640207, 54.00000000000000711 ) ) ;
#33446=CARTESIAN_POINT ( 'NONE',  ( 8.835729544836338434, -8.144523737882822800, 54.00000000000000711 ) ) ;
#33452=EDGE_LOOP ( 'NONE', ( #11214, #65328, #33543, #31164 ) ) ;
#33456=CARTESIAN_POINT ( 'NONE',  ( 3.724485858128679716, 7.394232575409564134, 26.00000000000000711 ) ) ;
#33470=DIRECTION ( 'NONE',  ( -1.836970198721029934E-16, 1.836970198721036344E-16, -1.000000000000000000 ) ) ;
#33474=ADVANCED_FACE ( 'NONE', ( #22264 ), #16954, .F. ) ;
#33475=ORIENTED_EDGE ( 'NONE', *, *, #35375, .F. ) ;
#33486=CARTESIAN_POINT ( 'NONE',  ( -3.842976262117327124, -10.31452373788281207, 26.00000000000000000 ) ) ;
#33495=VECTOR ( 'NONE', #10828, 1000.000000000000000 ) ;
#33507=DIRECTION ( 'NONE',  ( 1.356437060717832013E-15, 1.000000000000000000, 0.000000000000000000 ) ) ;
#33510=VECTOR ( 'NONE', #65340, 1000.000000000000000 ) ;
#33512=ORIENTED_EDGE ( 'NONE', *, *, #18044, .T. ) ;
#33519=DIRECTION ( 'NONE',  ( -1.836970198721029934E-16, 1.836970198721036590E-16, -1.000000000000000000 ) ) ;
#33521=CARTESIAN_POINT ( 'NONE',  ( -4.459829165594022982, 6.892329165593917395, 26.00000000000000711 ) ) ;
#33523=DIRECTION ( 'NONE',  ( 0.7071067811865348052, -0.7071067811865602293, -3.278703137324831017E-30 ) ) ;
#33529=ADVANCED_FACE ( 'NONE', ( #11964 ), #17285, .T. ) ;
#33531=FACE_OUTER_BOUND ( 'NONE', #38575, .T. ) ;
#33532=CARTESIAN_POINT ( 'NONE',  ( -8.566576262117260754, 9.689726262117185129, 26.00000000000000711 ) ) ;
#33539=CARTESIAN_POINT ( 'NONE',  ( -5.538810540050023157, 7.342976262117183239, 54.00000000000000711 ) ) ;
#33542=CARTESIAN_POINT ( 'NONE',  ( -2.617976262117287956, -6.501044194225499062, 26.00000000000000711 ) ) ;
#33543=ORIENTED_EDGE ( 'NONE', *, *, #23564, .F. ) ;
#33545=EDGE_CURVE ( 'NONE', #42663, #45572, #13373, .T. ) ;
#33548=DIRECTION ( 'NONE',  ( 1.000000000000000000, 0.000000000000000000, 0.000000000000000000 ) ) ;
#33549=DIRECTION ( 'NONE',  ( -1.836970198721029934E-16, 1.836970198721036590E-16, -1.000000000000000000 ) ) ;
#33550=EDGE_CURVE ( 'NONE', #67635, #20187, #50842, .T. ) ;
#33555=VECTOR ( 'NONE', #25382, 1000.000000000000000 ) ;
#33559=DIRECTION ( 'NONE',  ( -0.000000000000000000, 3.673940397442059868E-16, -1.000000000000000000 ) ) ;
#33567=EDGE_CURVE ( 'NONE', #21827, #10161, #34219, .T. ) ;
#33576=CARTESIAN_POINT ( 'NONE',  ( 8.930623737882843471, 8.566576262117187923, 54.00000000000000711 ) ) ;
#33580=EDGE_CURVE ( 'NONE', #51180, #9398, #18668, .T. ) ;
#33582=AXIS2_PLACEMENT_3D ( 'NONE', #40642, #41693, #46293 ) ;
#33591=FACE_OUTER_BOUND ( 'NONE', #6272, .T. ) ;
#33602=PLANE ( 'NONE',  #42342 ) ;
#33608=EDGE_CURVE ( 'NONE', #64355, #40740, #28243, .T. ) ;
#33616=ADVANCED_FACE ( 'NONE', ( #34921 ), #40237, .F. ) ;
#33621=FACE_OUTER_BOUND ( 'NONE', #35661, .T. ) ;
#33624=ORIENTED_EDGE ( 'NONE', *, *, #45582, .T. ) ;
#33626=LINE ( 'NONE', #68150, #47819 ) ;
#33634=ORIENTED_EDGE ( 'NONE', *, *, #6043, .F. ) ;
#33636=CARTESIAN_POINT ( 'NONE',  ( 5.257023737882801306, 5.242976262117200470, 54.00000000000000711 ) ) ;
#33639=CARTESIAN_POINT ( 'NONE',  ( -8.916576262117340335, -8.580623737882760338, 26.00000000000000000 ) ) ;
#33647=ORIENTED_EDGE ( 'NONE', *, *, #60427, .F. ) ;
#33648=EDGE_LOOP ( 'NONE', ( #9196, #25200, #44336, #21288 ) ) ;
#33657=VECTOR ( 'NONE', #36606, 1000.000000000000000 ) ;
#33660=ORIENTED_EDGE ( 'NONE', *, *, #23597, .F. ) ;
#33663=DIRECTION ( 'NONE',  ( -1.836970198721029934E-16, 1.836970198721036590E-16, -1.000000000000000000 ) ) ;
#33668=ORIENTED_EDGE ( 'NONE', *, *, #9058, .F. ) ;
#33677=DIRECTION ( 'NONE',  ( 0.6414496315691537998, -0.7671651518153029814, -2.309356642088714001E-17 ) ) ;
#33678=ADVANCED_FACE ( 'NONE', ( #46587 ), #19370, .F. ) ;
#33680=FACE_OUTER_BOUND ( 'NONE', #12097, .T. ) ;
#33682=FACE_OUTER_BOUND ( 'NONE', #43952, .T. ) ;
#33691=CARTESIAN_POINT ( 'NONE',  ( 7.532023737882817649, -6.665817930929303969, 54.00000000000000711 ) ) ;
#33697=EDGE_CURVE ( 'NONE', #37598, #28520, #67125, .T. ) ;
#33715=FACE_OUTER_BOUND ( 'NONE', #62140, .T. ) ;
#33718=FACE_OUTER_BOUND ( 'NONE', #35104, .T. ) ;
#33726=CARTESIAN_POINT ( 'NONE',  ( 6.849523737882818430, 10.49297626211719603, 54.00000000000000711 ) ) ;
#33727=LINE ( 'NONE', #18156, #12317 ) ;
#33728=EDGE_CURVE ( 'NONE', #46086, #45981, #3123, .T. ) ;
#33729=CARTESIAN_POINT ( 'NONE',  ( 2.420780051175169145, 8.697938382363084031, 54.00000000000000711 ) ) ;
#33730=ORIENTED_EDGE ( 'NONE', *, *, #10560, .F. ) ;
#33740=CARTESIAN_POINT ( 'NONE',  ( -5.538810540050064901, -7.357023737882800951, 54.00000000000000711 ) ) ;
#33745=CARTESIAN_POINT ( 'NONE',  ( -10.49297626211726175, 3.650476262117184234, 54.00000000000000711 ) ) ;
#33746=ORIENTED_EDGE ( 'NONE', *, *, #28567, .T. ) ;
#33748=CARTESIAN_POINT ( 'NONE',  ( 6.657023737882815873, 10.30047626211719880, 26.00000000000000711 ) ) ;
#33750=VECTOR ( 'NONE', #46312, 1000.000000000000000 ) ;
#33755=VECTOR ( 'NONE', #13310, 1000.000000000000000 ) ;
#33762=AXIS2_PLACEMENT_3D ( 'NONE', #19151, #56635, #30112 ) ;
#33763=DIRECTION ( 'NONE',  ( -0.000000000000000000, -0.000000000000000000, -1.000000000000000000 ) ) ;
#33764=LINE ( 'NONE', #67690, #11072 ) ;
#33768=LINE ( 'NONE', #66639, #32066 ) ;
#33771=FACE_OUTER_BOUND ( 'NONE', #17304, .T. ) ;
#33773=PLANE ( 'NONE',  #50355 ) ;
#33776=DIRECTION ( 'NONE',  ( -3.491481338843133355E-15, -1.000000000000000000, 0.000000000000000000 ) ) ;
#33777=DIRECTION ( 'NONE',  ( 1.000000000000000000, 5.013651664672856055E-16, 0.000000000000000000 ) ) ;
#33779=CARTESIAN_POINT ( 'NONE',  ( 7.357023737882784076, 3.834182069070697807, 54.00000000000000711 ) ) ;
#33786=CARTESIAN_POINT ( 'NONE',  ( -3.650476262117223314, 10.30047626211716683, 54.00000000000000711 ) ) ;
#33802=AXIS2_PLACEMENT_3D ( 'NONE', #58512, #10062, #31634 ) ;
#33824=DIRECTION ( 'NONE',  ( 0.7071067811865475727, -0.7071067811865475727, 0.000000000000000000 ) ) ;
#33833=ORIENTED_EDGE ( 'NONE', *, *, #31771, .F. ) ;
#33844=VERTEX_POINT ( 'NONE', #59910 ) ;
#33847=DIRECTION ( 'NONE',  ( -0.8660254037844347108, 0.5000000000000068834, 2.509347957447884214E-16 ) ) ;
#33849=VECTOR ( 'NONE', #60570, 1000.000000000000000 ) ;
#33850=LINE ( 'NONE', #17935, #61542 ) ;
#33857=ORIENTED_EDGE ( 'NONE', *, *, #59973, .F. ) ;
#33858=DIRECTION ( 'NONE',  ( 1.000000000000000000, 0.000000000000000000, 0.000000000000000000 ) ) ;
#33859=LINE ( 'NONE', #6983, #21438 ) ;
#33860=ORIENTED_EDGE ( 'NONE', *, *, #1445, .T. ) ;
#33865=CARTESIAN_POINT ( 'NONE',  ( -2.355476262117325525, -9.562023737882830332, 54.00000000000000711 ) ) ;
#33869=VECTOR ( 'NONE', #56430, 1000.000000000000114 ) ;
#33872=DIRECTION ( 'NONE',  ( 6.308085367188448025E-15, 1.000000000000000000, 3.673940397442059868E-16 ) ) ;
#33883=CIRCLE ( 'NONE', #41826, 0.1749999999999998224 ) ;
#33884=CARTESIAN_POINT ( 'NONE',  ( -6.817976262117321440, -9.737023737882781305, 26.00000000000000000 ) ) ;
#33885=ORIENTED_EDGE ( 'NONE', *, *, #38588, .F. ) ;
#33887=VECTOR ( 'NONE', #42831, 1000.000000000000000 ) ;
#33892=CARTESIAN_POINT ( 'NONE',  ( -2.355476262117313979, -8.835729544836350868, 26.00000000000000711 ) ) ;
#33901=ORIENTED_EDGE ( 'NONE', *, *, #64693, .F. ) ;
#33904=EDGE_LOOP ( 'NONE', ( #45100, #36161, #46475, #66150 ) ) ;
#33942=CARTESIAN_POINT ( 'NONE',  ( -6.817976262117261044, 9.722976262117182245, 26.00000000000000711 ) ) ;
#33945=CARTESIAN_POINT ( 'NONE',  ( -3.650476262117335668, -10.50702373788282173, 54.00000000000000711 ) ) ;
#33950=EDGE_CURVE ( 'NONE', #63093, #24327, #41117, .T. ) ;
#33965=ORIENTED_EDGE ( 'NONE', *, *, #60498, .F. ) ;
#33980=AXIS2_PLACEMENT_3D ( 'NONE', #68557, #38712, #31437 ) ;
#33986=ORIENTED_EDGE ( 'NONE', *, *, #14065, .F. ) ;
#33989=DIRECTION ( 'NONE',  ( -1.261617073437657735E-14, -1.000000000000000000, 0.000000000000000000 ) ) ;
#33990=ORIENTED_EDGE ( 'NONE', *, *, #24043, .T. ) ;
#33994=FACE_OUTER_BOUND ( 'NONE', #66908, .T. ) ;
#33996=CARTESIAN_POINT ( 'NONE',  ( 9.562023737882805463, 7.955476262117186614, 54.00000000000000711 ) ) ;
#34002=ORIENTED_EDGE ( 'NONE', *, *, #38865, .T. ) ;
#34007=DIRECTION ( 'NONE',  ( 0.7671651518152998728, -0.6414496315691575745, 2.309356642088859447E-17 ) ) ;
#34010=DIRECTION ( 'NONE',  ( -1.000000000000000000, 0.000000000000000000, 0.000000000000000000 ) ) ;
#34023=VERTEX_POINT ( 'NONE', #66938 ) ;
#34024=EDGE_LOOP ( 'NONE', ( #66955, #12912, #4383, #31122 ) ) ;
#34025=DIRECTION ( 'NONE',  ( -0.000000000000000000, 3.673940397442059868E-16, -1.000000000000000000 ) ) ;
#34028=DIRECTION ( 'NONE',  ( 1.836970198721029934E-16, 1.836970198721010706E-16, -1.000000000000000000 ) ) ;
#34034=ORIENTED_EDGE ( 'NONE', *, *, #10460, .F. ) ;
#34050=ORIENTED_EDGE ( 'NONE', *, *, #24276, .F. ) ;
#34059=EDGE_CURVE ( 'NONE', #15670, #58198, #52088, .T. ) ;
#34067=ORIENTED_EDGE ( 'NONE', *, *, #47197, .T. ) ;
#34083=ORIENTED_EDGE ( 'NONE', *, *, #38585, .F. ) ;
#34090=DIRECTION ( 'NONE',  ( -0.8660254037844510311, -0.4999999999999785727, 0.000000000000000000 ) ) ;
#34093=CIRCLE ( 'NONE', #3637, 1.929199999999997139 ) ;
#34094=CARTESIAN_POINT ( 'NONE',  ( 9.404523737882753309, 0.9414762621171547385, 54.00000000000000711 ) ) ;
#34098=EDGE_CURVE ( 'NONE', #46086, #19854, #53159, .T. ) ;
#34102=CARTESIAN_POINT ( 'NONE',  ( -6.486996718459931088, 3.142976262117182173, 54.00000000000000711 ) ) ;
#34104=ORIENTED_EDGE ( 'NONE', *, *, #58097, .T. ) ;
#34113=DIRECTION ( 'NONE',  ( 1.836970198721029934E-16, 1.836970198721010706E-16, -1.000000000000000000 ) ) ;
#34115=CARTESIAN_POINT ( 'NONE',  ( -8.916576262117358098, -9.703773737882734451, 54.00000000000000711 ) ) ;
#34121=DIRECTION ( 'NONE',  ( -1.000000000000000000, 5.120954910632640039E-15, 1.881408311965255020E-30 ) ) ;
#34125=ORIENTED_EDGE ( 'NONE', *, *, #34728, .F. ) ;
#34127=LINE ( 'NONE', #18934, #66597 ) ;
#34132=VECTOR ( 'NONE', #62326, 1000.000000000000000 ) ;
#34136=CARTESIAN_POINT ( 'NONE',  ( -3.650476262117335668, -10.50702373788282173, 54.00000000000000711 ) ) ;
#34138=ADVANCED_FACE ( 'NONE', ( #63047 ), #4704, .F. ) ;
#34157=ORIENTED_EDGE ( 'NONE', *, *, #60195, .T. ) ;
#34162=ORIENTED_EDGE ( 'NONE', *, *, #58742, .F. ) ;
#34180=DIRECTION ( 'NONE',  ( 0.000000000000000000, -3.673940397442059868E-16, 1.000000000000000000 ) ) ;
#34181=DIRECTION ( 'NONE',  ( 3.510749891857827507E-15, 1.000000000000000000, 0.000000000000000000 ) ) ;
#34182=ADVANCED_FACE ( 'NONE', ( #21664 ), #32269, .F. ) ;
#34187=CARTESIAN_POINT ( 'NONE',  ( -6.642976262117323394, -9.912023737882783792, 26.00000000000000000 ) ) ;
#34194=CARTESIAN_POINT ( 'NONE',  ( -8.821682069070780230, 7.955476262117183062, 54.00000000000000711 ) ) ;
#34197=CYLINDRICAL_SURFACE ( 'NONE', #48040, 0.1749999999999998224 ) ;
#34198=DIRECTION ( 'NONE',  ( 0.000000000000000000, -1.000000000000000000, 0.000000000000000000 ) ) ;
#34199=FACE_OUTER_BOUND ( 'NONE', #13094, .T. ) ;
#34211=ORIENTED_EDGE ( 'NONE', *, *, #34829, .F. ) ;
#34219=LINE ( 'NONE', #44492, #34348 ) ;
#34223=CARTESIAN_POINT ( 'NONE',  ( 3.664523737882778853, -10.50702373788281285, 54.00000000000000711 ) ) ;
#34224=CARTESIAN_POINT ( 'NONE',  ( 6.872275254348383378, 2.989207322240120313, 54.00000000000000711 ) ) ;
#34225=DIRECTION ( 'NONE',  ( 0.7071067811865475727, 0.7071067811865475727, -0.000000000000000000 ) ) ;
#34227=CARTESIAN_POINT ( 'NONE',  ( -3.667976262117228714, 9.722976262117169810, 54.00000000000000711 ) ) ;
#34231=EDGE_CURVE ( 'NONE', #34255, #32932, #22693, .T. ) ;
#34234=EDGE_CURVE ( 'NONE', #4514, #65565, #11720, .T. ) ;
#34239=CIRCLE ( 'NONE', #53518, 0.5249999999999990230 ) ;
#34249=ORIENTED_EDGE ( 'NONE', *, *, #7265, .T. ) ;
#34250=DIRECTION ( 'NONE',  ( 1.836970198721029934E-16, 1.836970198721010706E-16, -1.000000000000000000 ) ) ;
#34255=VERTEX_POINT ( 'NONE', #43567 ) ;
#34261=EDGE_LOOP ( 'NONE', ( #25842, #29055, #41, #7392 ) ) ;
#34263=LINE ( 'NONE', #2108, #48801 ) ;
#34265=DIRECTION ( 'NONE',  ( 1.000000000000000000, 1.671920889371702854E-15, 0.000000000000000000 ) ) ;
#34270=FACE_OUTER_BOUND ( 'NONE', #68101, .T. ) ;
#34273=EDGE_CURVE ( 'NONE', #14139, #52552, #38276, .T. ) ;
#34292=CARTESIAN_POINT ( 'NONE',  ( 8.580623737882818958, -8.930623737882855906, 54.00000000000000711 ) ) ;
#34294=VERTEX_POINT ( 'NONE', #25442 ) ;
#34297=AXIS2_PLACEMENT_3D ( 'NONE', #55678, #67345, #6882 ) ;
#34301=DIRECTION ( 'NONE',  ( -1.836970198721029934E-16, 1.836970198721036590E-16, -1.000000000000000000 ) ) ;
#34304=CARTESIAN_POINT ( 'NONE',  ( -8.227189898828699555, -1.634292677759815904, 54.00000000000000711 ) ) ;
#34305=ORIENTED_EDGE ( 'NONE', *, *, #30878, .T. ) ;
#34318=ADVANCED_FACE ( 'NONE', ( #31464 ), #48056, .F. ) ;
#34319=CARTESIAN_POINT ( 'NONE',  ( 8.093267424590464998, -8.711985858128690197, 26.00000000000000000 ) ) ;
#34334=VECTOR ( 'NONE', #11511, 1000.000000000000000 ) ;
#34335=VECTOR ( 'NONE', #22364, 1000.000000000000000 ) ;
#34336=LINE ( 'NONE', #35043, #14430 ) ;
#34338=ORIENTED_EDGE ( 'NONE', *, *, #17453, .F. ) ;
#34341=CARTESIAN_POINT ( 'NONE',  ( -5.242976262117259978, 5.242976262117182706, 54.00000000000000711 ) ) ;
#34344=DIRECTION ( 'NONE',  ( 0.6414496315691617934, -0.7671651518152962090, -2.818519042763987834E-16 ) ) ;
#34348=VECTOR ( 'NONE', #56503, 1000.000000000000000 ) ;
#34350=EDGE_LOOP ( 'NONE', ( #2861, #42865, #69285, #43979 ) ) ;
#34352=CARTESIAN_POINT ( 'NONE',  ( 10.31452373788281562, -3.664523737882826815, 54.00000000000000711 ) ) ;
#34353=ORIENTED_EDGE ( 'NONE', *, *, #30254, .F. ) ;
#34357=VECTOR ( 'NONE', #41730, 1000.000000000000000 ) ;
#34358=CARTESIAN_POINT ( 'NONE',  ( -10.03972626211722918, 9.689726262117183353, 26.00000000000000711 ) ) ;
#34368=VERTEX_POINT ( 'NONE', #4925 ) ;
#34370=CARTESIAN_POINT ( 'NONE',  ( 7.969523737882818537, -9.562023737882819674, 54.00000000000000711 ) ) ;
#34371=CARTESIAN_POINT ( 'NONE',  ( -9.915476262117200790, -0.9555237378827209360, 54.00000000000000711 ) ) ;
#34373=VERTEX_POINT ( 'NONE', #30746 ) ;
#34375=VECTOR ( 'NONE', #21450, 1000.000000000000000 ) ;
#34380=ORIENTED_EDGE ( 'NONE', *, *, #60966, .T. ) ;
#34381=FACE_OUTER_BOUND ( 'NONE', #42797, .T. ) ;
#34382=ORIENTED_EDGE ( 'NONE', *, *, #31913, .F. ) ;
#34383=ORIENTED_EDGE ( 'NONE', *, *, #22268, .T. ) ;
#34384=VECTOR ( 'NONE', #66806, 1000.000000000000000 ) ;
#34387=CARTESIAN_POINT ( 'NONE',  ( 4.961189459950039904, -7.357023737882821379, 54.00000000000000711 ) ) ;
#34394=VERTEX_POINT ( 'NONE', #63629 ) ;
#34404=VERTEX_POINT ( 'NONE', #9177 ) ;
#34407=VECTOR ( 'NONE', #49937, 1000.000000000000000 ) ;
#34409=ORIENTED_EDGE ( 'NONE', *, *, #42128, .F. ) ;
#34414=ORIENTED_EDGE ( 'NONE', *, *, #60597, .T. ) ;
#34417=CYLINDRICAL_SURFACE ( 'NONE', #42444, 1.929199999999998028 ) ;
#34419=ADVANCED_FACE ( 'NONE', ( #16220 ), #31767, .F. ) ;
#34423=CARTESIAN_POINT ( 'NONE',  ( -9.547976262117304103, -8.144523737882758851, 54.00000000000000711 ) ) ;
#34431=FACE_BOUND ( 'NONE', #11460, .T. ) ;
#34435=DIRECTION ( 'NONE',  ( -0.6414496315691415873, 0.7671651518153131954, 2.309356642089129694E-17 ) ) ;
#34441=AXIS2_PLACEMENT_3D ( 'NONE', #29803, #25210, #18485 ) ;
#34446=AXIS2_PLACEMENT_3D ( 'NONE', #6441, #5417, #43220 ) ;
#34452=EDGE_LOOP ( 'NONE', ( #53774, #28291, #26864, #3202 ) ) ;
#34455=CARTESIAN_POINT ( 'NONE',  ( -10.30047626211725031, -3.857023737882713466, 54.00000000000000711 ) ) ;
#34463=LINE ( 'NONE', #52149, #418 ) ;
#34470=DIRECTION ( 'NONE',  ( 1.047444401652940007E-14, 1.000000000000000000, 1.836970198721029934E-16 ) ) ;
#34473=AXIS2_PLACEMENT_3D ( 'NONE', #5259, #26826, #43070 ) ;
#34478=ORIENTED_EDGE ( 'NONE', *, *, #17230, .F. ) ;
#34482=PLANE ( 'NONE',  #65073 ) ;
#34486=CARTESIAN_POINT ( 'NONE',  ( 5.257023737882807524, 7.172176262117201162, 54.00000000000000711 ) ) ;
#34493=EDGE_CURVE ( 'NONE', #43115, #41827, #37758, .T. ) ;
#34494=ORIENTED_EDGE ( 'NONE', *, *, #36821, .T. ) ;
#34498=CARTESIAN_POINT ( 'NONE',  ( -4.135079735113166954, 3.663616288757006512, 54.00000000000000711 ) ) ;
#34506=DIRECTION ( 'NONE',  ( 0.000000000000000000, -0.000000000000000000, -1.000000000000000000 ) ) ;
#34509=ORIENTED_EDGE ( 'NONE', *, *, #36210, .F. ) ;
#34516=ORIENTED_EDGE ( 'NONE', *, *, #57417, .F. ) ;
#34525=DIRECTION ( 'NONE',  ( 1.920885163218982051E-15, 1.000000000000000000, 1.836970198721033139E-16 ) ) ;
#34529=ADVANCED_FACE ( 'NONE', ( #42012 ), #47315, .T. ) ;
#34535=EDGE_CURVE ( 'NONE', #55973, #46792, #64287, .T. ) ;
#34547=ORIENTED_EDGE ( 'NONE', *, *, #8787, .F. ) ;
#34548=LINE ( 'NONE', #56134, #28696 ) ;
#34569=DIRECTION ( 'NONE',  ( 0.000000000000000000, 0.000000000000000000, 1.000000000000000000 ) ) ;
#34572=ORIENTED_EDGE ( 'NONE', *, *, #3440, .T. ) ;
#34586=DIRECTION ( 'NONE',  ( -0.000000000000000000, -0.000000000000000000, -1.000000000000000000 ) ) ;
#34590=AXIS2_PLACEMENT_3D ( 'NONE', #68643, #20192, #41753 ) ;
#34595=AXIS2_PLACEMENT_3D ( 'NONE', #46453, #15337, #14293 ) ;
#34600=VERTEX_POINT ( 'NONE', #27146 ) ;
#34601=EDGE_LOOP ( 'NONE', ( #35497, #2813, #69065, #39322 ) ) ;
#34602=VECTOR ( 'NONE', #16740, 1000.000000000000114 ) ;
#34604=FACE_OUTER_BOUND ( 'NONE', #10353, .T. ) ;
#34606=ORIENTED_EDGE ( 'NONE', *, *, #37957, .T. ) ;
#34608=CIRCLE ( 'NONE', #40268, 0.1750000000000002387 ) ;
#34611=VERTEX_POINT ( 'NONE', #1638 ) ;
#34617=CARTESIAN_POINT ( 'NONE',  ( 2.544523737882787184, -9.562023737882800134, 54.00000000000000711 ) ) ;
#34621=DIRECTION ( 'NONE',  ( -0.000000000000000000, 3.673940397442059868E-16, -1.000000000000000000 ) ) ;
#34627=FACE_OUTER_BOUND ( 'NONE', #24548, .T. ) ;
#34631=CARTESIAN_POINT ( 'NONE',  ( -8.566576262117349572, -8.930623737882770641, 54.00000000000000711 ) ) ;
#34632=DIRECTION ( 'NONE',  ( 1.836970198721029934E-16, -1.836970198721036344E-16, 1.000000000000000000 ) ) ;
#34633=EDGE_CURVE ( 'NONE', #21960, #62934, #17215, .T. ) ;
#34641=CYLINDRICAL_SURFACE ( 'NONE', #49270, 0.1750000000000002387 ) ;
#34646=EDGE_CURVE ( 'NONE', #45166, #8148, #55072, .T. ) ;
#34647=EDGE_CURVE ( 'NONE', #52649, #45380, #63862, .T. ) ;
#34651=DIRECTION ( 'NONE',  ( -0.000000000000000000, -0.000000000000000000, -1.000000000000000000 ) ) ;
#34653=ORIENTED_EDGE ( 'NONE', *, *, #31250, .T. ) ;
#34663=ORIENTED_EDGE ( 'NONE', *, *, #32359, .F. ) ;
#34668=CARTESIAN_POINT ( 'NONE',  ( 5.257023737882819070, -5.257023737882825287, 54.00000000000000711 ) ) ;
#34669=DIRECTION ( 'NONE',  ( -1.203165845134433242E-14, -1.000000000000000000, -1.836970198721014403E-16 ) ) ;
#34673=CARTESIAN_POINT ( 'NONE',  ( -10.49297626211726175, 6.835476262117182955, 54.00000000000000711 ) ) ;
#34682=ORIENTED_EDGE ( 'NONE', *, *, #52764, .T. ) ;
#34701=DIRECTION ( 'NONE',  ( 0.6414496315691526895, 0.7671651518153038696, 2.587583378555111534E-16 ) ) ;
#34704=DIRECTION ( 'NONE',  ( 1.000000000000000000, -3.491481338843133355E-15, 0.000000000000000000 ) ) ;
#34718=ADVANCED_FACE ( 'NONE', ( #18599 ), #29560, .F. ) ;
#34723=LINE ( 'NONE', #6486, #48419 ) ;
#34726=ORIENTED_EDGE ( 'NONE', *, *, #15561, .F. ) ;
#34727=CARTESIAN_POINT ( 'NONE',  ( 8.612468434717241550, -2.005523737882825674, 54.00000000000000711 ) ) ;
#34728=EDGE_CURVE ( 'NONE', #5750, #48101, #51845, .T. ) ;
#34735=ORIENTED_EDGE ( 'NONE', *, *, #18131, .T. ) ;
#34744=VERTEX_POINT ( 'NONE', #2346 ) ;
#34750=DIRECTION ( 'NONE',  ( -0.7071067811865361374, 0.7071067811865588970, 2.810316974849854557E-30 ) ) ;
#34762=ORIENTED_EDGE ( 'NONE', *, *, #36754, .T. ) ;
#34764=DIRECTION ( 'NONE',  ( -1.000000000000000000, 3.903627567395476653E-15, 1.836970198721037083E-16 ) ) ;
#34766=VECTOR ( 'NONE', #60210, 1000.000000000000000 ) ;
#34774=LINE ( 'NONE', #51040, #30550 ) ;
#34787=MECHANICAL_DESIGN_GEOMETRIC_PRESENTATION_REPRESENTATION('',(#65304),#12178);
#34788=DIRECTION ( 'NONE',  ( 1.836970198721029934E-16, -1.836970198721036344E-16, 1.000000000000000000 ) ) ;
#34789=ORIENTED_EDGE ( 'NONE', *, *, #18273, .T. ) ;
#34793=FACE_OUTER_BOUND ( 'NONE', #8939, .T. ) ;
#34796=AXIS2_PLACEMENT_3D ( 'NONE', #51548, #33872, #55796 ) ;
#34800=LINE ( 'NONE', #56377, #22322 ) ;
#34804=CYLINDRICAL_SURFACE ( 'NONE', #864, 0.1749999999999998224 ) ;
#34809=EDGE_CURVE ( 'NONE', #45363, #50155, #62425, .T. ) ;
#34811=LINE ( 'NONE', #28462, #62018 ) ;
#34812=FACE_OUTER_BOUND ( 'NONE', #7354, .T. ) ;
#34814=LINE ( 'NONE', #18208, #69203 ) ;
#34815=CARTESIAN_POINT ( 'NONE',  ( 6.358413763958941978, 4.706725378239156932, 26.00000000000000711 ) ) ;
#34822=PRODUCT_DEFINITION ( 'UNKNOWN', '', #18914, #2750 ) ;
#34829=EDGE_CURVE ( 'NONE', #7825, #41567, #24377, .T. ) ;
#34832=VERTEX_POINT ( 'NONE', #8335 ) ;
#34849=ORIENTED_EDGE ( 'NONE', *, *, #61631, .F. ) ;
#34852=VECTOR ( 'NONE', #48855, 1000.000000000000000 ) ;
#34854=LINE ( 'NONE', #1636, #27043 ) ;
#34860=ORIENTED_EDGE ( 'NONE', *, *, #28657, .F. ) ;
#34864=EDGE_CURVE ( 'NONE', #41567, #59591, #9405, .T. ) ;
#34866=DIRECTION ( 'NONE',  ( 5.013651664672856055E-16, -1.000000000000000000, -3.673940397442059868E-16 ) ) ;
#34868=EDGE_CURVE ( 'NONE', #46792, #46314, #52544, .T. ) ;
#34877=CIRCLE ( 'NONE', #55249, 0.1749999999999998224 ) ;
#34896=VECTOR ( 'NONE', #9415, 1000.000000000000000 ) ;
#34898=LINE ( 'NONE', #40213, #47749 ) ;
#34912=CARTESIAN_POINT ( 'NONE',  ( -1.620245201994301665, 8.227189898828640935, 54.00000000000000711 ) ) ;
#34913=CARTESIAN_POINT ( 'NONE',  ( -3.142976262117286979, -6.501044194225493733, 26.00000000000000711 ) ) ;
#34920=CARTESIAN_POINT ( 'NONE',  ( -5.242976262117294617, -7.186223737882800222, 26.00000000000000711 ) ) ;
#34921=FACE_OUTER_BOUND ( 'NONE', #13013, .T. ) ;
#34922=AXIS2_PLACEMENT_3D ( 'NONE', #29036, #2510, #61544 ) ;
#34924=CARTESIAN_POINT ( 'NONE',  ( 9.703773737882785966, -10.05377373788282469, 54.00000000000000711 ) ) ;
#34925=PLANE ( 'NONE',  #29886 ) ;
#34928=LINE ( 'NONE', #60771, #1481 ) ;
#34929=EDGE_LOOP ( 'NONE', ( #32224, #31030, #69028, #52516 ) ) ;
#34934=VECTOR ( 'NONE', #63194, 1000.000000000000000 ) ;
#34936=EDGE_LOOP ( 'NONE', ( #11758, #46490, #54284, #27053 ) ) ;
#34937=EDGE_CURVE ( 'NONE', #5797, #55172, #52187, .T. ) ;
#34939=DIRECTION ( 'NONE',  ( 1.836970198721029934E-16, 1.836970198721010706E-16, -1.000000000000000000 ) ) ;
#34942=EDGE_CURVE ( 'NONE', #17328, #69660, #57488, .T. ) ;
#34943=CARTESIAN_POINT ( 'NONE',  ( 9.562023737882814345, -7.969523737882825642, 54.00000000000000711 ) ) ;
#34946=VERTEX_POINT ( 'NONE', #57838 ) ;
#34958=EDGE_LOOP ( 'NONE', ( #4710, #9555, #53947, #7561 ) ) ;
#34968=EDGE_CURVE ( 'NONE', #64092, #65251, #32378, .T. ) ;
#34974=ADVANCED_FACE ( 'NONE', ( #59593 ), #60267, .T. ) ;
#34990=AXIS2_PLACEMENT_3D ( 'NONE', #55295, #21726, #11790 ) ;
#34991=CIRCLE ( 'NONE', #16949, 1.929199999999998028 ) ;
#34996=LINE ( 'NONE', #36051, #46170 ) ;
#35004=VERTEX_POINT ( 'NONE', #6190 ) ;
#35011=ADVANCED_FACE ( 'NONE', ( #22460 ), #5507, .T. ) ;
#35018=DIRECTION ( 'NONE',  ( -1.000000000000000000, 1.047444401652940007E-14, -1.836970198721010706E-16 ) ) ;
#35026=EDGE_CURVE ( 'NONE', #65806, #41000, #48631, .T. ) ;
#35029=ORIENTED_EDGE ( 'NONE', *, *, #61055, .T. ) ;
#35030=EDGE_LOOP ( 'NONE', ( #23935, #40350, #8222, #11638 ) ) ;
#35043=CARTESIAN_POINT ( 'NONE',  ( -6.817976262117325881, -9.737023737882786634, 54.00000000000000711 ) ) ;
#35055=CARTESIAN_POINT ( 'NONE',  ( 2.544523737882787184, -9.562023737882791252, 26.00000000000000000 ) ) ;
#35057=VERTEX_POINT ( 'NONE', #38036 ) ;
#35058=PLANE ( 'NONE',  #58655 ) ;
#35061=DIRECTION ( 'NONE',  ( 0.000000000000000000, 1.000000000000000000, 0.000000000000000000 ) ) ;
#35066=DIRECTION ( 'NONE',  ( 1.000000000000000000, 1.570596175624152290E-15, 5.770276737693577136E-31 ) ) ;
#35068=PLANE ( 'NONE',  #4955 ) ;
#35087=EDGE_LOOP ( 'NONE', ( #23724, #22879, #11870, #35135 ) ) ;
#35088=AXIS2_PLACEMENT_3D ( 'NONE', #12522, #7216, #40454 ) ;
#35090=VERTEX_POINT ( 'NONE', #44686 ) ;
#35091=ORIENTED_EDGE ( 'NONE', *, *, #36256, .F. ) ;
#35093=LINE ( 'NONE', #8226, #4403 ) ;
#35104=EDGE_LOOP ( 'NONE', ( #53396, #52087, #2692, #49946 ) ) ;
#35125=ADVANCED_FACE ( 'NONE', ( #7210 ), #24885, .F. ) ;
#35135=ORIENTED_EDGE ( 'NONE', *, *, #24711, .T. ) ;
#35139=VECTOR ( 'NONE', #13138, 1000.000000000000000 ) ;
#35141=CARTESIAN_POINT ( 'NONE',  ( 8.144523737882817471, -9.562023737882817898, 54.00000000000000711 ) ) ;
#35159=EDGE_CURVE ( 'NONE', #6950, #44516, #68455, .T. ) ;
#35162=DIRECTION ( 'NONE',  ( 1.000000000000000000, -1.828336019306068695E-14, 0.000000000000000000 ) ) ;
#35185=CARTESIAN_POINT ( 'NONE',  ( -4.135079735113167843, 3.663616288757005623, 54.00000000000000711 ) ) ;
#35186=DIRECTION ( 'NONE',  ( 4.745709458399858621E-16, 1.000000000000000000, 1.836970198721035604E-16 ) ) ;
#35189=ORIENTED_EDGE ( 'NONE', *, *, #993, .F. ) ;
#35202=DIRECTION ( 'NONE',  ( 1.280238727658158432E-15, 1.000000000000000000, -0.000000000000000000 ) ) ;
#35207=EDGE_LOOP ( 'NONE', ( #15152, #19535, #20107, #35591 ) ) ;
#35211=LINE ( 'NONE', #39146, #38320 ) ;
#35214=FACE_OUTER_BOUND ( 'NONE', #10639, .T. ) ;
#35216=ORIENTED_EDGE ( 'NONE', *, *, #20663, .T. ) ;
#35220=CARTESIAN_POINT ( 'NONE',  ( -3.663616288757055806, 6.350872789121238426, 54.00000000000000711 ) ) ;
#35225=DIRECTION ( 'NONE',  ( 0.7071067811865475727, 0.7071067811865475727, 2.597868168706480597E-16 ) ) ;
#35231=CARTESIAN_POINT ( 'NONE',  ( 8.711985858128686644, 8.079219948824833963, 54.00000000000000711 ) ) ;
#35239=VECTOR ( 'NONE', #15390, 1000.000000000000000 ) ;
#35247=CIRCLE ( 'NONE', #53369, 0.5249999999999994671 ) ;
#35252=LINE ( 'NONE', #12991, #56259 ) ;
#35267=ORIENTED_EDGE ( 'NONE', *, *, #50852, .T. ) ;
#35297=LINE ( 'NONE', #46618, #14329 ) ;
#35299=LINE ( 'NONE', #56880, #48930 ) ;
#35304=FACE_OUTER_BOUND ( 'NONE', #41953, .T. ) ;
#35305=AXIS2_PLACEMENT_3D ( 'NONE', #13348, #56479, #9096 ) ;
#35309=CIRCLE ( 'NONE', #53427, 0.1749999999999998224 ) ;
#35321=ORIENTED_EDGE ( 'NONE', *, *, #11685, .T. ) ;
#35328=DIRECTION ( 'NONE',  ( 7.808916176531286882E-15, 1.000000000000000000, 0.000000000000000000 ) ) ;
#35331=DIRECTION ( 'NONE',  ( -0.000000000000000000, 3.673940397442059868E-16, -1.000000000000000000 ) ) ;
#35344=ORIENTED_EDGE ( 'NONE', *, *, #23166, .T. ) ;
#35347=VERTEX_POINT ( 'NONE', #368 ) ;
#35348=DIRECTION ( 'NONE',  ( 1.000000000000000000, 0.000000000000000000, 0.000000000000000000 ) ) ;
#35355=EDGE_CURVE ( 'NONE', #16502, #29534, #32195, .T. ) ;
#35360=AXIS2_PLACEMENT_3D ( 'NONE', #67705, #56055, #8664 ) ;
#35361=AXIS2_PLACEMENT_3D ( 'NONE', #19208, #40433, #61986 ) ;
#35367=VERTEX_POINT ( 'NONE', #3672 ) ;
#35375=EDGE_CURVE ( 'NONE', #37989, #38190, #54989, .T. ) ;
#35377=ORIENTED_EDGE ( 'NONE', *, *, #44000, .F. ) ;
#35378=EDGE_CURVE ( 'NONE', #55218, #4451, #60098, .T. ) ;
#35379=LINE ( 'NONE', #4631, #3691 ) ;
#35385=EDGE_CURVE ( 'NONE', #30244, #53683, #50535, .T. ) ;
#35390=CARTESIAN_POINT ( 'NONE',  ( -8.130476262117316111, -8.835729544836294025, 54.00000000000000711 ) ) ;
#35398=ADVANCED_FACE ( 'NONE', ( #23313 ), #61471, .F. ) ;
#35413=VECTOR ( 'NONE', #66236, 1000.000000000000000 ) ;
#35431=CARTESIAN_POINT ( 'NONE',  ( 7.357023737882778747, 3.834182069070702692, 26.00000000000000711 ) ) ;
#35438=ORIENTED_EDGE ( 'NONE', *, *, #47606, .F. ) ;
#35448=LINE ( 'NONE', #61266, #34132 ) ;
#35461=ORIENTED_EDGE ( 'NONE', *, *, #29316, .F. ) ;
#35464=ORIENTED_EDGE ( 'NONE', *, *, #931, .F. ) ;
#35474=CARTESIAN_POINT ( 'NONE',  ( -10.30047626211725031, -3.857023737882713466, 54.00000000000000711 ) ) ;
#35476=ORIENTED_EDGE ( 'NONE', *, *, #17117, .T. ) ;
#35481=CARTESIAN_POINT ( 'NONE',  ( -3.842976262117332453, -10.31452373788281740, 54.00000000000000711 ) ) ;
#35487=CARTESIAN_POINT ( 'NONE',  ( 9.737023737882816832, -6.832023737882823688, 54.00000000000000711 ) ) ;
#35488=DIRECTION ( 'NONE',  ( -1.000000000000000000, 0.000000000000000000, 0.000000000000000000 ) ) ;
#35494=DIRECTION ( 'NONE',  ( 0.000000000000000000, 1.000000000000000000, 0.000000000000000000 ) ) ;
#35495=PLANE ( 'NONE',  #29474 ) ;
#35497=ORIENTED_EDGE ( 'NONE', *, *, #46528, .F. ) ;
#35501=AXIS2_PLACEMENT_3D ( 'NONE', #19266, #31301, #40832 ) ;
#35505=PLANE ( 'NONE',  #38323 ) ;
#35507=FACE_OUTER_BOUND ( 'NONE', #14075, .T. ) ;
#35516=ADVANCED_FACE ( 'NONE', ( #2439 ), #24356, .F. ) ;
#35520=EDGE_CURVE ( 'NONE', #15650, #9312, #13395, .T. ) ;
#35523=VERTEX_POINT ( 'NONE', #52282 ) ;
#35531=FACE_OUTER_BOUND ( 'NONE', #55905, .T. ) ;
#35538=DIRECTION ( 'NONE',  ( 9.912705577010336396E-15, 1.000000000000000000, 0.000000000000000000 ) ) ;
#35544=DIRECTION ( 'NONE',  ( 1.047444401652940007E-14, 1.000000000000000000, 0.000000000000000000 ) ) ;
#35548=ORIENTED_EDGE ( 'NONE', *, *, #50003, .F. ) ;
#35553=ORIENTED_EDGE ( 'NONE', *, *, #31049, .F. ) ;
#35558=DIRECTION ( 'NONE',  ( -0.000000000000000000, 3.673940397442059868E-16, -1.000000000000000000 ) ) ;
#35559=CIRCLE ( 'NONE', #14119, 0.3499999999999996447 ) ;
#35563=EDGE_CURVE ( 'NONE', #17133, #29536, #49335, .T. ) ;
#35571=AXIS2_PLACEMENT_3D ( 'NONE', #1186, #61239, #55272 ) ;
#35572=CARTESIAN_POINT ( 'NONE',  ( 5.257023737882819070, -3.157023737882825198, 54.00000000000000711 ) ) ;
#35586=LINE ( 'NONE', #24996, #43550 ) ;
#35587=EDGE_CURVE ( 'NONE', #54124, #56837, #34608, .T. ) ;
#35591=ORIENTED_EDGE ( 'NONE', *, *, #26767, .T. ) ;
#35596=CARTESIAN_POINT ( 'NONE',  ( -6.344366288193421077, -4.720772854004749775, 54.00000000000000711 ) ) ;
#35600=DIRECTION ( 'NONE',  ( -1.836970198721029934E-16, 1.836970198721036590E-16, -1.000000000000000000 ) ) ;
#35604=VECTOR ( 'NONE', #67321, 1000.000000000000000 ) ;
#35606=VECTOR ( 'NONE', #25941, 1000.000000000000000 ) ;
#35613=AXIS2_PLACEMENT_3D ( 'NONE', #30685, #58610, #68863 ) ;
#35623=CARTESIAN_POINT ( 'NONE',  ( -8.916576262117260399, 8.916576262117214213, 54.00000000000000711 ) ) ;
#35624=CARTESIAN_POINT ( 'NONE',  ( -8.916576262117258622, 10.03972626211718477, 54.00000000000000711 ) ) ;
#35635=ORIENTED_EDGE ( 'NONE', *, *, #36287, .T. ) ;
#35643=CIRCLE ( 'NONE', #60485, 0.1750000000000002387 ) ;
#35654=EDGE_LOOP ( 'NONE', ( #36788, #60076, #9943, #27041 ) ) ;
#35656=VECTOR ( 'NONE', #36855, 1000.000000000000000 ) ;
#35657=AXIS2_PLACEMENT_3D ( 'NONE', #20529, #4632, #8871 ) ;
#35658=CARTESIAN_POINT ( 'NONE',  ( -7.342976262117259623, 5.538810540049946773, 26.00000000000000711 ) ) ;
#35659=CARTESIAN_POINT ( 'NONE',  ( -6.835476262117260227, 10.49297626211718359, 54.00000000000000711 ) ) ;
#35661=EDGE_LOOP ( 'NONE', ( #255, #57038, #33212, #68719 ) ) ;
#35663=ORIENTED_EDGE ( 'NONE', *, *, #32304, .T. ) ;
#35664=CARTESIAN_POINT ( 'NONE',  ( 7.969523737882818537, -9.737023737882809726, 26.00000000000000000 ) ) ;
#35668=CARTESIAN_POINT ( 'NONE',  ( -7.955476262117259445, 9.722976262117178692, 54.00000000000000711 ) ) ;
#35680=AXIS2_PLACEMENT_3D ( 'NONE', #53379, #48412, #6313 ) ;
#35681=DIRECTION ( 'NONE',  ( 7.808916176531286882E-15, 1.000000000000000000, -0.000000000000000000 ) ) ;
#35688=DIRECTION ( 'NONE',  ( 0.000000000000000000, 1.000000000000000000, 0.000000000000000000 ) ) ;
#35694=DIRECTION ( 'NONE',  ( -1.836970198721029934E-16, 1.836970198721036590E-16, -1.000000000000000000 ) ) ;
#35698=VECTOR ( 'NONE', #51334, 1000.000000000000000 ) ;
#35717=VECTOR ( 'NONE', #18334, 1000.000000000000000 ) ;
#35723=DIRECTION ( 'NONE',  ( -1.000000000000000000, 0.000000000000000000, 0.000000000000000000 ) ) ;
#35752=ORIENTED_EDGE ( 'NONE', *, *, #42722, .F. ) ;
#35760=DIRECTION ( 'NONE',  ( -0.7671651518152998728, 0.6414496315691575745, 0.000000000000000000 ) ) ;
#35764=CARTESIAN_POINT ( 'NONE',  ( 2.420780051175169145, 8.697938382363084031, 54.00000000000000711 ) ) ;
#35776=VECTOR ( 'NONE', #36071, 1000.000000000000000 ) ;
#35780=EDGE_CURVE ( 'NONE', #25974, #38025, #26822, .T. ) ;
#35781=ORIENTED_EDGE ( 'NONE', *, *, #67095, .T. ) ;
#35787=EDGE_CURVE ( 'NONE', #6189, #27468, #69602, .T. ) ;
#35791=DIRECTION ( 'NONE',  ( -0.000000000000000000, 3.673940397442059868E-16, -1.000000000000000000 ) ) ;
#35795=CARTESIAN_POINT ( 'NONE',  ( -8.130476262117259267, 8.821682069070703847, 26.00000000000000711 ) ) ;
#35799=DIRECTION ( 'NONE',  ( 1.836970198721029934E-16, 1.836970198721010706E-16, -1.000000000000000000 ) ) ;
#35812=VERTEX_POINT ( 'NONE', #69244 ) ;
#35817=DIRECTION ( 'NONE',  ( -1.000000000000000000, 8.339399738404101090E-15, -1.836970198721014896E-16 ) ) ;
#35818=CARTESIAN_POINT ( 'NONE',  ( -3.842976262117332453, -10.31452373788281740, 54.00000000000000711 ) ) ;
#35822=CARTESIAN_POINT ( 'NONE',  ( -5.779227145995285753, 4.141586236041028712, 26.00000000000000711 ) ) ;
#35834=EDGE_CURVE ( 'NONE', #50705, #51075, #58984, .T. ) ;
#35842=VECTOR ( 'NONE', #23328, 1000.000000000000000 ) ;
#35845=ADVANCED_FACE ( 'NONE', ( #65675 ), #39142, .F. ) ;
#35847=EDGE_LOOP ( 'NONE', ( #17268, #3808, #46766, #6064, #54523, #46387, #23290, #31892 ) ) ;
#35863=LINE ( 'NONE', #13943, #38526 ) ;
#35871=DIRECTION ( 'NONE',  ( -3.491481338843133355E-15, -1.000000000000000000, -1.836970198721029934E-16 ) ) ;
#35873=EDGE_CURVE ( 'NONE', #96, #27729, #50447, .T. ) ;
#35884=DIRECTION ( 'NONE',  ( -0.000000000000000000, -0.000000000000000000, -1.000000000000000000 ) ) ;
#35890=FACE_OUTER_BOUND ( 'NONE', #46239, .T. ) ;
#35900=CARTESIAN_POINT ( 'NONE',  ( 10.05377373788278739, -9.703773737882814387, 26.00000000000000000 ) ) ;
#35909=DIRECTION ( 'NONE',  ( -1.836970198721029934E-16, 1.836970198721036590E-16, -1.000000000000000000 ) ) ;
#35913=COLOUR_RGB ( '', 0.40784314, 0.44705882, 0.49803922) ;
#35914=ORIENTED_EDGE ( 'NONE', *, *, #44456, .T. ) ;
#35916=CARTESIAN_POINT ( 'NONE',  ( -5.538810540050064901, -7.357023737882800951, 54.00000000000000711 ) ) ;
#35927=EDGE_CURVE ( 'NONE', #17187, #59026, #49427, .T. ) ;
#35928=DIRECTION ( 'NONE',  ( -1.000000000000000000, 0.000000000000000000, 0.000000000000000000 ) ) ;
#35930=ORIENTED_EDGE ( 'NONE', *, *, #66831, .F. ) ;
#35931=EDGE_CURVE ( 'NONE', #15613, #15881, #3036, .T. ) ;
#35934=EDGE_CURVE ( 'NONE', #22077, #51741, #50094, .T. ) ;
#35936=FACE_OUTER_BOUND ( 'NONE', #30510, .T. ) ;
#35937=ADVANCED_FACE ( 'NONE', ( #35936 ), #13311, .F. ) ;
#35942=FACE_OUTER_BOUND ( 'NONE', #4630, .T. ) ;
#35946=DIRECTION ( 'NONE',  ( -3.491481338843133355E-15, -1.000000000000000000, -1.836970198721029934E-16 ) ) ;
#35948=CARTESIAN_POINT ( 'NONE',  ( -3.142976262117292308, -6.501044194225499062, 54.00000000000000711 ) ) ;
#35952=DIRECTION ( 'NONE',  ( -1.000000000000000000, 1.901462112903059913E-14, -1.836970198720994682E-16 ) ) ;
#35954=FACE_OUTER_BOUND ( 'NONE', #48670, .T. ) ;
#35958=CARTESIAN_POINT ( 'NONE',  ( -6.344366288193410419, 5.779227145995219139, 54.00000000000000711 ) ) ;
#35960=LINE ( 'NONE', #52587, #15200 ) ;
#35966=FACE_OUTER_BOUND ( 'NONE', #62988, .T. ) ;
#35969=VECTOR ( 'NONE', #44654, 1000.000000000000000 ) ;
#35983=ORIENTED_EDGE ( 'NONE', *, *, #24711, .F. ) ;
#35996=ORIENTED_EDGE ( 'NONE', *, *, #7262, .T. ) ;
#36010=VERTEX_POINT ( 'NONE', #56789 ) ;
#36011=AXIS2_PLACEMENT_3D ( 'NONE', #43658, #525, #16090 ) ;
#36012=DIRECTION ( 'NONE',  ( -1.836970198721029934E-16, 1.836970198721036344E-16, -1.000000000000000000 ) ) ;
#36015=CARTESIAN_POINT ( 'NONE',  ( -6.486996718459931088, 2.617976262117183150, 54.00000000000000711 ) ) ;
#36019=EDGE_CURVE ( 'NONE', #31134, #28450, #56100, .T. ) ;
#36023=DIRECTION ( 'NONE',  ( 0.000000000000000000, 3.673940397442059868E-16, -1.000000000000000000 ) ) ;
#36028=CARTESIAN_POINT ( 'NONE',  ( 4.046023737882794791, 3.142976262117205266, 54.00000000000000711 ) ) ;
#36042=ORIENTED_EDGE ( 'NONE', *, *, #20663, .F. ) ;
#36051=CARTESIAN_POINT ( 'NONE',  ( 8.580623737882845603, 8.916576262117189344, 54.00000000000000711 ) ) ;
#36056=EDGE_CURVE ( 'NONE', #21095, #67352, #28847, .T. ) ;
#36071=DIRECTION ( 'NONE',  ( 1.901462112903059913E-14, 1.000000000000000000, 1.836970198721045958E-16 ) ) ;
#36072=DIRECTION ( 'NONE',  ( 1.836970198721029934E-16, 1.836970198721010706E-16, -1.000000000000000000 ) ) ;
#36077=CARTESIAN_POINT ( 'NONE',  ( 9.703773737882785966, -8.930623737882845248, 26.00000000000000000 ) ) ;
#36089=VECTOR ( 'NONE', #32450, 1000.000000000000000 ) ;
#36090=CARTESIAN_POINT ( 'NONE',  ( -2.530476262117320907, -9.562023737882823227, 26.00000000000000711 ) ) ;
#36103=CARTESIAN_POINT ( 'NONE',  ( -9.689726262117227762, 8.566576262117216345, 54.00000000000000711 ) ) ;
#36105=VERTEX_POINT ( 'NONE', #42280 ) ;
#36107=EDGE_CURVE ( 'NONE', #19393, #55229, #15424, .T. ) ;
#36108=DIRECTION ( 'NONE',  ( -1.920292680692490463E-14, -1.000000000000000000, -1.836970198721045958E-16 ) ) ;
#36111=DIRECTION ( 'NONE',  ( 0.000000000000000000, 3.673940397442059868E-16, -1.000000000000000000 ) ) ;
#36120=ORIENTED_EDGE ( 'NONE', *, *, #35934, .F. ) ;
#36126=CARTESIAN_POINT ( 'NONE',  ( 4.720772854004775532, -4.155633711806681063, 54.00000000000000711 ) ) ;
#36137=FACE_OUTER_BOUND ( 'NONE', #6465, .T. ) ;
#36143=LINE ( 'NONE', #63733, #54720 ) ;
#36147=DIRECTION ( 'NONE',  ( -0.7071067811865398012, 0.7071067811865552333, 2.597868168706484541E-16 ) ) ;
#36149=VERTEX_POINT ( 'NONE', #48294 ) ;
#36153=DIRECTION ( 'NONE',  ( 3.304235192336781428E-15, 1.000000000000000000, 0.000000000000000000 ) ) ;
#36156=LINE ( 'NONE', #69386, #17551 ) ;
#36157=ADVANCED_FACE ( 'NONE', ( #21414 ), #69855, .F. ) ;
#36159=ORIENTED_EDGE ( 'NONE', *, *, #52892, .F. ) ;
#36161=ORIENTED_EDGE ( 'NONE', *, *, #19737, .F. ) ;
#36180=ORIENTED_EDGE ( 'NONE', *, *, #65320, .F. ) ;
#36182=AXIS2_PLACEMENT_3D ( 'NONE', #28349, #66530, #1826 ) ;
#36195=ADVANCED_FACE ( 'NONE', ( #52555 ), #25690, .F. ) ;
#36200=EDGE_LOOP ( 'NONE', ( #46753, #23616, #1212, #34789 ) ) ;
#36201=CARTESIAN_POINT ( 'NONE',  ( 7.532023737882801662, 6.651770455163677376, 26.00000000000000711 ) ) ;
#36204=CARTESIAN_POINT ( 'NONE',  ( 6.358413763958968623, -5.793274621760850174, 26.00000000000000711 ) ) ;
#36205=AXIS2_PLACEMENT_3D ( 'NONE', #64127, #46778, #25587 ) ;
#36209=CARTESIAN_POINT ( 'NONE',  ( -9.722976262117258628, 6.817976262117182884, 26.00000000000000711 ) ) ;
#36210=EDGE_CURVE ( 'NONE', #29126, #50794, #19879, .T. ) ;
#36215=AXIS2_PLACEMENT_3D ( 'NONE', #16982, #33241, #39231 ) ;
#36228=CARTESIAN_POINT ( 'NONE',  ( 3.848229544836323512, -7.357023737882812497, 54.00000000000000711 ) ) ;
#36244=CARTESIAN_POINT ( 'NONE',  ( -8.227189898828699555, -1.634292677759815904, 54.00000000000000711 ) ) ;
#36246=EDGE_LOOP ( 'NONE', ( #2313, #6540, #14242, #38107 ) ) ;
#36248=VERTEX_POINT ( 'NONE', #38379 ) ;
#36256=EDGE_CURVE ( 'NONE', #67352, #52963, #48991, .T. ) ;
#36262=EDGE_CURVE ( 'NONE', #52784, #32281, #49345, .T. ) ;
#36264=EDGE_CURVE ( 'NONE', #37820, #67667, #6305, .T. ) ;
#36269=VECTOR ( 'NONE', #34007, 999.9999999999998863 ) ;
#36272=EDGE_CURVE ( 'NONE', #28438, #25974, #17149, .T. ) ;
#36276=EDGE_CURVE ( 'NONE', #50090, #59591, #5212, .T. ) ;
#36287=EDGE_CURVE ( 'NONE', #64473, #8910, #1242, .T. ) ;
#36288=DIRECTION ( 'NONE',  ( 0.000000000000000000, 1.000000000000000000, 0.000000000000000000 ) ) ;
#36289=CARTESIAN_POINT ( 'NONE',  ( 3.003254798005743353, 6.858227778582815404, 54.00000000000000711 ) ) ;
#36294=LINE ( 'NONE', #67765, #36421 ) ;
#36305=DIRECTION ( 'NONE',  ( -0.7071067811865500152, -0.7071067811865451302, 4.683861624749757595E-31 ) ) ;
#36306=DIRECTION ( 'NONE',  ( -1.836970198721029934E-16, 1.836970198721036590E-16, -1.000000000000000000 ) ) ;
#36310=EDGE_LOOP ( 'NONE', ( #35663, #39855, #69127, #64744 ) ) ;
#36311=DIRECTION ( 'NONE',  ( 1.836970198721029934E-16, 1.836970198721010706E-16, -1.000000000000000000 ) ) ;
#36313=CARTESIAN_POINT ( 'NONE',  ( -5.538810540050023157, 7.342976262117183239, 54.00000000000000711 ) ) ;
#36315=VECTOR ( 'NONE', #29312, 1000.000000000000000 ) ;
#36323=CARTESIAN_POINT ( 'NONE',  ( 3.157023737882819425, -4.046023737882816107, 26.00000000000000711 ) ) ;
#36326=ORIENTED_EDGE ( 'NONE', *, *, #68616, .T. ) ;
#36327=AXIS2_PLACEMENT_3D ( 'NONE', #67189, #7782, #12384 ) ;
#36330=ORIENTED_EDGE ( 'NONE', *, *, #47581, .F. ) ;
#36331=EDGE_CURVE ( 'NONE', #46858, #61120, #23841, .T. ) ;
#36342=LINE ( 'NONE', #20431, #16918 ) ;
#36346=ORIENTED_EDGE ( 'NONE', *, *, #53545, .F. ) ;
#36352=ORIENTED_EDGE ( 'NONE', *, *, #48560, .F. ) ;
#36359=VECTOR ( 'NONE', #67446, 1000.000000000000000 ) ;
#36364=VECTOR ( 'NONE', #66379, 1000.000000000000114 ) ;
#36377=DIRECTION ( 'NONE',  ( -0.000000000000000000, -0.000000000000000000, -1.000000000000000000 ) ) ;
#36381=CARTESIAN_POINT ( 'NONE',  ( -8.697938382363185283, -8.093267424590415260, 54.00000000000000711 ) ) ;
#36383=DIRECTION ( 'NONE',  ( -1.000000000000000000, 0.000000000000000000, 0.000000000000000000 ) ) ;
#36388=ORIENTED_EDGE ( 'NONE', *, *, #2138, .F. ) ;
#36390=VECTOR ( 'NONE', #33184, 1000.000000000000114 ) ;
#36394=ORIENTED_EDGE ( 'NONE', *, *, #12999, .T. ) ;
#36397=ORIENTED_EDGE ( 'NONE', *, *, #15102, .T. ) ;
#36400=DIRECTION ( 'NONE',  ( -0.000000000000000000, -0.000000000000000000, -1.000000000000000000 ) ) ;
#36408=ORIENTED_EDGE ( 'NONE', *, *, #64693, .T. ) ;
#36410=ADVANCED_FACE ( 'NONE', ( #7918 ), #50708, .F. ) ;
#36412=EDGE_CURVE ( 'NONE', #64953, #41781, #28785, .T. ) ;
#36417=ORIENTED_EDGE ( 'NONE', *, *, #48821, .F. ) ;
#36421=VECTOR ( 'NONE', #45847, 1000.000000000000000 ) ;
#36425=DIRECTION ( 'NONE',  ( 0.000000000000000000, 0.000000000000000000, 1.000000000000000000 ) ) ;
#36429=VERTEX_POINT ( 'NONE', #56717 ) ;
#36430=CARTESIAN_POINT ( 'NONE',  ( -8.916576262117260399, 8.916576262117214213, 26.00000000000000711 ) ) ;
#36436=ORIENTED_EDGE ( 'NONE', *, *, #16425, .T. ) ;
#36438=CARTESIAN_POINT ( 'NONE',  ( 5.257023737882819070, -4.032023737882826531, 54.00000000000000711 ) ) ;
#36446=ORIENTED_EDGE ( 'NONE', *, *, #53912, .T. ) ;
#36453=DIRECTION ( 'NONE',  ( 0.000000000000000000, 1.000000000000000000, 0.000000000000000000 ) ) ;
#36462=CARTESIAN_POINT ( 'NONE',  ( -5.242976262117280406, -5.257023737882805747, 54.00000000000000711 ) ) ;
#36469=AXIS2_PLACEMENT_3D ( 'NONE', #62504, #39304, #807 ) ;
#36472=DIRECTION ( 'NONE',  ( 1.000000000000000000, 0.000000000000000000, 0.000000000000000000 ) ) ;
#36477=AXIS2_PLACEMENT_3D ( 'NONE', #34227, #8059, #12314 ) ;
#36489=VERTEX_POINT ( 'NONE', #63431 ) ;
#36491=AXIS2_PLACEMENT_3D ( 'NONE', #20655, #26672, #42580 ) ;
#36495=VECTOR ( 'NONE', #47624, 1000.000000000000000 ) ;
#36509=DIRECTION ( 'NONE',  ( 1.836970198721029934E-16, -1.836970198721036344E-16, 1.000000000000000000 ) ) ;
#36512=CIRCLE ( 'NONE', #8281, 1.929199999999998916 ) ;
#36515=ORIENTED_EDGE ( 'NONE', *, *, #12682, .F. ) ;
#36524=ORIENTED_EDGE ( 'NONE', *, *, #23273, .F. ) ;
#36532=ORIENTED_EDGE ( 'NONE', *, *, #29304, .F. ) ;
#36536=ORIENTED_EDGE ( 'NONE', *, *, #23325, .T. ) ;
#36537=VECTOR ( 'NONE', #32228, 1000.000000000000000 ) ;
#36550=LINE ( 'NONE', #42203, #56066 ) ;
#36555=DIRECTION ( 'NONE',  ( -1.000000000000000000, 0.000000000000000000, 0.000000000000000000 ) ) ;
#36563=EDGE_CURVE ( 'NONE', #67923, #27113, #15404, .T. ) ;
#36576=DIRECTION ( 'NONE',  ( -1.836970198721029934E-16, 1.836970198721036590E-16, -1.000000000000000000 ) ) ;
#36579=DIRECTION ( 'NONE',  ( -0.7671651518153105309, 0.6414496315691445849, 2.356647714346206145E-16 ) ) ;
#36583=EDGE_CURVE ( 'NONE', #36864, #4457, #36550, .T. ) ;
#36584=AXIS2_PLACEMENT_3D ( 'NONE', #36761, #30398, #4584 ) ;
#36585=AXIS2_PLACEMENT_3D ( 'NONE', #14349, #46504, #68079 ) ;
#36586=CARTESIAN_POINT ( 'NONE',  ( -1.620245201994373385, -8.241237374594328813, 54.00000000000000711 ) ) ;
#36589=DIRECTION ( 'NONE',  ( -4.956352788505168198E-15, -1.000000000000000000, 0.000000000000000000 ) ) ;
#36593=VECTOR ( 'NONE', #18472, 1000.000000000000000 ) ;
#36599=ADVANCED_FACE ( 'NONE', ( #10039 ), #31614, .T. ) ;
#36600=CIRCLE ( 'NONE', #20799, 0.1749999999999998224 ) ;
#36603=CARTESIAN_POINT ( 'NONE',  ( 8.241237374594247100, 1.620245201994230611, 54.00000000000000711 ) ) ;
#36606=DIRECTION ( 'NONE',  ( -1.836970198721029934E-16, 1.836970198721036590E-16, -1.000000000000000000 ) ) ;
#36608=ORIENTED_EDGE ( 'NONE', *, *, #39908, .T. ) ;
#36619=ORIENTED_EDGE ( 'NONE', *, *, #15675, .T. ) ;
#36623=CARTESIAN_POINT ( 'NONE',  ( -3.834182069070823040, -7.357023737882818715, 54.00000000000000711 ) ) ;
#36625=AXIS2_PLACEMENT_3D ( 'NONE', #31635, #26320, #27368 ) ;
#36628=EDGE_CURVE ( 'NONE', #57897, #36105, #48162, .T. ) ;
#36643=CIRCLE ( 'NONE', #33268, 0.3499999999999996447 ) ;
#36645=AXIS2_PLACEMENT_3D ( 'NONE', #13718, #19030, #56845 ) ;
#36646=EDGE_CURVE ( 'NONE', #11146, #54627, #49277, .T. ) ;
#36648=VERTEX_POINT ( 'NONE', #49932 ) ;
#36667=EDGE_CURVE ( 'NONE', #16772, #65595, #6472, .T. ) ;
#36671=CARTESIAN_POINT ( 'NONE',  ( -8.598420958951683346, 1.991476262117183316, 26.00000000000000711 ) ) ;
#36674=EDGE_CURVE ( 'NONE', #56714, #34394, #18765, .T. ) ;
#36676=LINE ( 'NONE', #15806, #47379 ) ;
#36690=EDGE_CURVE ( 'NONE', #10380, #68245, #11416, .T. ) ;
#36696=AXIS2_PLACEMENT_3D ( 'NONE', #49142, #48103, #10274 ) ;
#36703=ORIENTED_EDGE ( 'NONE', *, *, #69159, .F. ) ;
#36704=ORIENTED_EDGE ( 'NONE', *, *, #6823, .F. ) ;
#36705=EDGE_CURVE ( 'NONE', #23856, #63336, #21691, .T. ) ;
#36712=VERTEX_POINT ( 'NONE', #133 ) ;
#36713=DIRECTION ( 'NONE',  ( -0.6414496315691526895, -0.7671651518153038696, 0.000000000000000000 ) ) ;
#36716=VECTOR ( 'NONE', #54913, 1000.000000000000000 ) ;
#36728=CYLINDRICAL_SURFACE ( 'NONE', #9684, 0.5249999999999990230 ) ;
#36734=ADVANCED_FACE ( 'NONE', ( #12779 ), #3243, .T. ) ;
#36736=FACE_OUTER_BOUND ( 'NONE', #54646, .T. ) ;
#36754=EDGE_CURVE ( 'NONE', #62419, #13697, #45310, .T. ) ;
#36755=DIRECTION ( 'NONE',  ( -0.000000000000000000, 3.673940397442059868E-16, -1.000000000000000000 ) ) ;
#36757=VECTOR ( 'NONE', #3819, 1000.000000000000000 ) ;
#36761=CARTESIAN_POINT ( 'NONE',  ( -2.406732575409671337, -8.711985858128709737, 54.00000000000000711 ) ) ;
#36773=VECTOR ( 'NONE', #23158, 1000.000000000000000 ) ;
#36776=CARTESIAN_POINT ( 'NONE',  ( 8.241237374594303944, -1.634292677759877410, 26.00000000000000711 ) ) ;
#36777=ORIENTED_EDGE ( 'NONE', *, *, #43846, .T. ) ;
#36785=CARTESIAN_POINT ( 'NONE',  ( 7.532023737882806103, 6.651770455163672047, 54.00000000000000711 ) ) ;
#36788=ORIENTED_EDGE ( 'NONE', *, *, #10808, .T. ) ;
#36799=LINE ( 'NONE', #8860, #8194 ) ;
#36807=CIRCLE ( 'NONE', #31153, 0.1749999999999998224 ) ;
#36809=VERTEX_POINT ( 'NONE', #55592 ) ;
#36818=AXIS2_PLACEMENT_3D ( 'NONE', #55746, #50775, #13301 ) ;
#36821=EDGE_CURVE ( 'NONE', #57153, #61785, #36867, .T. ) ;
#36823=PLANE ( 'NONE',  #47534 ) ;
#36855=DIRECTION ( 'NONE',  ( -1.836970198721029934E-16, 1.836970198721036590E-16, -1.000000000000000000 ) ) ;
#36857=DIRECTION ( 'NONE',  ( -1.000000000000000000, 2.309061475090597584E-14, 0.000000000000000000 ) ) ;
#36864=VERTEX_POINT ( 'NONE', #30109 ) ;
#36867=CIRCLE ( 'NONE', #45862, 1.929199999999998028 ) ;
#36893=CARTESIAN_POINT ( 'NONE',  ( -2.406732575409671337, -8.711985858128709737, 54.00000000000000711 ) ) ;
#36894=ORIENTED_EDGE ( 'NONE', *, *, #59583, .F. ) ;
#36898=PLANE ( 'NONE',  #36205 ) ;
#36903=ORIENTED_EDGE ( 'NONE', *, *, #47130, .T. ) ;
#36904=VECTOR ( 'NONE', #12690, 1000.000000000000114 ) ;
#36909=AXIS2_PLACEMENT_3D ( 'NONE', #51085, #56739, #35162 ) ;
#36913=CARTESIAN_POINT ( 'NONE',  ( -6.822336235477446387, 4.135079735113101229, 54.00000000000000711 ) ) ;
#36916=DIRECTION ( 'NONE',  ( 1.000000000000000000, 0.000000000000000000, 0.000000000000000000 ) ) ;
#36926=AXIS2_PLACEMENT_3D ( 'NONE', #30007, #8430, #46971 ) ;
#36927=EDGE_CURVE ( 'NONE', #56572, #27049, #64062, .T. ) ;
#36931=VERTEX_POINT ( 'NONE', #26213 ) ;
#36932=AXIS2_PLACEMENT_3D ( 'NONE', #40373, #61931, #8889 ) ;
#36935=EDGE_CURVE ( 'NONE', #9829, #47150, #17711, .T. ) ;
#36939=ORIENTED_EDGE ( 'NONE', *, *, #31398, .T. ) ;
#36944=CARTESIAN_POINT ( 'NONE',  ( -3.650476262117335668, -10.50702373788282173, 54.00000000000000711 ) ) ;
#36954=AXIS2_PLACEMENT_3D ( 'NONE', #39834, #60725, #6636 ) ;
#36967=EDGE_CURVE ( 'NONE', #6666, #29645, #4206, .T. ) ;
#36984=EDGE_LOOP ( 'NONE', ( #69487, #14704, #21508, #64518 ) ) ;
#36988=DIRECTION ( 'NONE',  ( -1.836970198721029934E-16, 1.836970198721036590E-16, -1.000000000000000000 ) ) ;
#36994=AXIS2_PLACEMENT_3D ( 'NONE', #10057, #69096, #46816 ) ;
#36998=VECTOR ( 'NONE', #46384, 1000.000000000000000 ) ;
#37002=EDGE_CURVE ( 'NONE', #65543, #2608, #24481, .T. ) ;
#37003=VECTOR ( 'NONE', #23363, 1000.000000000000000 ) ;
#37009=EDGE_CURVE ( 'NONE', #42510, #6950, #25871, .T. ) ;
#37018=DIRECTION ( 'NONE',  ( -1.678252938371784572E-14, -1.000000000000000000, -1.836970198721041520E-16 ) ) ;
#37019=DIRECTION ( 'NONE',  ( -0.000000000000000000, 3.673940397442059868E-16, -1.000000000000000000 ) ) ;
#37022=LINE ( 'NONE', #26393, #6507 ) ;
#37023=CARTESIAN_POINT ( 'NONE',  ( -6.642976262117260333, 10.30047626211718104, 54.00000000000000711 ) ) ;
#37024=EDGE_CURVE ( 'NONE', #60715, #63093, #58402, .T. ) ;
#37026=VECTOR ( 'NONE', #37018, 1000.000000000000000 ) ;
#37035=DIRECTION ( 'NONE',  ( -0.000000000000000000, -0.000000000000000000, -1.000000000000000000 ) ) ;
#37041=CARTESIAN_POINT ( 'NONE',  ( -6.642976262117328723, -9.912023737882789121, 54.00000000000000711 ) ) ;
#37047=VERTEX_POINT ( 'NONE', #21944 ) ;
#37052=ORIENTED_EDGE ( 'NONE', *, *, #57253, .F. ) ;
#37059=CARTESIAN_POINT ( 'NONE',  ( -7.394232575409614761, 3.710438382363058896, 54.00000000000000711 ) ) ;
#37068=VERTEX_POINT ( 'NONE', #28283 ) ;
#37071=DIRECTION ( 'NONE',  ( 1.000000000000000000, -6.308085367188448025E-15, 0.000000000000000000 ) ) ;
#37073=AXIS2_PLACEMENT_3D ( 'NONE', #18193, #60973, #28454 ) ;
#37080=EDGE_CURVE ( 'NONE', #40018, #43115, #43162, .T. ) ;
#37084=PLANE ( 'NONE',  #58844 ) ;
#37086=CARTESIAN_POINT ( 'NONE',  ( -2.617976262117251540, 6.486996718459834277, 54.00000000000000711 ) ) ;
#37087=FACE_OUTER_BOUND ( 'NONE', #54979, .T. ) ;
#37091=CARTESIAN_POINT ( 'NONE',  ( -7.955476262117317177, -8.835729544836295801, 54.00000000000000711 ) ) ;
#37094=CARTESIAN_POINT ( 'NONE',  ( -6.858227778582845602, -3.003254798005714488, 54.00000000000000711 ) ) ;
#37099=ORIENTED_EDGE ( 'NONE', *, *, #31049, .T. ) ;
#37102=LINE ( 'NONE', #15873, #43575 ) ;
#37103=EDGE_CURVE ( 'NONE', #1387, #19218, #18815, .T. ) ;
#37120=CARTESIAN_POINT ( 'NONE',  ( -6.835476262117334834, -10.50702373788278798, 54.00000000000000711 ) ) ;
#37123=ORIENTED_EDGE ( 'NONE', *, *, #41959, .F. ) ;
#37127=ORIENTED_EDGE ( 'NONE', *, *, #35355, .T. ) ;
#37128=PLANE ( 'NONE',  #922 ) ;
#37133=ORIENTED_EDGE ( 'NONE', *, *, #23918, .T. ) ;
#37138=DIRECTION ( 'NONE',  ( -0.000000000000000000, 1.000000000000000000, 3.673940397442059868E-16 ) ) ;
#37154=AXIS2_PLACEMENT_3D ( 'NONE', #52799, #48176, #15652 ) ;
#37155=CARTESIAN_POINT ( 'NONE',  ( -8.598420958951683346, 1.466476262117183182, 54.00000000000000711 ) ) ;
#37170=DIRECTION ( 'NONE',  ( 1.836970198721029934E-16, -1.836970198721036344E-16, 1.000000000000000000 ) ) ;
#37171=ORIENTED_EDGE ( 'NONE', *, *, #990, .T. ) ;
#37184=DIRECTION ( 'NONE',  ( -0.000000000000000000, 3.673940397442059868E-16, -1.000000000000000000 ) ) ;
#37188=ORIENTED_EDGE ( 'NONE', *, *, #36276, .F. ) ;
#37191=EDGE_CURVE ( 'NONE', #11281, #15650, #45846, .T. ) ;
#37192=ORIENTED_EDGE ( 'NONE', *, *, #7332, .T. ) ;
#37195=DIRECTION ( 'NONE',  ( 0.7671651518153105309, -0.6414496315691445849, 0.000000000000000000 ) ) ;
#37222=CARTESIAN_POINT ( 'NONE',  ( -10.49297626211726175, 6.835476262117182955, 54.00000000000000711 ) ) ;
#37226=VECTOR ( 'NONE', #28417, 1000.000000000000000 ) ;
#37236=CARTESIAN_POINT ( 'NONE',  ( -5.242976262117275077, -5.257023737882800418, 26.00000000000000711 ) ) ;
#37238=CARTESIAN_POINT ( 'NONE',  ( 7.357023737882817827, -3.848229544836346605, 54.00000000000000711 ) ) ;
#37243=CYLINDRICAL_SURFACE ( 'NONE', #10223, 1.224999999999998757 ) ;
#37244=ORIENTED_EDGE ( 'NONE', *, *, #34937, .T. ) ;
#37247=ORIENTED_EDGE ( 'NONE', *, *, #8550, .T. ) ;
#37249=ORIENTED_EDGE ( 'NONE', *, *, #16604, .F. ) ;
#37271=ORIENTED_EDGE ( 'NONE', *, *, #11354, .F. ) ;
#37277=AXIS2_PLACEMENT_3D ( 'NONE', #45752, #35488, #20289 ) ;
#37287=DIRECTION ( 'NONE',  ( 1.836970198721029934E-16, 1.836970198721010706E-16, -1.000000000000000000 ) ) ;
#37293=LINE ( 'NONE', #4075, #69308 ) ;
#37294=CARTESIAN_POINT ( 'NONE',  ( -8.821682069070780230, 2.355476262117184305, 26.00000000000000711 ) ) ;
#37295=ORIENTED_EDGE ( 'NONE', *, *, #65957, .F. ) ;
#37304=ORIENTED_EDGE ( 'NONE', *, *, #56465, .T. ) ;
#37305=VECTOR ( 'NONE', #59002, 1000.000000000000000 ) ;
#37306=DIRECTION ( 'NONE',  ( 0.000000000000000000, 1.000000000000000000, 0.000000000000000000 ) ) ;
#37309=ORIENTED_EDGE ( 'NONE', *, *, #7271, .F. ) ;
#37321=EDGE_CURVE ( 'NONE', #33225, #61431, #52568, .T. ) ;
#37333=LINE ( 'NONE', #32026, #2856 ) ;
#37335=CARTESIAN_POINT ( 'NONE',  ( -7.342976262117253405, -3.848229544836288429, 54.00000000000000711 ) ) ;
#37340=CARTESIAN_POINT ( 'NONE',  ( -8.821682069070780230, 2.530476262117183683, 26.00000000000000711 ) ) ;
#37345=VECTOR ( 'NONE', #62270, 1000.000000000000000 ) ;
#37348=ORIENTED_EDGE ( 'NONE', *, *, #13042, .T. ) ;
#37356=VECTOR ( 'NONE', #17877, 1000.000000000000000 ) ;
#37357=CARTESIAN_POINT ( 'NONE',  ( -8.130476262117324993, -9.562023737882769936, 54.00000000000000711 ) ) ;
#37365=DIRECTION ( 'NONE',  ( -4.956352788505168198E-15, -1.000000000000000000, 0.000000000000000000 ) ) ;
#37369=FACE_OUTER_BOUND ( 'NONE', #12391, .T. ) ;
#37370=ORIENTED_EDGE ( 'NONE', *, *, #1445, .F. ) ;
#37377=ORIENTED_EDGE ( 'NONE', *, *, #45644, .T. ) ;
#37381=CARTESIAN_POINT ( 'NONE',  ( -5.242976262117259978, 5.242976262117182706, 26.00000000000000711 ) ) ;
#37392=EDGE_LOOP ( 'NONE', ( #53663, #58726, #9289, #30770 ) ) ;
#37394=CARTESIAN_POINT ( 'NONE',  ( -6.817976262117322328, -9.912023737882780239, 26.00000000000000000 ) ) ;
#37400=VERTEX_POINT ( 'NONE', #31704 ) ;
#37405=ORIENTED_EDGE ( 'NONE', *, *, #1447, .T. ) ;
#37408=AXIS2_PLACEMENT_3D ( 'NONE', #52526, #19288, #35538 ) ;
#37410=EDGE_LOOP ( 'NONE', ( #29371, #46245, #2240, #29295 ) ) ;
#37412=EDGE_CURVE ( 'NONE', #51741, #22546, #43332, .T. ) ;
#37419=VERTEX_POINT ( 'NONE', #26388 ) ;
#37426=CARTESIAN_POINT ( 'NONE',  ( 10.31452373788281562, -6.849523737882823760, 54.00000000000000711 ) ) ;
#37434=DIRECTION ( 'NONE',  ( 0.7071067811865401342, -0.7071067811865550112, -1.355854680848614216E-30 ) ) ;
#37438=EDGE_CURVE ( 'NONE', #58190, #33133, #5520, .T. ) ;
#37440=VERTEX_POINT ( 'NONE', #59257 ) ;
#37441=DIRECTION ( 'NONE',  ( -0.000000000000000000, 0.000000000000000000, -1.000000000000000000 ) ) ;
#37454=EDGE_LOOP ( 'NONE', ( #51707, #42423, #55146, #48571 ) ) ;
#37462=CARTESIAN_POINT ( 'NONE',  ( 9.562023737882812569, -2.369523737882815784, 26.00000000000000711 ) ) ;
#37468=CARTESIAN_POINT ( 'NONE',  ( -6.822336235477446387, 6.350872789121265072, 54.00000000000000711 ) ) ;
#37496=ADVANCED_FACE ( 'NONE', ( #45061 ), #11839, .F. ) ;
#37499=EDGE_CURVE ( 'NONE', #18067, #9829, #33429, .T. ) ;
#37501=ORIENTED_EDGE ( 'NONE', *, *, #26485, .T. ) ;
#37504=ORIENTED_EDGE ( 'NONE', *, *, #41521, .F. ) ;
#37510=DIRECTION ( 'NONE',  ( 2.135044278125299371E-15, -1.000000000000000000, 0.000000000000000000 ) ) ;
#37518=DIRECTION ( 'NONE',  ( -0.000000000000000000, -0.000000000000000000, -1.000000000000000000 ) ) ;
#37519=ORIENTED_EDGE ( 'NONE', *, *, #13480, .F. ) ;
#37525=EDGE_CURVE ( 'NONE', #48981, #48595, #12190, .T. ) ;
#37529=CARTESIAN_POINT ( 'NONE',  ( 10.50702373788281818, -9.795823737882813020, 54.00000000000000711 ) ) ;
#37532=VERTEX_POINT ( 'NONE', #11157 ) ;
#37536=CARTESIAN_POINT ( 'NONE',  ( 1.480523737882788238, -9.404523737882794165, 54.00000000000000711 ) ) ;
#37554=DIRECTION ( 'NONE',  ( 1.034072152899299800E-14, 1.000000000000000000, 0.000000000000000000 ) ) ;
#37562=CARTESIAN_POINT ( 'NONE',  ( -6.817976262117327657, -9.912023737882785568, 54.00000000000000711 ) ) ;
#37564=EDGE_CURVE ( 'NONE', #42141, #56866, #53924, .T. ) ;
#37565=ORIENTED_EDGE ( 'NONE', *, *, #54771, .F. ) ;
#37567=CIRCLE ( 'NONE', #28497, 0.5250000000000003553 ) ;
#37573=LINE ( 'NONE', #19901, #22066 ) ;
#37574=FACE_OUTER_BOUND ( 'NONE', #10999, .T. ) ;
#37575=DIRECTION ( 'NONE',  ( -0.7071067811865514585, -0.7071067811865435759, -2.597868168706465806E-16 ) ) ;
#37577=VERTEX_POINT ( 'NONE', #40463 ) ;
#37581=ORIENTED_EDGE ( 'NONE', *, *, #59732, .F. ) ;
#37582=CARTESIAN_POINT ( 'NONE',  ( -6.817976262117261044, 9.722976262117182245, 26.00000000000000711 ) ) ;
#37585=DIRECTION ( 'NONE',  ( -0.000000000000000000, 3.673940397442059868E-16, -1.000000000000000000 ) ) ;
#37598=VERTEX_POINT ( 'NONE', #51071 ) ;
#37603=CARTESIAN_POINT ( 'NONE',  ( -6.344366288193437953, -5.793274621760813758, 26.00000000000000711 ) ) ;
#37606=EDGE_LOOP ( 'NONE', ( #29227, #33005, #21140, #43997 ) ) ;
#37612=EDGE_CURVE ( 'NONE', #45178, #62286, #31366, .T. ) ;
#37622=EDGE_CURVE ( 'NONE', #35004, #57266, #34800, .T. ) ;
#37624=CARTESIAN_POINT ( 'NONE',  ( -7.342976262117259623, 3.834182069070703580, 26.00000000000000711 ) ) ;
#37627=ADVANCED_FACE ( 'NONE', ( #29153 ), #45764, .F. ) ;
#37630=AXIS2_PLACEMENT_3D ( 'NONE', #37357, #47958, #64921 ) ;
#37636=ORIENTED_EDGE ( 'NONE', *, *, #68476, .F. ) ;
#37637=CARTESIAN_POINT ( 'NONE',  ( -8.821682069070746479, -2.544523737882736558, 26.00000000000000711 ) ) ;
#37662=DIRECTION ( 'NONE',  ( 0.000000000000000000, 1.000000000000000000, 0.000000000000000000 ) ) ;
#37663=EDGE_CURVE ( 'NONE', #27468, #59664, #23851, .T. ) ;
#37671=ORIENTED_EDGE ( 'NONE', *, *, #36563, .T. ) ;
#37679=DIRECTION ( 'NONE',  ( -0.5000000000000019984, -0.8660254037844375974, -0.000000000000000000 ) ) ;
#37683=CARTESIAN_POINT ( 'NONE',  ( -3.142976262117267883, -4.046023737882828542, 54.00000000000000711 ) ) ;
#37684=CARTESIAN_POINT ( 'NONE',  ( -4.141586236041124636, -4.720772854004768426, 26.00000000000000711 ) ) ;
#37690=VERTEX_POINT ( 'NONE', #51781 ) ;
#37696=ADVANCED_FACE ( 'NONE', ( #3339 ), #24904, .F. ) ;
#37697=ADVANCED_FACE ( 'NONE', ( #61317 ), #29850, .T. ) ;
#37700=CARTESIAN_POINT ( 'NONE',  ( 9.562023737882803687, 7.955476262117190167, 26.00000000000000711 ) ) ;
#37701=EDGE_CURVE ( 'NONE', #46952, #2701, #57777, .T. ) ;
#37709=CARTESIAN_POINT ( 'NONE',  ( -3.842976262117221875, 10.30047626211716860, 26.00000000000000711 ) ) ;
#37711=DIRECTION ( 'NONE',  ( 0.000000000000000000, -3.673940397442059868E-16, 1.000000000000000000 ) ) ;
#37712=DIRECTION ( 'NONE',  ( 1.221996412923863792E-14, 1.000000000000000000, 1.836970198721013910E-16 ) ) ;
#37713=VECTOR ( 'NONE', #29096, 1000.000000000000000 ) ;
#37714=ORIENTED_EDGE ( 'NONE', *, *, #50942, .F. ) ;
#37719=VECTOR ( 'NONE', #55089, 1000.000000000000000 ) ;
#37726=PLANE ( 'NONE',  #68834 ) ;
#37735=ORIENTED_EDGE ( 'NONE', *, *, #65404, .T. ) ;
#37737=EDGE_LOOP ( 'NONE', ( #25684, #38362, #13640, #11809 ) ) ;
#37747=EDGE_CURVE ( 'NONE', #41000, #55063, #31284, .T. ) ;
#37750=ORIENTED_EDGE ( 'NONE', *, *, #26449, .F. ) ;
#37758=LINE ( 'NONE', #15836, #5164 ) ;
#37760=VECTOR ( 'NONE', #54540, 1000.000000000000000 ) ;
#37773=DIRECTION ( 'NONE',  ( -1.000000000000000000, 0.000000000000000000, 0.000000000000000000 ) ) ;
#37774=DIRECTION ( 'NONE',  ( -7.808916176531286882E-15, -1.000000000000000000, -3.673940397442059868E-16 ) ) ;
#37780=DIRECTION ( 'NONE',  ( -1.000000000000000000, 0.000000000000000000, 0.000000000000000000 ) ) ;
#37781=CARTESIAN_POINT ( 'NONE',  ( -9.781776262117249487, 10.49297626211718359, 26.00000000000000711 ) ) ;
#37783=DIRECTION ( 'NONE',  ( -1.000000000000000000, 0.000000000000000000, 0.000000000000000000 ) ) ;
#37785=ORIENTED_EDGE ( 'NONE', *, *, #7332, .F. ) ;
#37786=CARTESIAN_POINT ( 'NONE',  ( -9.897976262117250457, -3.857023737882721903, 54.00000000000000711 ) ) ;
#37796=DIRECTION ( 'NONE',  ( -0.000000000000000000, 3.673940397442059868E-16, -1.000000000000000000 ) ) ;
#37800=CARTESIAN_POINT ( 'NONE',  ( -7.342976262117259623, 4.947141984184421304, 26.00000000000000711 ) ) ;
#37815=DIRECTION ( 'NONE',  ( 0.000000000000000000, 1.000000000000000000, 0.000000000000000000 ) ) ;
#37818=AXIS2_PLACEMENT_3D ( 'NONE', #9832, #47302, #51910 ) ;
#37819=DIRECTION ( 'NONE',  ( -1.000000000000000000, 0.000000000000000000, 0.000000000000000000 ) ) ;
#37820=VERTEX_POINT ( 'NONE', #53892 ) ;
#37824=ORIENTED_EDGE ( 'NONE', *, *, #12061, .T. ) ;
#37839=CARTESIAN_POINT ( 'NONE',  ( -8.916576262117349216, -8.930623737882767088, 54.00000000000000711 ) ) ;
#37843=LINE ( 'NONE', #53074, #2808 ) ;
#37844=CARTESIAN_POINT ( 'NONE',  ( -6.835476262117260227, 10.30047626211718104, 54.00000000000000711 ) ) ;
#37851=ORIENTED_EDGE ( 'NONE', *, *, #56565, .F. ) ;
#37856=ORIENTED_EDGE ( 'NONE', *, *, #25569, .T. ) ;
#37857=AXIS2_PLACEMENT_3D ( 'NONE', #52768, #45670, #35061 ) ;
#37858=CIRCLE ( 'NONE', #20939, 1.929199999999998028 ) ;
#37862=EDGE_LOOP ( 'NONE', ( #56348, #25105, #31912, #28421 ) ) ;
#37872=DIRECTION ( 'NONE',  ( -7.457533623526253657E-15, -1.000000000000000000, -1.836970198721024757E-16 ) ) ;
#37879=VERTEX_POINT ( 'NONE', #64839 ) ;
#37891=EDGE_CURVE ( 'NONE', #58674, #26866, #12114, .T. ) ;
#37895=CARTESIAN_POINT ( 'NONE',  ( -9.722976262117258628, 3.667976262117184749, 26.00000000000000711 ) ) ;
#37896=ADVANCED_FACE ( 'NONE', ( #33682 ), #33001, .F. ) ;
#37899=LINE ( 'NONE', #59460, #34852 ) ;
#37908=ORIENTED_EDGE ( 'NONE', *, *, #60240, .F. ) ;
#37916=CARTESIAN_POINT ( 'NONE',  ( -5.242976262117280406, -5.257023737882805747, 54.00000000000000711 ) ) ;
#37917=CARTESIAN_POINT ( 'NONE',  ( -8.079219948824961861, -8.711985858128649340, 54.00000000000000711 ) ) ;
#37918=DIRECTION ( 'NONE',  ( 0.000000000000000000, 3.673940397442059868E-16, -1.000000000000000000 ) ) ;
#37924=CARTESIAN_POINT ( 'NONE',  ( 10.31452373788280497, 6.642976262117183062, 54.00000000000000711 ) ) ;
#37929=ORIENTED_EDGE ( 'NONE', *, *, #27902, .F. ) ;
#37932=LINE ( 'NONE', #16014, #34335 ) ;
#37945=EDGE_CURVE ( 'NONE', #28048, #56362, #44625, .T. ) ;
#37950=AXIS2_PLACEMENT_3D ( 'NONE', #39070, #6884, #49350 ) ;
#37951=CARTESIAN_POINT ( 'NONE',  ( 10.05377373788278739, -9.703773737882823269, 54.00000000000000711 ) ) ;
#37954=FACE_OUTER_BOUND ( 'NONE', #11466, .T. ) ;
#37957=EDGE_CURVE ( 'NONE', #59636, #38923, #39336, .T. ) ;
#37962=DIRECTION ( 'NONE',  ( -8.339399738404099512E-15, -1.000000000000000000, 0.000000000000000000 ) ) ;
#37977=AXIS2_PLACEMENT_3D ( 'NONE', #66279, #61290, #1923 ) ;
#37983=ORIENTED_EDGE ( 'NONE', *, *, #47854, .T. ) ;
#37984=DIRECTION ( 'NONE',  ( 0.7071067811865398012, -0.7071067811865552333, 0.000000000000000000 ) ) ;
#37989=VERTEX_POINT ( 'NONE', #7144 ) ;
#37991=EDGE_CURVE ( 'NONE', #12647, #64953, #18919, .T. ) ;
#38002=CIRCLE ( 'NONE', #59445, 1.929199999999998028 ) ;
#38011=ORIENTED_EDGE ( 'NONE', *, *, #31972, .F. ) ;
#38018=EDGE_LOOP ( 'NONE', ( #5892, #50245, #66945, #20261 ) ) ;
#38020=ORIENTED_EDGE ( 'NONE', *, *, #47501, .T. ) ;
#38024=VECTOR ( 'NONE', #5232, 999.9999999999998863 ) ;
#38025=VERTEX_POINT ( 'NONE', #29079 ) ;
#38036=CARTESIAN_POINT ( 'NONE',  ( -2.355476262117229158, 9.547976262117156665, 26.00000000000000711 ) ) ;
#38040=DIRECTION ( 'NONE',  ( -1.000000000000000000, -0.000000000000000000, -0.000000000000000000 ) ) ;
#38042=ORIENTED_EDGE ( 'NONE', *, *, #5978, .F. ) ;
#38045=ADVANCED_FACE ( 'NONE', ( #18447 ), #67258, .F. ) ;
#38046=DIRECTION ( 'NONE',  ( 9.912705577010361640E-15, 1.000000000000000000, 0.000000000000000000 ) ) ;
#38052=VECTOR ( 'NONE', #60470, 1000.000000000000000 ) ;
#38060=CARTESIAN_POINT ( 'NONE',  ( 0.9555237378827827754, -9.929523737882790968, 54.00000000000000711 ) ) ;
#38083=DIRECTION ( 'NONE',  ( -0.000000000000000000, -0.000000000000000000, -1.000000000000000000 ) ) ;
#38087=LINE ( 'NONE', #59639, #13501 ) ;
#38096=ORIENTED_EDGE ( 'NONE', *, *, #36412, .T. ) ;
#38099=DIRECTION ( 'NONE',  ( -1.836970198721029934E-16, -1.836970198721010706E-16, 1.000000000000000000 ) ) ;
#38107=ORIENTED_EDGE ( 'NONE', *, *, #65871, .T. ) ;
#38122=CARTESIAN_POINT ( 'NONE',  ( 2.632023737882809744, -6.501044194225465311, 26.00000000000000711 ) ) ;
#38123=FACE_OUTER_BOUND ( 'NONE', #57697, .T. ) ;
#38127=VECTOR ( 'NONE', #26090, 1000.000000000000000 ) ;
#38140=PLANE ( 'NONE',  #62898 ) ;
#38145=DIRECTION ( 'NONE',  ( -0.5000000000000067724, -0.8660254037844345998, 0.000000000000000000 ) ) ;
#38167=ORIENTED_EDGE ( 'NONE', *, *, #44793, .T. ) ;
#38173=ADVANCED_FACE ( 'NONE', ( #55827 ), #65069, .F. ) ;
#38174=ORIENTED_EDGE ( 'NONE', *, *, #47677, .T. ) ;
#38184=ORIENTED_EDGE ( 'NONE', *, *, #67048, .F. ) ;
#38186=EDGE_CURVE ( 'NONE', #28620, #14583, #61114, .T. ) ;
#38189=DIRECTION ( 'NONE',  ( 1.836970198721029934E-16, 1.836970198721010706E-16, -1.000000000000000000 ) ) ;
#38190=VERTEX_POINT ( 'NONE', #22952 ) ;
#38192=FACE_OUTER_BOUND ( 'NONE', #56276, .T. ) ;
#38197=ORIENTED_EDGE ( 'NONE', *, *, #30643, .T. ) ;
#38199=ORIENTED_EDGE ( 'NONE', *, *, #40277, .F. ) ;
#38203=DIRECTION ( 'NONE',  ( -1.836970198721029934E-16, 1.836970198721036590E-16, -1.000000000000000000 ) ) ;
#38206=VECTOR ( 'NONE', #20221, 1000.000000000000000 ) ;
#38208=ORIENTED_EDGE ( 'NONE', *, *, #16289, .T. ) ;
#38218=DIRECTION ( 'NONE',  ( 1.836970198721029934E-16, 1.836970198721010706E-16, -1.000000000000000000 ) ) ;
#38220=ORIENTED_EDGE ( 'NONE', *, *, #9114, .F. ) ;
#38221=CARTESIAN_POINT ( 'NONE',  ( 6.358413763958946419, 4.706725378239151603, 54.00000000000000711 ) ) ;
#38239=EDGE_CURVE ( 'NONE', #29684, #7626, #32879, .T. ) ;
#38265=DIRECTION ( 'NONE',  ( 0.7071067811865550112, 0.7071067811865401342, 2.597868168706466299E-16 ) ) ;
#38269=CARTESIAN_POINT ( 'NONE',  ( 10.50702373788281996, -6.849523737882823760, 54.00000000000000711 ) ) ;
#38276=LINE ( 'NONE', #37582, #26564 ) ;
#38292=ORIENTED_EDGE ( 'NONE', *, *, #51138, .F. ) ;
#38293=PLANE ( 'NONE',  #14738 ) ;
#38298=DIRECTION ( 'NONE',  ( 1.836970198721029934E-16, 1.836970198721010706E-16, -1.000000000000000000 ) ) ;
#38302=DIRECTION ( 'NONE',  ( 3.491481338843133355E-15, 1.000000000000000000, 0.000000000000000000 ) ) ;
#38314=DIRECTION ( 'NONE',  ( -1.000000000000000000, 0.000000000000000000, 0.000000000000000000 ) ) ;
#38320=VECTOR ( 'NONE', #18256, 1000.000000000000000 ) ;
#38322=CARTESIAN_POINT ( 'NONE',  ( 3.003254798005738468, 6.858227778582820733, 26.00000000000000711 ) ) ;
#38323=AXIS2_PLACEMENT_3D ( 'NONE', #46476, #53211, #19601 ) ;
#38325=ORIENTED_EDGE ( 'NONE', *, *, #19552, .T. ) ;
#38335=CARTESIAN_POINT ( 'NONE',  ( 4.961189459950039904, -7.357023737882811609, 26.00000000000000000 ) ) ;
#38341=VERTEX_POINT ( 'NONE', #39889 ) ;
#38360=ORIENTED_EDGE ( 'NONE', *, *, #32304, .F. ) ;
#38362=ORIENTED_EDGE ( 'NONE', *, *, #36019, .F. ) ;
#38364=VERTEX_POINT ( 'NONE', #7722 ) ;
#38371=ORIENTED_EDGE ( 'NONE', *, *, #27708, .F. ) ;
#38379=CARTESIAN_POINT ( 'NONE',  ( 4.155633711806649977, 4.706725378239165813, 26.00000000000000711 ) ) ;
#38399=DIRECTION ( 'NONE',  ( 0.000000000000000000, 1.000000000000000000, 3.673940397442059868E-16 ) ) ;
#38400=AXIS2_PLACEMENT_3D ( 'NONE', #21447, #10488, #20399 ) ;
#38412=DIRECTION ( 'NONE',  ( -1.000000000000000000, 0.000000000000000000, 0.000000000000000000 ) ) ;
#38422=ORIENTED_EDGE ( 'NONE', *, *, #9214, .T. ) ;
#38423=EDGE_CURVE ( 'NONE', #16156, #34744, #40967, .T. ) ;
#38427=EDGE_CURVE ( 'NONE', #55973, #21406, #7739, .T. ) ;
#38435=EDGE_LOOP ( 'NONE', ( #6475, #12036, #60167, #62499 ) ) ;
#38442=ORIENTED_EDGE ( 'NONE', *, *, #26767, .F. ) ;
#38446=DIRECTION ( 'NONE',  ( -1.836970198721029934E-16, 1.836970198721036590E-16, -1.000000000000000000 ) ) ;
#38452=EDGE_CURVE ( 'NONE', #3816, #30867, #46070, .T. ) ;
#38455=EDGE_LOOP ( 'NONE', ( #28593, #60883, #32636, #15722 ) ) ;
#38456=ADVANCED_FACE ( 'NONE', ( #29656 ), #3156, .F. ) ;
#38459=DIRECTION ( 'NONE',  ( -3.304235192336773145E-15, -1.000000000000000000, 0.000000000000000000 ) ) ;
#38463=EDGE_LOOP ( 'NONE', ( #47925, #31567, #2541, #14360 ) ) ;
#38476=CARTESIAN_POINT ( 'NONE',  ( -4.135079735113167843, 6.822336235477362010, 54.00000000000000711 ) ) ;
#38479=DIRECTION ( 'NONE',  ( 0.000000000000000000, 3.673940397442059868E-16, -1.000000000000000000 ) ) ;
#38485=CARTESIAN_POINT ( 'NONE',  ( -9.547976262117300550, -7.969523737882755476, 26.00000000000000000 ) ) ;
#38486=AXIS2_PLACEMENT_3D ( 'NONE', #59674, #23215, #44768 ) ;
#38489=ADVANCED_FACE ( 'NONE', ( #30371 ), #24716, .F. ) ;
#38496=DIRECTION ( 'NONE',  ( -0.5000000000000019984, -0.8660254037844375974, -0.000000000000000000 ) ) ;
#38508=VECTOR ( 'NONE', #65449, 1000.000000000000000 ) ;
#38512=AXIS2_PLACEMENT_3D ( 'NONE', #41988, #14056, #57547 ) ;
#38513=LINE ( 'NONE', #11953, #51372 ) ;
#38521=CARTESIAN_POINT ( 'NONE',  ( -8.916576262117345664, -8.580623737882765667, 54.00000000000000711 ) ) ;
#38522=DIRECTION ( 'NONE',  ( -0.000000000000000000, -0.000000000000000000, -1.000000000000000000 ) ) ;
#38526=VECTOR ( 'NONE', #51425, 1000.000000000000000 ) ;
#38535=EDGE_CURVE ( 'NONE', #15450, #17979, #10053, .T. ) ;
#38548=CIRCLE ( 'NONE', #61124, 1.224999999999999423 ) ;
#38552=LINE ( 'NONE', #22969, #64458 ) ;
#38557=PLANE ( 'NONE',  #23461 ) ;
#38568=EDGE_LOOP ( 'NONE', ( #33990, #10858, #49231, #2949 ) ) ;
#38572=DIRECTION ( 'NONE',  ( 3.540251991789403884E-15, 1.000000000000000000, 0.000000000000000000 ) ) ;
#38575=EDGE_LOOP ( 'NONE', ( #48469, #30199, #9161, #23910 ) ) ;
#38585=EDGE_CURVE ( 'NONE', #22259, #36931, #52655, .T. ) ;
#38588=EDGE_CURVE ( 'NONE', #54361, #20807, #48406, .T. ) ;
#38591=ORIENTED_EDGE ( 'NONE', *, *, #51408, .T. ) ;
#38594=DIRECTION ( 'NONE',  ( -0.7671651518153043137, 0.6414496315691521344, 2.587583378555129776E-16 ) ) ;
#38601=ORIENTED_EDGE ( 'NONE', *, *, #38920, .F. ) ;
#38605=LINE ( 'NONE', #37917, #64831 ) ;
#38610=ORIENTED_EDGE ( 'NONE', *, *, #54940, .F. ) ;
#38617=CARTESIAN_POINT ( 'NONE',  ( 3.664523737882778853, -10.50702373788281285, 54.00000000000000711 ) ) ;
#38625=EDGE_CURVE ( 'NONE', #65963, #66645, #32390, .T. ) ;
#38626=AXIS2_PLACEMENT_3D ( 'NONE', #23677, #34632, #38908 ) ;
#38640=CARTESIAN_POINT ( 'NONE',  ( -8.821682069070829968, -8.144523737882765957, 54.00000000000000711 ) ) ;
#38646=ORIENTED_EDGE ( 'NONE', *, *, #23597, .T. ) ;
#38650=ADVANCED_FACE ( 'NONE', ( #43328, #59603, #16471, #11151, #32721, #17847, #55341, #34431, #45402, #60276 ), #28115, .T. ) ;
#38652=CARTESIAN_POINT ( 'NONE',  ( -10.49297626211725998, 9.781776262117173104, 54.00000000000000711 ) ) ;
#38662=CARTESIAN_POINT ( 'NONE',  ( 3.664523737882778853, -10.50702373788281285, 54.00000000000000711 ) ) ;
#38674=PLANE ( 'NONE',  #31200 ) ;
#38685=DIRECTION ( 'NONE',  ( 0.000000000000000000, 1.000000000000000000, 0.000000000000000000 ) ) ;
#38691=CARTESIAN_POINT ( 'NONE',  ( -3.834182069070819932, -7.532023737882814096, 26.00000000000000711 ) ) ;
#38697=ADVANCED_FACE ( 'NONE', ( #55676 ), #49678, .F. ) ;
#38700=ORIENTED_EDGE ( 'NONE', *, *, #61055, .F. ) ;
#38702=VERTEX_POINT ( 'NONE', #12867 ) ;
#38712=DIRECTION ( 'NONE',  ( -1.836970198721029934E-16, 1.836970198721036590E-16, -1.000000000000000000 ) ) ;
#38716=AXIS2_PLACEMENT_3D ( 'NONE', #55852, #61857, #28627 ) ;
#38719=DIRECTION ( 'NONE',  ( 1.836970198721029934E-16, 1.836970198721010706E-16, -1.000000000000000000 ) ) ;
#38725=VECTOR ( 'NONE', #39007, 1000.000000000000000 ) ;
#38729=VECTOR ( 'NONE', #29996, 1000.000000000000000 ) ;
#38732=ADVANCED_FACE ( 'NONE', ( #55005 ), #65927, .T. ) ;
#38743=DIRECTION ( 'NONE',  ( -0.6414496315691494699, -0.7671651518153064231, 0.000000000000000000 ) ) ;
#38747=ADVANCED_FACE ( 'NONE', ( #33422 ), #22807, .F. ) ;
#38749=ADVANCED_FACE ( 'NONE', ( #7921 ), #12528, .F. ) ;
#38754=ORIENTED_EDGE ( 'NONE', *, *, #46625, .F. ) ;
#38757=ORIENTED_EDGE ( 'NONE', *, *, #16939, .F. ) ;
#38779=VECTOR ( 'NONE', #49202, 1000.000000000000000 ) ;
#38785=DIRECTION ( 'NONE',  ( 0.7071067811865474617, 0.7071067811865474617, 2.597868168706479611E-16 ) ) ;
#38796=DIRECTION ( 'NONE',  ( -0.7071067811865500152, -0.7071067811865451302, 4.429638872090642462E-31 ) ) ;
#38798=DIRECTION ( 'NONE',  ( 0.6414496315691645689, 0.7671651518152940996, 2.309356642088551915E-17 ) ) ;
#38799=ORIENTED_EDGE ( 'NONE', *, *, #61365, .F. ) ;
#38804=CIRCLE ( 'NONE', #7196, 0.1750000000000002387 ) ;
#38808=DIRECTION ( 'NONE',  ( 0.7671651518153105309, -0.6414496315691445849, -0.000000000000000000 ) ) ;
#38817=DIRECTION ( 'NONE',  ( 0.000000000000000000, -1.000000000000000000, 0.000000000000000000 ) ) ;
#38820=ORIENTED_EDGE ( 'NONE', *, *, #10780, .F. ) ;
#38823=ORIENTED_EDGE ( 'NONE', *, *, #9207, .F. ) ;
#38825=FACE_OUTER_BOUND ( 'NONE', #33648, .T. ) ;
#38827=DIRECTION ( 'NONE',  ( 0.000000000000000000, 1.000000000000000000, 0.000000000000000000 ) ) ;
#38829=DIRECTION ( 'NONE',  ( 1.000000000000000000, -8.802523127157697409E-15, 1.836970198721013910E-16 ) ) ;
#38832=ORIENTED_EDGE ( 'NONE', *, *, #47581, .T. ) ;
#38836=DIRECTION ( 'NONE',  ( -0.000000000000000000, 3.673940397442059868E-16, -1.000000000000000000 ) ) ;
#38838=DIRECTION ( 'NONE',  ( 1.000000000000000000, -0.000000000000000000, 0.000000000000000000 ) ) ;
#38844=ORIENTED_EDGE ( 'NONE', *, *, #37525, .F. ) ;
#38846=CARTESIAN_POINT ( 'NONE',  ( -1.620245201994301665, 8.227189898828640935, 54.00000000000000711 ) ) ;
#38855=AXIS2_PLACEMENT_3D ( 'NONE', #55480, #34225, #65399 ) ;
#38860=VERTEX_POINT ( 'NONE', #25615 ) ;
#38864=DIRECTION ( 'NONE',  ( -0.000000000000000000, 3.673940397442059868E-16, -1.000000000000000000 ) ) ;
#38865=EDGE_CURVE ( 'NONE', #48716, #5287, #40459, .T. ) ;
#38872=FACE_OUTER_BOUND ( 'NONE', #29473, .T. ) ;
#38873=EDGE_CURVE ( 'NONE', #56170, #10380, #13408, .T. ) ;
#38876=CARTESIAN_POINT ( 'NONE',  ( 9.737023737882765317, 2.530476262117151709, 54.00000000000000711 ) ) ;
#38883=EDGE_CURVE ( 'NONE', #44762, #63705, #4408, .T. ) ;
#38887=LINE ( 'NONE', #60451, #36904 ) ;
#38893=LINE ( 'NONE', #32904, #56128 ) ;
#38897=DIRECTION ( 'NONE',  ( 1.836970198721029934E-16, 1.836970198721010706E-16, -1.000000000000000000 ) ) ;
#38899=ORIENTED_EDGE ( 'NONE', *, *, #55799, .F. ) ;
#38906=VECTOR ( 'NONE', #52815, 1000.000000000000000 ) ;
#38908=DIRECTION ( 'NONE',  ( -3.540251991789403884E-15, -1.000000000000000000, 0.000000000000000000 ) ) ;
#38914=ORIENTED_EDGE ( 'NONE', *, *, #63091, .T. ) ;
#38917=( NAMED_UNIT ( * ) SI_UNIT ( $, .STERADIAN. ) SOLID_ANGLE_UNIT ( ) );
#38920=EDGE_CURVE ( 'NONE', #10709, #961, #3268, .T. ) ;
#38922=VECTOR ( 'NONE', #14114, 1000.000000000000114 ) ;
#38923=VERTEX_POINT ( 'NONE', #10044 ) ;
#38925=ORIENTED_EDGE ( 'NONE', *, *, #35834, .T. ) ;
#38927=VECTOR ( 'NONE', #35018, 1000.000000000000000 ) ;
#38930=CARTESIAN_POINT ( 'NONE',  ( 9.404523737882758638, 1.466476262117154983, 54.00000000000000711 ) ) ;
#38935=ORIENTED_EDGE ( 'NONE', *, *, #11998, .T. ) ;
#38938=DIRECTION ( 'NONE',  ( -1.836970198721029934E-16, 1.836970198721036344E-16, -1.000000000000000000 ) ) ;
#38942=DIRECTION ( 'NONE',  ( -4.956352788505168198E-15, -1.000000000000000000, 0.000000000000000000 ) ) ;
#38947=ORIENTED_EDGE ( 'NONE', *, *, #45959, .T. ) ;
#38953=LINE ( 'NONE', #23389, #22932 ) ;
#38954=ORIENTED_EDGE ( 'NONE', *, *, #25563, .T. ) ;
#38958=CARTESIAN_POINT ( 'NONE',  ( 8.835729544836288696, 2.355476262117161657, 54.00000000000000711 ) ) ;
#38959=EDGE_CURVE ( 'NONE', #15483, #5750, #5788, .T. ) ;
#38960=DIRECTION ( 'NONE',  ( 0.000000000000000000, -1.000000000000000000, 0.000000000000000000 ) ) ;
#38964=DIRECTION ( 'NONE',  ( -0.7671651518153006499, 0.6414496315691565753, -0.000000000000000000 ) ) ;
#38967=EDGE_CURVE ( 'NONE', #24515, #23915, #479, .T. ) ;
#38969=ORIENTED_EDGE ( 'NONE', *, *, #2482, .T. ) ;
#38975=ORIENTED_EDGE ( 'NONE', *, *, #64844, .T. ) ;
#38976=DIRECTION ( 'NONE',  ( -1.000000000000000000, 0.000000000000000000, 0.000000000000000000 ) ) ;
#38985=EDGE_LOOP ( 'NONE', ( #39372, #27470, #38610, #68611 ) ) ;
#38986=DIRECTION ( 'NONE',  ( -0.000000000000000000, -0.000000000000000000, -1.000000000000000000 ) ) ;
#38996=LINE ( 'NONE', #38662, #17613 ) ;
#39007=DIRECTION ( 'NONE',  ( -0.000000000000000000, -0.000000000000000000, -1.000000000000000000 ) ) ;
#39016=ORIENTED_EDGE ( 'NONE', *, *, #64313, .T. ) ;
#39023=CARTESIAN_POINT ( 'NONE',  ( -5.242976262117259978, 5.242976262117182706, 54.00000000000000711 ) ) ;
#39027=DIRECTION ( 'NONE',  ( -1.836970198721029934E-16, 1.836970198721036590E-16, -1.000000000000000000 ) ) ;
#39032=LINE ( 'NONE', #60604, #64818 ) ;
#39034=EDGE_CURVE ( 'NONE', #9638, #42852, #5451, .T. ) ;
#39038=VERTEX_POINT ( 'NONE', #5086 ) ;
#39051=CARTESIAN_POINT ( 'NONE',  ( 3.677663764522603795, 6.350872789121277506, 26.00000000000000711 ) ) ;
#39052=VECTOR ( 'NONE', #26988, 1000.000000000000000 ) ;
#39056=ADVANCED_FACE ( 'NONE', ( #59865 ), #11419, .F. ) ;
#39061=VECTOR ( 'NONE', #56593, 1000.000000000000000 ) ;
#39062=DIRECTION ( 'NONE',  ( 1.000000000000000000, -1.047444401652940007E-14, 0.000000000000000000 ) ) ;
#39069=PLANE ( 'NONE',  #69309 ) ;
#39070=CARTESIAN_POINT ( 'NONE',  ( 7.532023737882817649, -6.665817930929295088, 26.00000000000000000 ) ) ;
#39078=DIRECTION ( 'NONE',  ( -0.000000000000000000, -0.000000000000000000, -1.000000000000000000 ) ) ;
#39084=CARTESIAN_POINT ( 'NONE',  ( -5.242976262117259978, 3.142976262117183062, 26.00000000000000711 ) ) ;
#39091=CARTESIAN_POINT ( 'NONE',  ( 8.241237374594243548, 1.620245201994235718, 26.00000000000000711 ) ) ;
#39099=DIRECTION ( 'NONE',  ( -1.000000000000000000, 0.000000000000000000, 0.000000000000000000 ) ) ;
#39105=DIRECTION ( 'NONE',  ( 0.000000000000000000, 0.000000000000000000, 1.000000000000000000 ) ) ;
#39114=EDGE_LOOP ( 'NONE', ( #5401, #13630, #8237, #30708, #42259, #24090, #23154, #18852, #27803, #64624, #13463, #35461, #65797, #67279, #55837, #4437, #32641 ) ) ;
#39116=CARTESIAN_POINT ( 'NONE',  ( 9.912023737882803331, 6.817976262117185549, 54.00000000000000711 ) ) ;
#39117=CARTESIAN_POINT ( 'NONE',  ( 8.930623737882843471, 9.689726262117160260, 26.00000000000000711 ) ) ;
#39120=ORIENTED_EDGE ( 'NONE', *, *, #23473, .F. ) ;
#39133=DIRECTION ( 'NONE',  ( -1.836970198721029934E-16, 1.836970198721036590E-16, -1.000000000000000000 ) ) ;
#39139=EDGE_CURVE ( 'NONE', #3338, #64676, #22726, .T. ) ;
#39142=PLANE ( 'NONE',  #26764 ) ;
#39145=EDGE_CURVE ( 'NONE', #24260, #902, #65854, .T. ) ;
#39146=CARTESIAN_POINT ( 'NONE',  ( 8.612468434717241550, -1.480523737882825985, 54.00000000000000711 ) ) ;
#39156=AXIS2_PLACEMENT_3D ( 'NONE', #4994, #41416, #63344 ) ;
#39162=CARTESIAN_POINT ( 'NONE',  ( -0.9414762621173295987, -9.929523737882849588, 54.00000000000000711 ) ) ;
#39163=ORIENTED_EDGE ( 'NONE', *, *, #49996, .T. ) ;
#39164=PLANE ( 'NONE',  #28997 ) ;
#39165=DIRECTION ( 'NONE',  ( -1.836970198721029934E-16, 1.836970198721036344E-16, -1.000000000000000000 ) ) ;
#39169=CIRCLE ( 'NONE', #19945, 0.1749999999999998224 ) ;
#39170=DIRECTION ( 'NONE',  ( 0.000000000000000000, -3.673940397442059868E-16, 1.000000000000000000 ) ) ;
#39175=DIRECTION ( 'NONE',  ( -5.013651664672856055E-16, 1.000000000000000000, 0.000000000000000000 ) ) ;
#39186=VECTOR ( 'NONE', #35681, 1000.000000000000000 ) ;
#39189=ADVANCED_FACE ( 'NONE', ( #40007 ), #22394, .T. ) ;
#39196=DIRECTION ( 'NONE',  ( 1.836970198721029934E-16, 1.836970198721010706E-16, -1.000000000000000000 ) ) ;
#39197=ORIENTED_EDGE ( 'NONE', *, *, #4985, .F. ) ;
#39203=DIRECTION ( 'NONE',  ( 0.000000000000000000, 1.000000000000000000, 0.000000000000000000 ) ) ;
#39210=ORIENTED_EDGE ( 'NONE', *, *, #11108, .T. ) ;
#39211=LINE ( 'NONE', #7018, #7126 ) ;
#39213=ORIENTED_EDGE ( 'NONE', *, *, #6317, .F. ) ;
#39215=DIRECTION ( 'NONE',  ( -8.359604446858500663E-15, -1.000000000000000000, 0.000000000000000000 ) ) ;
#39224=CARTESIAN_POINT ( 'NONE',  ( -9.689726262117313027, -8.930623737882751101, 26.00000000000000000 ) ) ;
#39231=DIRECTION ( 'NONE',  ( -1.000000000000000000, 0.000000000000000000, 0.000000000000000000 ) ) ;
#39245=CARTESIAN_POINT ( 'NONE',  ( 6.501044194225444883, 3.142976262117191943, 26.00000000000000711 ) ) ;
#39266=CIRCLE ( 'NONE', #24592, 1.929199999999998916 ) ;
#39281=PLANE ( 'NONE',  #211 ) ;
#39287=ADVANCED_FACE ( 'NONE', ( #57338 ), #35058, .F. ) ;
#39300=ADVANCED_FACE ( 'NONE', ( #2889 ), #52392, .F. ) ;
#39304=DIRECTION ( 'NONE',  ( 1.836970198721029934E-16, -1.836970198721036344E-16, 1.000000000000000000 ) ) ;
#39314=CARTESIAN_POINT ( 'NONE',  ( 9.912023737882815766, -6.657023737882814984, 26.00000000000000000 ) ) ;
#39317=VERTEX_POINT ( 'NONE', #24816 ) ;
#39322=ORIENTED_EDGE ( 'NONE', *, *, #52313, .T. ) ;
#39324=CARTESIAN_POINT ( 'NONE',  ( 3.848229544836330174, 7.517976262117205266, 54.00000000000000711 ) ) ;
#39328=CARTESIAN_POINT ( 'NONE',  ( 3.677663764522608680, 6.350872789121272177, 54.00000000000000711 ) ) ;
#39332=CARTESIAN_POINT ( 'NONE',  ( -5.538810540050064901, -7.357023737882800951, 54.00000000000000711 ) ) ;
#39334=FACE_OUTER_BOUND ( 'NONE', #26714, .T. ) ;
#39336=LINE ( 'NONE', #49604, #4313 ) ;
#39348=ORIENTED_EDGE ( 'NONE', *, *, #61803, .F. ) ;
#39349=EDGE_CURVE ( 'NONE', #42050, #11645, #4454, .T. ) ;
#39355=DIRECTION ( 'NONE',  ( 1.000000000000000000, -3.491481338843133355E-15, 0.000000000000000000 ) ) ;
#39368=ORIENTED_EDGE ( 'NONE', *, *, #67689, .T. ) ;
#39372=ORIENTED_EDGE ( 'NONE', *, *, #50087, .T. ) ;
#39378=VERTEX_POINT ( 'NONE', #21274 ) ;
#39391=CIRCLE ( 'NONE', #1103, 1.929199999999998916 ) ;
#39394=CARTESIAN_POINT ( 'NONE',  ( 2.369523737882817116, 9.547976262117204627, 54.00000000000000711 ) ) ;
#39405=CARTESIAN_POINT ( 'NONE',  ( 4.961189459950039904, -7.357023737882821379, 54.00000000000000711 ) ) ;
#39406=AXIS2_PLACEMENT_3D ( 'NONE', #26401, #47966, #26062 ) ;
#39409=DIRECTION ( 'NONE',  ( -1.836970198721029934E-16, 1.836970198721036590E-16, -1.000000000000000000 ) ) ;
#39410=ORIENTED_EDGE ( 'NONE', *, *, #32988, .F. ) ;
#39412=VECTOR ( 'NONE', #37872, 1000.000000000000000 ) ;
#39414=PLANE ( 'NONE',  #8832 ) ;
#39422=DIRECTION ( 'NONE',  ( 3.491481338843133355E-15, 1.000000000000000000, 1.836970198721029934E-16 ) ) ;
#39424=DIRECTION ( 'NONE',  ( -1.000000000000000000, 6.308085367188447236E-15, 0.000000000000000000 ) ) ;
#39442=VECTOR ( 'NONE', #60073, 1000.000000000000000 ) ;
#39446=ORIENTED_EDGE ( 'NONE', *, *, #54541, .T. ) ;
#39447=LINE ( 'NONE', #55047, #44247 ) ;
#39455=CIRCLE ( 'NONE', #21407, 1.929199999999998028 ) ;
#39457=CARTESIAN_POINT ( 'NONE',  ( -9.390476262117260831, 0.9414762621171833823, 54.00000000000000711 ) ) ;
#39461=AXIS2_PLACEMENT_3D ( 'NONE', #55311, #21477, #26439 ) ;
#39471=DIRECTION ( 'NONE',  ( 0.000000000000000000, 1.000000000000000000, 0.000000000000000000 ) ) ;
#39477=DIRECTION ( 'NONE',  ( 2.135044278125299371E-15, -1.000000000000000000, -3.673940397442060361E-16 ) ) ;
#39488=DIRECTION ( 'NONE',  ( 1.836970198721029934E-16, 1.836970198721010706E-16, -1.000000000000000000 ) ) ;
#39490=CARTESIAN_POINT ( 'NONE',  ( -6.775514141871427753, -7.408280051175141878, 54.00000000000000711 ) ) ;
#39500=VECTOR ( 'NONE', #11773, 1000.000000000000000 ) ;
#39506=VERTEX_POINT ( 'NONE', #37529 ) ;
#39514=DIRECTION ( 'NONE',  ( -1.836970198721029934E-16, 1.836970198721036590E-16, -1.000000000000000000 ) ) ;
#39520=CIRCLE ( 'NONE', #13539, 0.1749999999999989342 ) ;
#39526=VERTEX_POINT ( 'NONE', #6387 ) ;
#39527=EDGE_LOOP ( 'NONE', ( #61709, #66775, #12941, #11096 ) ) ;
#39529=VECTOR ( 'NONE', #63687, 1000.000000000000000 ) ;
#39533=LINE ( 'NONE', #29621, #27047 ) ;
#39541=ORIENTED_EDGE ( 'NONE', *, *, #35026, .T. ) ;
#39542=CARTESIAN_POINT ( 'NONE',  ( 8.093267424590459669, 8.697938382363064491, 54.00000000000000711 ) ) ;
#39547=LINE ( 'NONE', #18325, #10743 ) ;
#39556=LINE ( 'NONE', #7377, #26811 ) ;
#39557=DIRECTION ( 'NONE',  ( -0.4999999999999755196, 0.8660254037844526964, 2.509347957447861534E-16 ) ) ;
#39559=ADVANCED_FACE ( 'NONE', ( #22310 ), #33257, .F. ) ;
#39561=DIRECTION ( 'NONE',  ( -1.000000000000000000, 1.047444401652940007E-14, 0.000000000000000000 ) ) ;
#39562=LINE ( 'NONE', #49840, #7932 ) ;
#39568=ORIENTED_EDGE ( 'NONE', *, *, #40530, .T. ) ;
#39571=CARTESIAN_POINT ( 'NONE',  ( 3.677663764522614454, -4.149127210878761574, 26.00000000000000711 ) ) ;
#39575=CARTESIAN_POINT ( 'NONE',  ( -9.689726262117227762, 8.916576262117214213, 26.00000000000000711 ) ) ;
#39582=PLANE ( 'NONE',  #11905 ) ;
#39587=LINE ( 'NONE', #61150, #40874 ) ;
#39589=ORIENTED_EDGE ( 'NONE', *, *, #22219, .T. ) ;
#39591=FACE_OUTER_BOUND ( 'NONE', #54900, .T. ) ;
#39597=FACE_BOUND ( 'NONE', #61871, .T. ) ;
#39598=CARTESIAN_POINT ( 'NONE',  ( 1.480523737882794233, -8.612468434717218457, 54.00000000000000711 ) ) ;
#39604=LINE ( 'NONE', #34292, #69901 ) ;
#39607=ORIENTED_EDGE ( 'NONE', *, *, #25208, .F. ) ;
#39609=VECTOR ( 'NONE', #38808, 1000.000000000000114 ) ;
#39629=VERTEX_POINT ( 'NONE', #28287 ) ;
#39631=CARTESIAN_POINT ( 'NONE',  ( -8.566576262117346019, -8.930623737882765312, 26.00000000000000000 ) ) ;
#39632=FACE_OUTER_BOUND ( 'NONE', #50993, .T. ) ;
#39637=ORIENTED_EDGE ( 'NONE', *, *, #28478, .F. ) ;
#39656=LINE ( 'NONE', #65515, #27677 ) ;
#39663=CARTESIAN_POINT ( 'NONE',  ( 6.364920264886885448, -6.836383711243021466, 54.00000000000000711 ) ) ;
#39666=FACE_OUTER_BOUND ( 'NONE', #45383, .T. ) ;
#39668=DIRECTION ( 'NONE',  ( -1.000000000000000000, 0.000000000000000000, 0.000000000000000000 ) ) ;
#39673=EDGE_CURVE ( 'NONE', #52904, #14583, #1110, .T. ) ;
#39677=ORIENTED_EDGE ( 'NONE', *, *, #34234, .F. ) ;
#39681=DIRECTION ( 'NONE',  ( -0.8660254037844363761, 0.5000000000000038858, 0.000000000000000000 ) ) ;
#39691=VERTEX_POINT ( 'NONE', #18355 ) ;
#39695=ORIENTED_EDGE ( 'NONE', *, *, #30977, .F. ) ;
#39702=DIRECTION ( 'NONE',  ( 0.000000000000000000, 0.000000000000000000, 1.000000000000000000 ) ) ;
#39711=CARTESIAN_POINT ( 'NONE',  ( -9.547976262117304103, -8.144523737882758851, 54.00000000000000711 ) ) ;
#39714=ORIENTED_EDGE ( 'NONE', *, *, #52923, .T. ) ;
#39721=DIRECTION ( 'NONE',  ( 0.000000000000000000, 1.000000000000000000, 0.000000000000000000 ) ) ;
#39724=AXIS2_PLACEMENT_3D ( 'NONE', #60731, #49782, #11254 ) ;
#39747=DIRECTION ( 'NONE',  ( 0.6414496315691420314, -0.7671651518153128624, 0.000000000000000000 ) ) ;
#39748=DIRECTION ( 'NONE',  ( -0.7671651518153131954, -0.6414496315691415873, 0.000000000000000000 ) ) ;
#39752=DIRECTION ( 'NONE',  ( -0.000000000000000000, -0.000000000000000000, -1.000000000000000000 ) ) ;
#39755=FACE_OUTER_BOUND ( 'NONE', #30444, .T. ) ;
#39760=DIRECTION ( 'NONE',  ( 0.000000000000000000, -3.673940397442059868E-16, 1.000000000000000000 ) ) ;
#39764=CARTESIAN_POINT ( 'NONE',  ( 10.31452373788280497, 6.642976262117183062, 54.00000000000000711 ) ) ;
#39772=VECTOR ( 'NONE', #36306, 1000.000000000000000 ) ;
#39775=LINE ( 'NONE', #60998, #37356 ) ;
#39778=ORIENTED_EDGE ( 'NONE', *, *, #52302, .T. ) ;
#39779=DIRECTION ( 'NONE',  ( 0.000000000000000000, 3.673940397442059868E-16, -1.000000000000000000 ) ) ;
#39781=ADVANCED_FACE ( 'NONE', ( #46996 ), #32132, .F. ) ;
#39782=DIRECTION ( 'NONE',  ( -1.836970198721029934E-16, 1.836970198721036590E-16, -1.000000000000000000 ) ) ;
#39787=LINE ( 'NONE', #57728, #15405 ) ;
#39789=ORIENTED_EDGE ( 'NONE', *, *, #17746, .T. ) ;
#39796=ORIENTED_EDGE ( 'NONE', *, *, #19955, .T. ) ;
#39806=CARTESIAN_POINT ( 'NONE',  ( 6.832023737882818359, -9.912023737882819319, 54.00000000000000711 ) ) ;
#39816=ADVANCED_FACE ( 'NONE', ( #4574 ), #64650, .F. ) ;
#39819=EDGE_CURVE ( 'NONE', #38923, #21386, #64316, .T. ) ;
#39823=EDGE_CURVE ( 'NONE', #17091, #28438, #10912, .T. ) ;
#39824=CARTESIAN_POINT ( 'NONE',  ( -9.689726262117227762, 9.689726262117183353, 54.00000000000000711 ) ) ;
#39826=ORIENTED_EDGE ( 'NONE', *, *, #32434, .F. ) ;
#39828=VECTOR ( 'NONE', #6003, 1000.000000000000000 ) ;
#39834=CARTESIAN_POINT ( 'NONE',  ( 5.257023737882801306, 5.242976262117200470, 54.00000000000000711 ) ) ;
#39839=CARTESIAN_POINT ( 'NONE',  ( -10.30047626211725742, 3.842976262117182351, 54.00000000000000711 ) ) ;
#39853=VECTOR ( 'NONE', #3424, 1000.000000000000000 ) ;
#39855=ORIENTED_EDGE ( 'NONE', *, *, #19126, .F. ) ;
#39860=CARTESIAN_POINT ( 'NONE',  ( -10.50612335864049740, 6.822329165593917111, 26.00000000000000711 ) ) ;
#39869=EDGE_LOOP ( 'NONE', ( #58026, #7019, #64365, #7371 ) ) ;
#39889=CARTESIAN_POINT ( 'NONE',  ( 3.157023737882792780, 4.031976262117212606, 26.00000000000000711 ) ) ;
#39900=ORIENTED_EDGE ( 'NONE', *, *, #56094, .F. ) ;
#39903=VECTOR ( 'NONE', #54526, 1000.000000000000000 ) ;
#39908=EDGE_CURVE ( 'NONE', #29534, #36809, #9018, .T. ) ;
#39909=CARTESIAN_POINT ( 'NONE',  ( 8.144523737882812142, 8.821682069070710952, 54.00000000000000711 ) ) ;
#39911=CARTESIAN_POINT ( 'NONE',  ( 3.003254798005743353, 6.858227778582815404, 54.00000000000000711 ) ) ;
#39921=CARTESIAN_POINT ( 'NONE',  ( -3.667976262117325081, -9.912023737882812213, 26.00000000000000000 ) ) ;
#39924=DIRECTION ( 'NONE',  ( -0.7071067811865421326, 0.7071067811865530128, 0.000000000000000000 ) ) ;
#39927=DIRECTION ( 'NONE',  ( 1.000000000000000000, -1.671920889371702854E-15, 0.000000000000000000 ) ) ;
#39928=ORIENTED_EDGE ( 'NONE', *, *, #35355, .F. ) ;
#39930=DIRECTION ( 'NONE',  ( 0.000000000000000000, -1.000000000000000000, 0.000000000000000000 ) ) ;
#39945=DIRECTION ( 'NONE',  ( -1.000000000000000000, 0.000000000000000000, 0.000000000000000000 ) ) ;
#39949=ADVANCED_FACE ( 'NONE', ( #49444 ), #66385, .F. ) ;
#39950=VECTOR ( 'NONE', #3858, 999.9999999999998863 ) ;
#39956=ORIENTED_EDGE ( 'NONE', *, *, #65925, .F. ) ;
#39958=ORIENTED_EDGE ( 'NONE', *, *, #53136, .F. ) ;
#39969=ORIENTED_EDGE ( 'NONE', *, *, #6246, .F. ) ;
#39970=EDGE_LOOP ( 'NONE', ( #4017, #61808, #69206, #50684 ) ) ;
#39982=CARTESIAN_POINT ( 'NONE',  ( 0.9555237378827827754, -9.929523737882782086, 26.00000000000000000 ) ) ;
#39983=VERTEX_POINT ( 'NONE', #6971 ) ;
#39995=CARTESIAN_POINT ( 'NONE',  ( 6.832023737882815695, 9.722976262117192903, 54.00000000000000711 ) ) ;
#39998=LINE ( 'NONE', #61568, #35139 ) ;
#40007=FACE_OUTER_BOUND ( 'NONE', #14989, .T. ) ;
#40018=VERTEX_POINT ( 'NONE', #1338 ) ;
#40021=CARTESIAN_POINT ( 'NONE',  ( 10.31452373788278187, 3.650476262117146042, 54.00000000000000711 ) ) ;
#40034=VERTEX_POINT ( 'NONE', #23937 ) ;
#40035=ORIENTED_EDGE ( 'NONE', *, *, #52848, .F. ) ;
#40037=EDGE_LOOP ( 'NONE', ( #32482, #41632, #11707, #61759 ) ) ;
#40043=CYLINDRICAL_SURFACE ( 'NONE', #58350, 0.1749999999999989342 ) ;
#40065=DIRECTION ( 'NONE',  ( -1.836970198721029934E-16, 1.836970198721036590E-16, -1.000000000000000000 ) ) ;
#40074=VERTEX_POINT ( 'NONE', #68125 ) ;
#40080=ORIENTED_EDGE ( 'NONE', *, *, #43762, .F. ) ;
#40085=DIRECTION ( 'NONE',  ( -0.000000000000000000, -0.000000000000000000, -1.000000000000000000 ) ) ;
#40086=AXIS2_PLACEMENT_3D ( 'NONE', #32838, #59711, #42057 ) ;
#40094=DIRECTION ( 'NONE',  ( -1.000000000000000000, 1.221996412923863950E-14, 1.836970198721052367E-16 ) ) ;
#40099=VECTOR ( 'NONE', #41292, 1000.000000000000114 ) ;
#40102=CARTESIAN_POINT ( 'NONE',  ( -9.689726262117314803, -8.580623737882756785, 54.00000000000000711 ) ) ;
#40111=DIRECTION ( 'NONE',  ( 1.000000000000000000, 0.000000000000000000, 0.000000000000000000 ) ) ;
#40113=DIRECTION ( 'NONE',  ( -0.000000000000000000, -0.000000000000000000, -1.000000000000000000 ) ) ;
#40157=ORIENTED_EDGE ( 'NONE', *, *, #67241, .T. ) ;
#40159=ADVANCED_FACE ( 'NONE', ( #64236 ), #41606, .F. ) ;
#40163=LINE ( 'NONE', #28511, #33869 ) ;
#40164=FACE_OUTER_BOUND ( 'NONE', #46169, .T. ) ;
#40187=VECTOR ( 'NONE', #48681, 1000.000000000000000 ) ;
#40195=DIRECTION ( 'NONE',  ( 0.000000000000000000, -0.000000000000000000, -1.000000000000000000 ) ) ;
#40196=VECTOR ( 'NONE', #36305, 1000.000000000000114 ) ;
#40201=DIRECTION ( 'NONE',  ( -0.6414496315691494699, 0.7671651518153064231, 2.818519042764025305E-16 ) ) ;
#40202=VECTOR ( 'NONE', #37575, 1000.000000000000000 ) ;
#40204=CARTESIAN_POINT ( 'NONE',  ( -8.821682069070780230, 2.355476262117184305, 54.00000000000000711 ) ) ;
#40213=CARTESIAN_POINT ( 'NONE',  ( 7.357023737882817827, -5.552858015815587578, 54.00000000000000711 ) ) ;
#40220=PLANE ( 'NONE',  #6288 ) ;
#40226=DIRECTION ( 'NONE',  ( 0.000000000000000000, 3.673940397442059868E-16, -1.000000000000000000 ) ) ;
#40228=VERTEX_POINT ( 'NONE', #26745 ) ;
#40232=VERTEX_POINT ( 'NONE', #52577 ) ;
#40237=CYLINDRICAL_SURFACE ( 'NONE', #42295, 1.929199999999997139 ) ;
#40239=ORIENTED_EDGE ( 'NONE', *, *, #61790, .F. ) ;
#40260=ORIENTED_EDGE ( 'NONE', *, *, #12936, .T. ) ;
#40263=CARTESIAN_POINT ( 'NONE',  ( -8.598420958951630055, -1.480523737882741164, 26.00000000000000711 ) ) ;
#40266=PLANE ( 'NONE',  #13244 ) ;
#40267=CARTESIAN_POINT ( 'NONE',  ( -9.547976262117227719, -2.544523737882729453, 54.00000000000000711 ) ) ;
#40268=AXIS2_PLACEMENT_3D ( 'NONE', #40267, #40617, #62522 ) ;
#40269=DIRECTION ( 'NONE',  ( -0.000000000000000000, -0.000000000000000000, -1.000000000000000000 ) ) ;
#40277=EDGE_CURVE ( 'NONE', #45115, #66583, #15442, .T. ) ;
#40282=DIRECTION ( 'NONE',  ( 0.7071067811865486830, 0.7071067811865464625, 0.000000000000000000 ) ) ;
#40284=LINE ( 'NONE', #61856, #55379 ) ;
#40287=LINE ( 'NONE', #39245, #5306 ) ;
#40290=LINE ( 'NONE', #8102, #46920 ) ;
#40294=CARTESIAN_POINT ( 'NONE',  ( 8.930623737882818602, -8.580623737882856261, 54.00000000000000711 ) ) ;
#40302=AXIS2_PLACEMENT_3D ( 'NONE', #60029, #48043, #43081 ) ;
#40307=CIRCLE ( 'NONE', #4198, 1.224999999999999423 ) ;
#40312=ORIENTED_EDGE ( 'NONE', *, *, #42659, .T. ) ;
#40315=VECTOR ( 'NONE', #52127, 1000.000000000000000 ) ;
#40318=ADVANCED_FACE ( 'NONE', ( #33771 ), #44030, .F. ) ;
#40324=EDGE_CURVE ( 'NONE', #1387, #15802, #50029, .T. ) ;
#40326=EDGE_CURVE ( 'NONE', #57897, #5949, #22819, .T. ) ;
#40331=CARTESIAN_POINT ( 'NONE',  ( -10.30047626211725031, -3.857023737882713466, 54.00000000000000711 ) ) ;
#40333=EDGE_CURVE ( 'NONE', #60944, #19926, #53974, .T. ) ;
#40336=DIRECTION ( 'NONE',  ( -1.000000000000000000, -3.016910393003147986E-15, -0.000000000000000000 ) ) ;
#40350=ORIENTED_EDGE ( 'NONE', *, *, #32508, .F. ) ;
#40351=ORIENTED_EDGE ( 'NONE', *, *, #33427, .T. ) ;
#40355=DIRECTION ( 'NONE',  ( 0.000000000000000000, 1.000000000000000000, 0.000000000000000000 ) ) ;
#40356=ORIENTED_EDGE ( 'NONE', *, *, #4935, .F. ) ;
#40361=DIRECTION ( 'NONE',  ( -1.000000000000000000, 0.000000000000000000, 0.000000000000000000 ) ) ;
#40362=DIRECTION ( 'NONE',  ( -0.5000000000000049960, -0.8660254037844358210, -6.723777587268367771E-17 ) ) ;
#40370=LINE ( 'NONE', #17402, #1854 ) ;
#40371=VECTOR ( 'NONE', #51557, 1000.000000000000114 ) ;
#40373=CARTESIAN_POINT ( 'NONE',  ( -6.817976262117261044, 9.897976262117179402, 54.00000000000000711 ) ) ;
#40374=DIRECTION ( 'NONE',  ( 0.6414496315691539108, -0.7671651518153028704, -2.587583378555131256E-16 ) ) ;
#40379=CARTESIAN_POINT ( 'NONE',  ( -6.651770455163781293, -7.357023737882790293, 54.00000000000000711 ) ) ;
#40385=CARTESIAN_POINT ( 'NONE',  ( 8.835729544836290472, 2.530476262117160591, 54.00000000000000711 ) ) ;
#40386=DIRECTION ( 'NONE',  ( -1.000000000000000000, 0.000000000000000000, 0.000000000000000000 ) ) ;
#40391=DIRECTION ( 'NONE',  ( 0.5000000000000038858, 0.8660254037844363761, 3.181725716174712116E-16 ) ) ;
#40394=EDGE_LOOP ( 'NONE', ( #24251, #60496, #30487, #16093 ) ) ;
#40399=CARTESIAN_POINT ( 'NONE',  ( -9.689726262117227762, 8.566576262117216345, 54.00000000000000711 ) ) ;
#40418=EDGE_CURVE ( 'NONE', #13431, #65287, #221, .T. ) ;
#40424=ORIENTED_EDGE ( 'NONE', *, *, #49261, .T. ) ;
#40432=VECTOR ( 'NONE', #30562, 1000.000000000000000 ) ;
#40433=DIRECTION ( 'NONE',  ( -0.000000000000000000, 3.673940397442059868E-16, -1.000000000000000000 ) ) ;
#40437=CARTESIAN_POINT ( 'NONE',  ( -8.697938382363185283, -8.093267424590415260, 54.00000000000000711 ) ) ;
#40448=LINE ( 'NONE', #12515, #48786 ) ;
#40454=DIRECTION ( 'NONE',  ( -1.000000000000000000, 0.000000000000000000, 0.000000000000000000 ) ) ;
#40456=EDGE_CURVE ( 'NONE', #17044, #19926, #41783, .T. ) ;
#40459=LINE ( 'NONE', #35141, #7747 ) ;
#40463=CARTESIAN_POINT ( 'NONE',  ( -8.916576262117356322, -10.05377373788272877, 26.00000000000000000 ) ) ;
#40466=CARTESIAN_POINT ( 'NONE',  ( -9.897976262117257562, 3.667976262117184749, 26.00000000000000711 ) ) ;
#40469=ADVANCED_FACE ( 'NONE', ( #68673 ), #23511, .F. ) ;
#40472=ORIENTED_EDGE ( 'NONE', *, *, #4067, .F. ) ;
#40490=LINE ( 'NONE', #55377, #42483 ) ;
#40498=ORIENTED_EDGE ( 'NONE', *, *, #7594, .F. ) ;
#40500=DIRECTION ( 'NONE',  ( 1.000000000000000000, -1.671920889371702854E-15, 0.000000000000000000 ) ) ;
#40502=PLANE ( 'NONE',  #54624 ) ;
#40507=ORIENTED_EDGE ( 'NONE', *, *, #53281, .T. ) ;
#40512=ORIENTED_EDGE ( 'NONE', *, *, #38427, .F. ) ;
#40530=EDGE_CURVE ( 'NONE', #59528, #23856, #31197, .T. ) ;
#40539=DIRECTION ( 'NONE',  ( 1.047444401652940007E-14, 1.000000000000000000, 1.836970198721029934E-16 ) ) ;
#40545=FACE_OUTER_BOUND ( 'NONE', #4642, .T. ) ;
#40548=CARTESIAN_POINT ( 'NONE',  ( -10.49297626211726175, 3.650476262117184234, 54.00000000000000711 ) ) ;
#40550=EDGE_CURVE ( 'NONE', #51881, #40074, #11346, .T. ) ;
#40553=AXIS2_PLACEMENT_3D ( 'NONE', #36201, #9338, #42906 ) ;
#40555=ORIENTED_EDGE ( 'NONE', *, *, #61710, .T. ) ;
#40558=ADVANCED_FACE ( 'NONE', ( #20917 ), #31543, .T. ) ;
#40560=CARTESIAN_POINT ( 'NONE',  ( -6.822336235477489019, -6.364920264886856138, 26.00000000000000711 ) ) ;
#40562=EDGE_CURVE ( 'NONE', #18663, #23009, #42132, .T. ) ;
#40563=FACE_OUTER_BOUND ( 'NONE', #63945, .T. ) ;
#40568=ORIENTED_EDGE ( 'NONE', *, *, #48780, .F. ) ;
#40571=DIRECTION ( 'NONE',  ( -0.000000000000000000, 3.673940397442059868E-16, -1.000000000000000000 ) ) ;
#40572=EDGE_LOOP ( 'NONE', ( #12039, #38899, #26103, #45688 ) ) ;
#40577=DIRECTION ( 'NONE',  ( 1.836970198721029934E-16, 1.836970198721010706E-16, -1.000000000000000000 ) ) ;
#40579=VECTOR ( 'NONE', #65924, 1000.000000000000000 ) ;
#40589=LINE ( 'NONE', #2410, #18034 ) ;
#40608=ORIENTED_EDGE ( 'NONE', *, *, #58669, .F. ) ;
#40610=AXIS2_PLACEMENT_3D ( 'NONE', #45231, #56550, #51243 ) ;
#40614=VECTOR ( 'NONE', #45965, 1000.000000000000000 ) ;
#40617=DIRECTION ( 'NONE',  ( 1.836970198721029934E-16, 1.836970198721010706E-16, -1.000000000000000000 ) ) ;
#40625=ORIENTED_EDGE ( 'NONE', *, *, #4743, .T. ) ;
#40627=VERTEX_POINT ( 'NONE', #63 ) ;
#40629=DIRECTION ( 'NONE',  ( -1.000000000000000000, 1.130039751537442024E-14, 0.000000000000000000 ) ) ;
#40640=DIRECTION ( 'NONE',  ( -1.836970198721029934E-16, 1.836970198721036590E-16, -1.000000000000000000 ) ) ;
#40642=CARTESIAN_POINT ( 'NONE',  ( 2.005523737882793256, -8.612468434717222010, 54.00000000000000711 ) ) ;
#40646=ORIENTED_EDGE ( 'NONE', *, *, #15487, .F. ) ;
#40647=CARTESIAN_POINT ( 'NONE',  ( 1.480523737882811330, 9.390476262117216422, 26.00000000000000711 ) ) ;
#40649=ORIENTED_EDGE ( 'NONE', *, *, #65786, .T. ) ;
#40656=VECTOR ( 'NONE', #52257, 1000.000000000000000 ) ;
#40660=DIRECTION ( 'NONE',  ( 1.000000000000000000, 0.000000000000000000, -0.000000000000000000 ) ) ;
#40664=CARTESIAN_POINT ( 'NONE',  ( -8.130476262117259267, 8.821682069070703847, 54.00000000000000711 ) ) ;
#40674=CIRCLE ( 'NONE', #24727, 0.1749999999999998224 ) ;
#40676=EDGE_CURVE ( 'NONE', #22000, #13327, #45239, .T. ) ;
#40683=VECTOR ( 'NONE', #56286, 1000.000000000000000 ) ;
#40688=FACE_OUTER_BOUND ( 'NONE', #64935, .T. ) ;
#40710=CARTESIAN_POINT ( 'NONE',  ( -9.781776262117247711, 9.781776262117171328, 54.00000000000000711 ) ) ;
#40713=VECTOR ( 'NONE', #27083, 1000.000000000000000 ) ;
#40726=VERTEX_POINT ( 'NONE', #33942 ) ;
#40740=VERTEX_POINT ( 'NONE', #7069 ) ;
#40745=DIRECTION ( 'NONE',  ( 7.304098846218132892E-15, 1.000000000000000000, 3.673940397442059868E-16 ) ) ;
#40746=VERTEX_POINT ( 'NONE', #22327 ) ;
#40748=CARTESIAN_POINT ( 'NONE',  ( 1.480523737882816881, 9.390476262117212869, 54.00000000000000711 ) ) ;
#40751=LINE ( 'NONE', #51721, #67064 ) ;
#40753=ORIENTED_EDGE ( 'NONE', *, *, #11302, .T. ) ;
#40755=AXIS2_PLACEMENT_3D ( 'NONE', #32116, #33417, #65922 ) ;
#40756=DIRECTION ( 'NONE',  ( -1.000000000000000000, 0.000000000000000000, 0.000000000000000000 ) ) ;
#40764=CARTESIAN_POINT ( 'NONE',  ( -9.722976262117258628, 6.817976262117182884, 54.00000000000000711 ) ) ;
#40766=ADVANCED_FACE ( 'NONE', ( #39591 ), #43872, .F. ) ;
#40768=EDGE_CURVE ( 'NONE', #42852, #45427, #2125, .T. ) ;
#40773=EDGE_CURVE ( 'NONE', #56509, #42896, #17007, .T. ) ;
#40781=CYLINDRICAL_SURFACE ( 'NONE', #35361, 0.5250000000000001332 ) ;
#40782=AXIS2_PLACEMENT_3D ( 'NONE', #29310, #13754, #56884 ) ;
#40785=ORIENTED_EDGE ( 'NONE', *, *, #11468, .F. ) ;
#40788=VERTEX_POINT ( 'NONE', #8111 ) ;
#40790=DIRECTION ( 'NONE',  ( 1.000000000000000000, -7.304098846218132892E-15, 0.000000000000000000 ) ) ;
#40799=DIRECTION ( 'NONE',  ( 2.135044278125299371E-15, 1.000000000000000000, 0.000000000000000000 ) ) ;
#40806=DIRECTION ( 'NONE',  ( -1.000000000000000000, 0.000000000000000000, 0.000000000000000000 ) ) ;
#40807=EDGE_CURVE ( 'NONE', #59980, #63544, #56564, .T. ) ;
#40809=ORIENTED_EDGE ( 'NONE', *, *, #12375, .T. ) ;
#40811=LINE ( 'NONE', #9339, #50160 ) ;
#40817=DIRECTION ( 'NONE',  ( 0.000000000000000000, -1.000000000000000000, -3.673940397442059868E-16 ) ) ;
#40818=LINE ( 'NONE', #30218, #52880 ) ;
#40825=VERTEX_POINT ( 'NONE', #24392 ) ;
#40826=CARTESIAN_POINT ( 'NONE',  ( 8.930623737882843471, 10.03972626211716168, 26.00000000000000711 ) ) ;
#40831=EDGE_LOOP ( 'NONE', ( #20856, #69102, #30434, #10160 ) ) ;
#40832=DIRECTION ( 'NONE',  ( 0.5000000000000129896, 0.8660254037844311581, 0.000000000000000000 ) ) ;
#40833=CARTESIAN_POINT ( 'NONE',  ( 7.357023737882802727, 5.538810540049955655, 54.00000000000000711 ) ) ;
#40846=ORIENTED_EDGE ( 'NONE', *, *, #229, .F. ) ;
#40856=ORIENTED_EDGE ( 'NONE', *, *, #45202, .T. ) ;
#40861=ORIENTED_EDGE ( 'NONE', *, *, #12908, .T. ) ;
#40864=ORIENTED_EDGE ( 'NONE', *, *, #568, .T. ) ;
#40874=VECTOR ( 'NONE', #39927, 1000.000000000000000 ) ;
#40878=EDGE_CURVE ( 'NONE', #32932, #30081, #62552, .T. ) ;
#40886=LINE ( 'NONE', #14728, #46855 ) ;
#40888=CARTESIAN_POINT ( 'NONE',  ( -3.142976262117292752, -6.501044194225499062, 54.00000000000000711 ) ) ;
#40893=CARTESIAN_POINT ( 'NONE',  ( -6.835476262117330393, -10.50702373788278265, 26.00000000000000000 ) ) ;
#40896=DIRECTION ( 'NONE',  ( 9.912705577010386883E-15, 1.000000000000000000, 0.000000000000000000 ) ) ;
#40901=DIRECTION ( 'NONE',  ( 1.836970198721029934E-16, 1.836970198721010706E-16, -1.000000000000000000 ) ) ;
#40902=VECTOR ( 'NONE', #42864, 1000.000000000000000 ) ;
#40909=VECTOR ( 'NONE', #65560, 1000.000000000000114 ) ;
#40912=LINE ( 'NONE', #42669, #56775 ) ;
#40928=EDGE_LOOP ( 'NONE', ( #54294, #40864, #40507, #11042 ) ) ;
#40929=FACE_OUTER_BOUND ( 'NONE', #25815, .T. ) ;
#40938=LINE ( 'NONE', #31412, #4516 ) ;
#40941=ORIENTED_EDGE ( 'NONE', *, *, #9495, .T. ) ;
#40946=PRODUCT_CONTEXT ( 'NONE', #30935, 'mechanical' ) ;
#40948=CARTESIAN_POINT ( 'NONE',  ( 8.144523737882815695, 9.547976262117185087, 54.00000000000000711 ) ) ;
#40960=CARTESIAN_POINT ( 'NONE',  ( -7.955476262117320729, -9.562023737882766383, 26.00000000000000000 ) ) ;
#40961=DIRECTION ( 'NONE',  ( 1.836970198721029934E-16, -1.836970198721036344E-16, 1.000000000000000000 ) ) ;
#40963=ORIENTED_EDGE ( 'NONE', *, *, #23273, .T. ) ;
#40967=LINE ( 'NONE', #66788, #56263 ) ;
#40968=CARTESIAN_POINT ( 'NONE',  ( 3.857023737882817827, 10.30047626211720413, 54.00000000000000711 ) ) ;
#40970=DIRECTION ( 'NONE',  ( 0.000000000000000000, -3.673940397442059868E-16, 1.000000000000000000 ) ) ;
#40972=VECTOR ( 'NONE', #40113, 1000.000000000000000 ) ;
#40974=LINE ( 'NONE', #19409, #14930 ) ;
#40976=CARTESIAN_POINT ( 'NONE',  ( 10.31452373788278187, 3.842976262117144159, 54.00000000000000711 ) ) ;
#40982=CARTESIAN_POINT ( 'NONE',  ( -9.897976262117250457, -3.857023737882721903, 54.00000000000000711 ) ) ;
#40991=CARTESIAN_POINT ( 'NONE',  ( -3.663616288757055806, 4.135079735113128763, 26.00000000000000711 ) ) ;
#41000=VERTEX_POINT ( 'NONE', #37800 ) ;
#41005=VECTOR ( 'NONE', #16628, 1000.000000000000000 ) ;
#41006=CARTESIAN_POINT ( 'NONE',  ( -6.835476262117334834, -10.50702373788278798, 54.00000000000000711 ) ) ;
#41008=CARTESIAN_POINT ( 'NONE',  ( -3.142976262117292308, -6.501044194225499062, 54.00000000000000711 ) ) ;
#41009=LINE ( 'NONE', #30414, #29849 ) ;
#41013=VERTEX_POINT ( 'NONE', #316 ) ;
#41014=EDGE_CURVE ( 'NONE', #46952, #16502, #3524, .T. ) ;
#41032=ORIENTED_EDGE ( 'NONE', *, *, #29508, .F. ) ;
#41036=CIRCLE ( 'NONE', #30850, 0.5249999999999994671 ) ;
#41041=ORIENTED_EDGE ( 'NONE', *, *, #10796, .T. ) ;
#41046=EDGE_LOOP ( 'NONE', ( #37405, #31943, #37271, #69413 ) ) ;
#41047=ADVANCED_FACE ( 'NONE', ( #26851 ), #69974, .T. ) ;
#41056=DIRECTION ( 'NONE',  ( 1.000000000000000000, 2.135044278125301343E-15, 0.000000000000000000 ) ) ;
#41061=CARTESIAN_POINT ( 'NONE',  ( -8.916576262117260399, 8.566576262117216345, 54.00000000000000711 ) ) ;
#41077=DIRECTION ( 'NONE',  ( 0.000000000000000000, 1.000000000000000000, 3.673940397442059868E-16 ) ) ;
#41097=ORIENTED_EDGE ( 'NONE', *, *, #34868, .F. ) ;
#41109=CARTESIAN_POINT ( 'NONE',  ( 3.157023737882809655, -6.501044194225470640, 26.00000000000000711 ) ) ;
#41110=ADVANCED_FACE ( 'NONE', ( #17942 ), #16922, .F. ) ;
#41111=EDGE_LOOP ( 'NONE', ( #16613, #33136, #26689, #15010 ) ) ;
#41116=ORIENTED_EDGE ( 'NONE', *, *, #37663, .F. ) ;
#41117=LINE ( 'NONE', #7182, #61507 ) ;
#41119=EDGE_CURVE ( 'NONE', #54442, #10200, #51928, .T. ) ;
#41124=DIRECTION ( 'NONE',  ( 0.000000000000000000, 0.000000000000000000, 1.000000000000000000 ) ) ;
#41128=DIRECTION ( 'NONE',  ( 1.000000000000000000, -8.359604446858500663E-15, 0.000000000000000000 ) ) ;
#41144=ORIENTED_EDGE ( 'NONE', *, *, #49073, .F. ) ;
#41146=ORIENTED_EDGE ( 'NONE', *, *, #26376, .T. ) ;
#41147=CARTESIAN_POINT ( 'NONE',  ( -9.689726262117318356, -8.930623737882756430, 54.00000000000000711 ) ) ;
#41152=CARTESIAN_POINT ( 'NONE',  ( 2.632023737882801306, 6.486996718459885791, 26.00000000000000711 ) ) ;
#41161=DIRECTION ( 'NONE',  ( 1.047444401652940007E-14, 1.000000000000000000, 1.836970198721029934E-16 ) ) ;
#41164=FACE_OUTER_BOUND ( 'NONE', #44629, .T. ) ;
#41167=VECTOR ( 'NONE', #69761, 1000.000000000000000 ) ;
#41174=CARTESIAN_POINT ( 'NONE',  ( 5.552858015815581361, -7.357023737882814274, 26.00000000000000000 ) ) ;
#41175=VECTOR ( 'NONE', #48079, 1000.000000000000000 ) ;
#41176=ORIENTED_EDGE ( 'NONE', *, *, #11672, .F. ) ;
#41177=PLANE ( 'NONE',  #35501 ) ;
#41182=CARTESIAN_POINT ( 'NONE',  ( -9.722976262117258628, 6.817976262117182884, 54.00000000000000711 ) ) ;
#41183=ORIENTED_EDGE ( 'NONE', *, *, #21588, .F. ) ;
#41196=EDGE_LOOP ( 'NONE', ( #47839, #60408, #15495, #49195 ) ) ;
#41200=EDGE_CURVE ( 'NONE', #46851, #33133, #33859, .T. ) ;
#41207=CARTESIAN_POINT ( 'NONE',  ( 9.795823737882805915, -10.50702373788281463, 26.00000000000000000 ) ) ;
#41215=DIRECTION ( 'NONE',  ( -0.000000000000000000, 3.673940397442059868E-16, -1.000000000000000000 ) ) ;
#41233=ORIENTED_EDGE ( 'NONE', *, *, #57565, .T. ) ;
#41236=DIRECTION ( 'NONE',  ( 0.000000000000000000, 0.000000000000000000, -1.000000000000000000 ) ) ;
#41241=CARTESIAN_POINT ( 'NONE',  ( -9.689726262117227762, 8.566576262117216345, 26.00000000000000711 ) ) ;
#41244=ORIENTED_EDGE ( 'NONE', *, *, #2509, .T. ) ;
#41251=DIRECTION ( 'NONE',  ( -0.000000000000000000, -0.000000000000000000, -1.000000000000000000 ) ) ;
#41260=LINE ( 'NONE', #47278, #2795 ) ;
#41271=FACE_OUTER_BOUND ( 'NONE', #54043, .T. ) ;
#41278=ORIENTED_EDGE ( 'NONE', *, *, #3274, .F. ) ;
#41289=ORIENTED_EDGE ( 'NONE', *, *, #48558, .T. ) ;
#41292=DIRECTION ( 'NONE',  ( 0.7071067811865550112, 0.7071067811865401342, 2.597868168706466299E-16 ) ) ;
#41318=VECTOR ( 'NONE', #17054, 1000.000000000000000 ) ;
#41338=DIRECTION ( 'NONE',  ( 1.000000000000000000, 0.000000000000000000, 0.000000000000000000 ) ) ;
#41348=FACE_OUTER_BOUND ( 'NONE', #56345, .T. ) ;
#41349=CARTESIAN_POINT ( 'NONE',  ( -9.915476262117259409, 0.9414762621171833823, 54.00000000000000711 ) ) ;
#41353=ORIENTED_EDGE ( 'NONE', *, *, #68569, .T. ) ;
#41366=VERTEX_POINT ( 'NONE', #9091 ) ;
#41372=AXIS2_PLACEMENT_3D ( 'NONE', #2819, #67540, #47011 ) ;
#41375=CARTESIAN_POINT ( 'NONE',  ( 8.930623737882818602, -8.930623737882855906, 54.00000000000000711 ) ) ;
#41384=CARTESIAN_POINT ( 'NONE',  ( -7.447976262117260049, 9.880476262117177555, 26.00000000000000711 ) ) ;
#41385=FACE_OUTER_BOUND ( 'NONE', #34936, .T. ) ;
#41390=VECTOR ( 'NONE', #28268, 1000.000000000000000 ) ;
#41391=EDGE_CURVE ( 'NONE', #52982, #10498, #20330, .T. ) ;
#41405=CARTESIAN_POINT ( 'NONE',  ( -9.547976262117254365, 8.130476262117182884, 54.00000000000000711 ) ) ;
#41409=FACE_OUTER_BOUND ( 'NONE', #64486, .T. ) ;
#41414=FACE_OUTER_BOUND ( 'NONE', #21554, .T. ) ;
#41415=CARTESIAN_POINT ( 'NONE',  ( 10.31452373788278187, 3.650476262117146042, 54.00000000000000711 ) ) ;
#41416=DIRECTION ( 'NONE',  ( 1.836970198721029934E-16, 1.836970198721010706E-16, -1.000000000000000000 ) ) ;
#41421=LINE ( 'NONE', #68996, #23610 ) ;
#41433=AXIS2_PLACEMENT_3D ( 'NONE', #57334, #30813, #46716 ) ;
#41438=DIRECTION ( 'NONE',  ( -1.836970198721029934E-16, 1.836970198721036590E-16, -1.000000000000000000 ) ) ;
#41441=VECTOR ( 'NONE', #48378, 999.9999999999998863 ) ;
#41442=EDGE_CURVE ( 'NONE', #69370, #20669, #4500, .T. ) ;
#41443=VECTOR ( 'NONE', #12696, 1000.000000000000000 ) ;
#41445=ORIENTED_EDGE ( 'NONE', *, *, #20682, .T. ) ;
#41446=CARTESIAN_POINT ( 'NONE',  ( 8.144523737882817471, -8.835729544836345539, 54.00000000000000711 ) ) ;
#41451=PLANE ( 'NONE',  #61862 ) ;
#41458=DIRECTION ( 'NONE',  ( 9.912705577010336396E-15, 1.000000000000000000, 0.000000000000000000 ) ) ;
#41460=ORIENTED_EDGE ( 'NONE', *, *, #18070, .F. ) ;
#41463=EDGE_CURVE ( 'NONE', #1953, #268, #69882, .T. ) ;
#41464=ORIENTED_EDGE ( 'NONE', *, *, #66662, .T. ) ;
#41465=CYLINDRICAL_SURFACE ( 'NONE', #67618, 1.929199999999998916 ) ;
#41466=LINE ( 'NONE', #64104, #11701 ) ;
#41472=CARTESIAN_POINT ( 'NONE',  ( 7.357023737882797398, 4.947141984184415087, 54.00000000000000711 ) ) ;
#41476=ORIENTED_EDGE ( 'NONE', *, *, #5862, .F. ) ;
#41500=ORIENTED_EDGE ( 'NONE', *, *, #58554, .T. ) ;
#41504=CARTESIAN_POINT ( 'NONE',  ( 4.720772854004770203, 6.344366288193352688, 54.00000000000000711 ) ) ;
#41507=DIRECTION ( 'NONE',  ( 0.4999999999999695799, -0.8660254037844563602, -6.723777587269172655E-17 ) ) ;
#41511=VERTEX_POINT ( 'NONE', #47275 ) ;
#41520=LINE ( 'NONE', #63442, #40432 ) ;
#41521=EDGE_CURVE ( 'NONE', #7028, #69370, #60984, .T. ) ;
#41535=VECTOR ( 'NONE', #69798, 1000.000000000000000 ) ;
#41544=DIRECTION ( 'NONE',  ( -0.8660254037844528074, -0.4999999999999755196, 6.723777587269129514E-17 ) ) ;
#41549=VECTOR ( 'NONE', #11573, 1000.000000000000000 ) ;
#41554=DIRECTION ( 'NONE',  ( -1.836970198721029934E-16, 1.836970198721036590E-16, -1.000000000000000000 ) ) ;
#41561=PLANE ( 'NONE',  #13967 ) ;
#41564=EDGE_CURVE ( 'NONE', #29410, #4021, #33883, .T. ) ;
#41567=VERTEX_POINT ( 'NONE', #16838 ) ;
#41568=ADVANCED_FACE ( 'NONE', ( #945 ), #65622, .T. ) ;
#41575=DIRECTION ( 'NONE',  ( 9.912705577010386883E-15, 1.000000000000000000, 0.000000000000000000 ) ) ;
#41597=CARTESIAN_POINT ( 'NONE',  ( 7.357023737882800951, 6.651770455163678264, 26.00000000000000711 ) ) ;
#41598=LINE ( 'NONE', #15436, #37026 ) ;
#41601=DIRECTION ( 'NONE',  ( 1.678252938371784572E-14, 1.000000000000000000, 0.000000000000000000 ) ) ;
#41602=EDGE_CURVE ( 'NONE', #39378, #55613, #6584, .T. ) ;
#41606=PLANE ( 'NONE',  #3373 ) ;
#41619=CARTESIAN_POINT ( 'NONE',  ( 3.848229544836329730, 7.342976262117204556, 54.00000000000000711 ) ) ;
#41621=LINE ( 'NONE', #25363, #363 ) ;
#41627=CARTESIAN_POINT ( 'NONE',  ( 2.544523737882817382, 9.547976262117206403, 54.00000000000000711 ) ) ;
#41628=EDGE_LOOP ( 'NONE', ( #13804, #48504, #44743, #67103 ) ) ;
#41629=DIRECTION ( 'NONE',  ( -1.836970198721029934E-16, 1.836970198721036590E-16, -1.000000000000000000 ) ) ;
#41631=CARTESIAN_POINT ( 'NONE',  ( 7.357023737882784964, 3.834182069070697807, 54.00000000000000711 ) ) ;
#41632=ORIENTED_EDGE ( 'NONE', *, *, #31182, .F. ) ;
#41638=EDGE_LOOP ( 'NONE', ( #3057, #68648, #20146, #68419 ) ) ;
#41650=ORIENTED_EDGE ( 'NONE', *, *, #227, .T. ) ;
#41658=ORIENTED_EDGE ( 'NONE', *, *, #6317, .T. ) ;
#41661=ORIENTED_EDGE ( 'NONE', *, *, #11560, .F. ) ;
#41662=ORIENTED_EDGE ( 'NONE', *, *, #3298, .F. ) ;
#41663=DIRECTION ( 'NONE',  ( 0.6414496315691494699, -0.7671651518153064231, 0.000000000000000000 ) ) ;
#41669=ORIENTED_EDGE ( 'NONE', *, *, #45582, .F. ) ;
#41674=ORIENTED_EDGE ( 'NONE', *, *, #41851, .F. ) ;
#41678=AXIS2_PLACEMENT_3D ( 'NONE', #40379, #56638, #7834 ) ;
#41679=CARTESIAN_POINT ( 'NONE',  ( 6.832023737882815695, 9.722976262117192903, 54.00000000000000711 ) ) ;
#41691=CARTESIAN_POINT ( 'NONE',  ( -5.779227145995285753, 6.344366288193338477, 54.00000000000000711 ) ) ;
#41693=DIRECTION ( 'NONE',  ( 0.000000000000000000, -3.673940397442059868E-16, 1.000000000000000000 ) ) ;
#41698=ORIENTED_EDGE ( 'NONE', *, *, #19413, .T. ) ;
#41714=ORIENTED_EDGE ( 'NONE', *, *, #46205, .F. ) ;
#41715=FACE_OUTER_BOUND ( 'NONE', #59565, .T. ) ;
#41719=EDGE_LOOP ( 'NONE', ( #27056, #69293, #36326, #9022 ) ) ;
#41720=DIRECTION ( 'NONE',  ( 0.7671651518152895477, -0.6414496315691698980, 0.000000000000000000 ) ) ;
#41727=ORIENTED_EDGE ( 'NONE', *, *, #40333, .T. ) ;
#41730=DIRECTION ( 'NONE',  ( -2.990116172375847553E-15, -1.000000000000000000, -1.836970198721030920E-16 ) ) ;
#41734=ORIENTED_EDGE ( 'NONE', *, *, #30584, .T. ) ;
#41739=AXIS2_PLACEMENT_3D ( 'NONE', #54321, #11852, #21440 ) ;
#41741=ORIENTED_EDGE ( 'NONE', *, *, #62548, .T. ) ;
#41744=EDGE_CURVE ( 'NONE', #46007, #25422, #50737, .T. ) ;
#41746=LINE ( 'NONE', #19478, #59407 ) ;
#41748=ORIENTED_EDGE ( 'NONE', *, *, #42176, .F. ) ;
#41753=DIRECTION ( 'NONE',  ( 1.000000000000000000, 0.000000000000000000, 0.000000000000000000 ) ) ;
#41754=VECTOR ( 'NONE', #36988, 1000.000000000000000 ) ;
#41761=LINE ( 'NONE', #41415, #48228 ) ;
#41763=PLANE ( 'NONE',  #68961 ) ;
#41766=EDGE_LOOP ( 'NONE', ( #10034, #58490, #46595, #35476 ) ) ;
#41779=AXIS2_PLACEMENT_3D ( 'NONE', #43783, #33847, #38145 ) ;
#41781=VERTEX_POINT ( 'NONE', #45786 ) ;
#41783=LINE ( 'NONE', #25887, #4602 ) ;
#41794=ORIENTED_EDGE ( 'NONE', *, *, #29811, .F. ) ;
#41805=CARTESIAN_POINT ( 'NONE',  ( 8.711985858128638682, 2.406732575409522568, 26.00000000000000711 ) ) ;
#41807=ORIENTED_EDGE ( 'NONE', *, *, #44053, .T. ) ;
#41821=DIRECTION ( 'NONE',  ( -1.000000000000000000, 0.000000000000000000, 0.000000000000000000 ) ) ;
#41822=CARTESIAN_POINT ( 'NONE',  ( -6.822336235477446387, -4.149127210878696737, 54.00000000000000711 ) ) ;
#41826=AXIS2_PLACEMENT_3D ( 'NONE', #54329, #65294, #48672 ) ;
#41827=VERTEX_POINT ( 'NONE', #4072 ) ;
#41829=ORIENTED_EDGE ( 'NONE', *, *, #29811, .T. ) ;
#41843=LINE ( 'NONE', #19577, #26697 ) ;
#41849=DIRECTION ( 'NONE',  ( 9.912705577010336396E-15, 1.000000000000000000, 0.000000000000000000 ) ) ;
#41851=EDGE_CURVE ( 'NONE', #50527, #63961, #15019, .T. ) ;
#41855=CARTESIAN_POINT ( 'NONE',  ( 9.912023737882803331, 6.817976262117185549, 54.00000000000000711 ) ) ;
#41857=VERTEX_POINT ( 'NONE', #57796 ) ;
#41863=EDGE_CURVE ( 'NONE', #3011, #41013, #3472, .T. ) ;
#41869=LINE ( 'NONE', #21360, #69749 ) ;
#41880=DIRECTION ( 'NONE',  ( -1.000000000000000000, 9.973078850062115052E-15, -1.836970198721011692E-16 ) ) ;
#41881=CARTESIAN_POINT ( 'NONE',  ( -6.822336235477446387, 6.350872789121265072, 26.00000000000000711 ) ) ;
#41889=FACE_OUTER_BOUND ( 'NONE', #5912, .T. ) ;
#41894=AXIS2_PLACEMENT_3D ( 'NONE', #45352, #40756, #39702 ) ;
#41897=DIRECTION ( 'NONE',  ( -1.836970198721029934E-16, 1.836970198721036344E-16, -1.000000000000000000 ) ) ;
#41902=ORIENTED_EDGE ( 'NONE', *, *, #60547, .F. ) ;
#41905=EDGE_LOOP ( 'NONE', ( #37377, #23928, #30177, #7492 ) ) ;
#41909=DIRECTION ( 'NONE',  ( -0.000000000000000000, 3.673940397442059868E-16, -1.000000000000000000 ) ) ;
#41924=DIRECTION ( 'NONE',  ( 1.836970198721029934E-16, 1.836970198721010706E-16, -1.000000000000000000 ) ) ;
#41925=EDGE_LOOP ( 'NONE', ( #26531, #62272, #6409, #23468 ) ) ;
#41939=CARTESIAN_POINT ( 'NONE',  ( 6.836383711242997485, 6.350872789121265960, 26.00000000000000711 ) ) ;
#41941=VECTOR ( 'NONE', #45615, 1000.000000000000000 ) ;
#41944=DIRECTION ( 'NONE',  ( 7.665540703601096574E-15, 1.000000000000000000, 0.000000000000000000 ) ) ;
#41949=VECTOR ( 'NONE', #16751, 1000.000000000000000 ) ;
#41953=EDGE_LOOP ( 'NONE', ( #539, #39958, #9228, #12723 ) ) ;
#41954=CARTESIAN_POINT ( 'NONE',  ( 3.157023737882809655, -6.501044194225480410, 54.00000000000000711 ) ) ;
#41959=EDGE_CURVE ( 'NONE', #34744, #61431, #18790, .T. ) ;
#41965=ORIENTED_EDGE ( 'NONE', *, *, #41602, .T. ) ;
#41969=PLANE ( 'NONE',  #33405 ) ;
#41971=DIRECTION ( 'NONE',  ( -0.000000000000000000, 3.673940397442059868E-16, -1.000000000000000000 ) ) ;
#41974=ORIENTED_EDGE ( 'NONE', *, *, #6043, .T. ) ;
#41976=ORIENTED_EDGE ( 'NONE', *, *, #113, .T. ) ;
#41986=ORIENTED_EDGE ( 'NONE', *, *, #28057, .F. ) ;
#41988=CARTESIAN_POINT ( 'NONE',  ( 4.149127210878726046, 6.822336235477391320, 54.00000000000000711 ) ) ;
#41990=AXIS2_PLACEMENT_3D ( 'NONE', #20508, #62233, #41720 ) ;
#42000=CARTESIAN_POINT ( 'NONE',  ( -1.620245201994368500, -8.241237374594323484, 26.00000000000000711 ) ) ;
#42003=ADVANCED_FACE ( 'NONE', ( #13128 ), #25153, .F. ) ;
#42010=CARTESIAN_POINT ( 'NONE',  ( -3.650476262117223314, 10.30047626211716683, 54.00000000000000711 ) ) ;
#42012=FACE_OUTER_BOUND ( 'NONE', #45177, .T. ) ;
#42017=CARTESIAN_POINT ( 'NONE',  ( 6.836383711243005479, -6.364920264886905876, 54.00000000000000711 ) ) ;
#42020=CARTESIAN_POINT ( 'NONE',  ( -3.842976262117221875, 10.30047626211716860, 54.00000000000000711 ) ) ;
#42022=CARTESIAN_POINT ( 'NONE',  ( 3.664523737882778853, -10.50702373788280219, 26.00000000000000000 ) ) ;
#42029=CARTESIAN_POINT ( 'NONE',  ( 9.703773737882817940, 10.03972626211715280, 54.00000000000000711 ) ) ;
#42044=CARTESIAN_POINT ( 'NONE',  ( -3.142976262117251451, 6.486996718459839606, 26.00000000000000711 ) ) ;
#42050=VERTEX_POINT ( 'NONE', #47412 ) ;
#42053=ADVANCED_FACE ( 'NONE', ( #68984 ), #36823, .F. ) ;
#42056=EDGE_CURVE ( 'NONE', #29117, #7067, #58022, .T. ) ;
#42057=DIRECTION ( 'NONE',  ( 3.540251991789408222E-15, 1.000000000000000000, 0.000000000000000000 ) ) ;
#42059=DIRECTION ( 'NONE',  ( 0.7671651518153131954, 0.6414496315691415873, 2.587583378555109562E-16 ) ) ;
#42061=EDGE_LOOP ( 'NONE', ( #58868, #21698, #21752, #29442 ) ) ;
#42074=VERTEX_POINT ( 'NONE', #48123 ) ;
#42077=CARTESIAN_POINT ( 'NONE',  ( 7.357023737882817827, -5.552858015815587578, 54.00000000000000711 ) ) ;
#42093=AXIS2_PLACEMENT_3D ( 'NONE', #66244, #17806, #28077 ) ;
#42094=ADVANCED_FACE ( 'NONE', ( #37 ), #20193, .F. ) ;
#42102=CARTESIAN_POINT ( 'NONE',  ( 6.832023737882818359, -9.737023737882822161, 54.00000000000000711 ) ) ;
#42103=AXIS2_PLACEMENT_3D ( 'NONE', #36381, #57948, #9517 ) ;
#42108=LINE ( 'NONE', #16282, #19256 ) ;
#42109=VERTEX_POINT ( 'NONE', #20892 ) ;
#42111=ORIENTED_EDGE ( 'NONE', *, *, #16872, .F. ) ;
#42123=CYLINDRICAL_SURFACE ( 'NONE', #10936, 1.224999999999999423 ) ;
#42128=EDGE_CURVE ( 'NONE', #20150, #48411, #42108, .T. ) ;
#42131=FACE_OUTER_BOUND ( 'NONE', #653, .T. ) ;
#42132=LINE ( 'NONE', #21628, #17052 ) ;
#42141=VERTEX_POINT ( 'NONE', #53432 ) ;
#42149=CARTESIAN_POINT ( 'NONE',  ( -1.466476262117230034, 9.390476262117152473, 26.00000000000000711 ) ) ;
#42154=VERTEX_POINT ( 'NONE', #22632 ) ;
#42176=EDGE_CURVE ( 'NONE', #6834, #14797, #20425, .T. ) ;
#42186=EDGE_CURVE ( 'NONE', #17826, #62241, #60448, .T. ) ;
#42203=CARTESIAN_POINT ( 'NONE',  ( -6.892329165594001772, 4.459829165593958145, 26.00000000000000711 ) ) ;
#42216=ORIENTED_EDGE ( 'NONE', *, *, #60722, .T. ) ;
#42223=PLANE ( 'NONE',  #36491 ) ;
#42224=CIRCLE ( 'NONE', #11727, 1.929199999999997139 ) ;
#42226=DIRECTION ( 'NONE',  ( -1.000000000000000000, 0.000000000000000000, 0.000000000000000000 ) ) ;
#42229=FACE_OUTER_BOUND ( 'NONE', #47406, .T. ) ;
#42239=AXIS2_PLACEMENT_3D ( 'NONE', #32010, #42953, #64537 ) ;
#42241=DIRECTION ( 'NONE',  ( -0.000000000000000000, -0.000000000000000000, -1.000000000000000000 ) ) ;
#42243=EDGE_CURVE ( 'NONE', #69426, #37400, #38552, .T. ) ;
#42246=VECTOR ( 'NONE', #20584, 1000.000000000000000 ) ;
#42247=LINE ( 'NONE', #63828, #35239 ) ;
#42259=ORIENTED_EDGE ( 'NONE', *, *, #59149, .F. ) ;
#42266=ORIENTED_EDGE ( 'NONE', *, *, #10649, .F. ) ;
#42269=EDGE_CURVE ( 'NONE', #41366, #4835, #12481, .T. ) ;
#42271=ORIENTED_EDGE ( 'NONE', *, *, #28973, .F. ) ;
#42275=DIRECTION ( 'NONE',  ( 1.000000000000000000, 0.000000000000000000, 0.000000000000000000 ) ) ;
#42278=ORIENTED_EDGE ( 'NONE', *, *, #61698, .T. ) ;
#42280=CARTESIAN_POINT ( 'NONE',  ( -6.344366288193410419, 4.706725378239148050, 54.00000000000000711 ) ) ;
#42282=ORIENTED_EDGE ( 'NONE', *, *, #1989, .T. ) ;
#42295=AXIS2_PLACEMENT_3D ( 'NONE', #1378, #12308, #50154 ) ;
#42296=DIRECTION ( 'NONE',  ( 0.6414496315691494699, 0.7671651518153064231, 2.818519042764025305E-16 ) ) ;
#42300=PLANE ( 'NONE',  #54780 ) ;
#42311=DIRECTION ( 'NONE',  ( 9.912705577010336396E-15, 1.000000000000000000, 0.000000000000000000 ) ) ;
#42323=EDGE_CURVE ( 'NONE', #48280, #4451, #21684, .T. ) ;
#42325=VECTOR ( 'NONE', #16941, 1000.000000000000000 ) ;
#42335=ORIENTED_EDGE ( 'NONE', *, *, #50444, .T. ) ;
#42336=ORIENTED_EDGE ( 'NONE', *, *, #26573, .T. ) ;
#42339=ADVANCED_FACE ( 'NONE', ( #32292 ), #58824, .T. ) ;
#42342=AXIS2_PLACEMENT_3D ( 'NONE', #50201, #12015, #6718 ) ;
#42349=LINE ( 'NONE', #22183, #1701 ) ;
#42353=ORIENTED_EDGE ( 'NONE', *, *, #47629, .T. ) ;
#42360=DIRECTION ( 'NONE',  ( 0.000000000000000000, -1.000000000000000000, -3.673940397442059868E-16 ) ) ;
#42364=ORIENTED_EDGE ( 'NONE', *, *, #52383, .F. ) ;
#42370=DIRECTION ( 'NONE',  ( -1.047444401652940007E-14, -1.000000000000000000, -1.836970198721029934E-16 ) ) ;
#42374=ORIENTED_EDGE ( 'NONE', *, *, #26941, .F. ) ;
#42381=CIRCLE ( 'NONE', #40086, 1.224999999999997868 ) ;
#42384=CARTESIAN_POINT ( 'NONE',  ( 3.848229544836329730, 7.342976262117204556, 54.00000000000000711 ) ) ;
#42391=AXIS2_PLACEMENT_3D ( 'NONE', #38485, #28886, #60033 ) ;
#42405=LINE ( 'NONE', #63991, #26668 ) ;
#42416=EDGE_LOOP ( 'NONE', ( #9375, #12052, #2776, #49834 ) ) ;
#42418=VECTOR ( 'NONE', #28983, 1000.000000000000000 ) ;
#42423=ORIENTED_EDGE ( 'NONE', *, *, #69036, .F. ) ;
#42436=ORIENTED_EDGE ( 'NONE', *, *, #1028, .T. ) ;
#42438=EDGE_LOOP ( 'NONE', ( #66594, #51464, #13392, #13008 ) ) ;
#42444=AXIS2_PLACEMENT_3D ( 'NONE', #7567, #29133, #50696 ) ;
#42455=EDGE_LOOP ( 'NONE', ( #4791, #49998, #7088, #66142 ) ) ;
#42460=AXIS2_PLACEMENT_3D ( 'NONE', #57966, #26154, #61952 ) ;
#42461=FACE_OUTER_BOUND ( 'NONE', #32861, .T. ) ;
#42463=DIRECTION ( 'NONE',  ( -0.000000000000000000, -0.000000000000000000, -1.000000000000000000 ) ) ;
#42470=CARTESIAN_POINT ( 'NONE',  ( -6.822336235477446387, 6.350872789121265072, 54.00000000000000711 ) ) ;
#42473=CARTESIAN_POINT ( 'NONE',  ( 8.930623737882818602, -10.05377373788282469, 54.00000000000000711 ) ) ;
#42477=CARTESIAN_POINT ( 'NONE',  ( 6.665817930929289759, 7.517976262117195496, 54.00000000000000711 ) ) ;
#42483=VECTOR ( 'NONE', #23185, 1000.000000000000000 ) ;
#42498=CARTESIAN_POINT ( 'NONE',  ( 9.562023737882812569, -8.144523737882824577, 54.00000000000000711 ) ) ;
#42501=DIRECTION ( 'NONE',  ( -1.000000000000000000, 0.000000000000000000, 0.000000000000000000 ) ) ;
#42510=VERTEX_POINT ( 'NONE', #1832 ) ;
#42514=AXIS2_PLACEMENT_3D ( 'NONE', #67331, #66622, #55666 ) ;
#42529=VERTEX_POINT ( 'NONE', #13484 ) ;
#42538=EDGE_CURVE ( 'NONE', #32965, #65821, #13130, .T. ) ;
#42541=CIRCLE ( 'NONE', #27849, 0.1749999999999980738 ) ;
#42542=AXIS2_PLACEMENT_3D ( 'NONE', #68983, #3940, #30099 ) ;
#42545=ORIENTED_EDGE ( 'NONE', *, *, #59801, .F. ) ;
#42548=VECTOR ( 'NONE', #67134, 1000.000000000000000 ) ;
#42554=PLANE ( 'NONE',  #20244 ) ;
#42556=DIRECTION ( 'NONE',  ( -0.000000000000000000, 3.673940397442059868E-16, -1.000000000000000000 ) ) ;
#42557=AXIS2_PLACEMENT_3D ( 'NONE', #30609, #3734, #20349 ) ;
#42558=DIRECTION ( 'NONE',  ( -8.802523127157697409E-15, -1.000000000000000000, -1.836970198721026976E-16 ) ) ;
#42561=AXIS2_PLACEMENT_3D ( 'NONE', #22545, #49756, #1321 ) ;
#42564=ORIENTED_EDGE ( 'NONE', *, *, #51494, .F. ) ;
#42574=EDGE_CURVE ( 'NONE', #21827, #68424, #18792, .T. ) ;
#42575=VERTEX_POINT ( 'NONE', #57326 ) ;
#42580=DIRECTION ( 'NONE',  ( -0.6414496315691367023, 0.7671651518153173033, 0.000000000000000000 ) ) ;
#42582=LINE ( 'NONE', #57792, #60178 ) ;
#42591=VERTEX_POINT ( 'NONE', #67591 ) ;
#42594=ADVANCED_FACE ( 'NONE', ( #41409 ), #58025, .F. ) ;
#42604=DIRECTION ( 'NONE',  ( 1.000000000000000000, -3.491481338843133355E-15, 0.000000000000000000 ) ) ;
#42609=CARTESIAN_POINT ( 'NONE',  ( 1.480523737882788238, -9.404523737882794165, 54.00000000000000711 ) ) ;
#42632=VECTOR ( 'NONE', #69526, 1000.000000000000000 ) ;
#42639=CARTESIAN_POINT ( 'NONE',  ( 6.872275254348383378, 2.989207322240120313, 54.00000000000000711 ) ) ;
#42649=FACE_OUTER_BOUND ( 'NONE', #57782, .T. ) ;
#42653=CARTESIAN_POINT ( 'NONE',  ( -3.842976262117224984, 9.897976262117168744, 54.00000000000000711 ) ) ;
#42656=ADVANCED_FACE ( 'NONE', ( #25154 ), #31173, .T. ) ;
#42659=EDGE_CURVE ( 'NONE', #114, #60715, #62271, .T. ) ;
#42663=VERTEX_POINT ( 'NONE', #36103 ) ;
#42669=CARTESIAN_POINT ( 'NONE',  ( 8.580623737882818958, -8.930623737882855906, 54.00000000000000711 ) ) ;
#42673=EDGE_CURVE ( 'NONE', #62419, #64092, #9954, .T. ) ;
#42676=CARTESIAN_POINT ( 'NONE',  ( -6.835476262117260227, 10.30047626211718104, 26.00000000000000711 ) ) ;
#42686=VERTEX_POINT ( 'NONE', #68647 ) ;
#42690=CARTESIAN_POINT ( 'NONE',  ( -5.242976262117280406, -5.257023737882805747, 54.00000000000000711 ) ) ;
#42692=ORIENTED_EDGE ( 'NONE', *, *, #52129, .F. ) ;
#42703=ORIENTED_EDGE ( 'NONE', *, *, #67052, .F. ) ;
#42719=ORIENTED_EDGE ( 'NONE', *, *, #24149, .T. ) ;
#42721=CARTESIAN_POINT ( 'NONE',  ( 4.046023737882819660, -3.157023737882815873, 26.00000000000000711 ) ) ;
#42722=EDGE_CURVE ( 'NONE', #22368, #8035, #65695, .T. ) ;
#42747=AXIS2_PLACEMENT_3D ( 'NONE', #46114, #8633, #36555 ) ;
#42749=ORIENTED_EDGE ( 'NONE', *, *, #67987, .F. ) ;
#42752=ORIENTED_EDGE ( 'NONE', *, *, #16191, .T. ) ;
#42765=VERTEX_POINT ( 'NONE', #5689 ) ;
#42768=DIRECTION ( 'NONE',  ( 0.7671651518153083105, -0.6414496315691473605, -2.587583378555127804E-16 ) ) ;
#42769=CARTESIAN_POINT ( 'NONE',  ( -9.722976262117303037, -7.969523737882757253, 54.00000000000000711 ) ) ;
#42773=ORIENTED_EDGE ( 'NONE', *, *, #3400, .T. ) ;
#42780=CARTESIAN_POINT ( 'NONE',  ( 2.420780051175147829, -8.711985858128677762, 54.00000000000000711 ) ) ;
#42782=ORIENTED_EDGE ( 'NONE', *, *, #38920, .T. ) ;
#42784=ORIENTED_EDGE ( 'NONE', *, *, #46205, .T. ) ;
#42788=CARTESIAN_POINT ( 'NONE',  ( 4.149127210878725158, -3.677663764522638434, 26.00000000000000711 ) ) ;
#42797=EDGE_LOOP ( 'NONE', ( #2062, #18359, #62731, #1538 ) ) ;
#42804=VERTEX_POINT ( 'NONE', #2102 ) ;
#42812=ORIENTED_EDGE ( 'NONE', *, *, #22470, .F. ) ;
#42825=DIRECTION ( 'NONE',  ( -1.000000000000000000, 8.339399738404101090E-15, -1.836970198721014896E-16 ) ) ;
#42827=CARTESIAN_POINT ( 'NONE',  ( -2.355476262117234931, 8.821682069070680754, 26.00000000000000711 ) ) ;
#42831=DIRECTION ( 'NONE',  ( -0.000000000000000000, 3.673940397442059868E-16, -1.000000000000000000 ) ) ;
#42836=SURFACE_STYLE_FILL_AREA ( #11352 ) ;
#42842=LINE ( 'NONE', #69734, #48458 ) ;
#42852=VERTEX_POINT ( 'NONE', #55842 ) ;
#42855=ORIENTED_EDGE ( 'NONE', *, *, #12668, .T. ) ;
#42860=CARTESIAN_POINT ( 'NONE',  ( -10.30047626211725742, 6.835476262117182955, 26.00000000000000711 ) ) ;
#42863=ORIENTED_EDGE ( 'NONE', *, *, #27630, .F. ) ;
#42864=DIRECTION ( 'NONE',  ( -0.000000000000000000, -0.000000000000000000, -1.000000000000000000 ) ) ;
#42865=ORIENTED_EDGE ( 'NONE', *, *, #51404, .F. ) ;
#42869=DIRECTION ( 'NONE',  ( -1.836970198721029934E-16, -1.836970198721010706E-16, 1.000000000000000000 ) ) ;
#42870=EDGE_CURVE ( 'NONE', #19926, #12566, #55505, .T. ) ;
#42872=VECTOR ( 'NONE', #1634, 999.9999999999998863 ) ;
#42880=EDGE_CURVE ( 'NONE', #43217, #44762, #28969, .T. ) ;
#42881=LINE ( 'NONE', #16025, #41318 ) ;
#42883=VERTEX_POINT ( 'NONE', #44183 ) ;
#42890=EDGE_LOOP ( 'NONE', ( #30256, #47658, #49387, #50663 ) ) ;
#42896=VERTEX_POINT ( 'NONE', #40968 ) ;
#42898=AXIS2_PLACEMENT_3D ( 'NONE', #303, #39165, #34181 ) ;
#42899=FACE_OUTER_BOUND ( 'NONE', #36310, .T. ) ;
#42904=CARTESIAN_POINT ( 'NONE',  ( -8.821682069070780230, 8.130476262117182884, 26.00000000000000711 ) ) ;
#42906=DIRECTION ( 'NONE',  ( -4.956352788505168198E-15, -1.000000000000000000, 0.000000000000000000 ) ) ;
#42909=DIRECTION ( 'NONE',  ( -1.000000000000000000, -0.000000000000000000, -0.000000000000000000 ) ) ;
#42910=CARTESIAN_POINT ( 'NONE',  ( 7.357023737882779635, 3.834182069070702692, 26.00000000000000711 ) ) ;
#42923=CARTESIAN_POINT ( 'NONE',  ( -7.342976262117252517, -3.848229544836288429, 54.00000000000000711 ) ) ;
#42924=CARTESIAN_POINT ( 'NONE',  ( -9.689726262117227762, 10.03972626211718300, 26.00000000000000711 ) ) ;
#42945=VECTOR ( 'NONE', #10819, 1000.000000000000000 ) ;
#42949=ORIENTED_EDGE ( 'NONE', *, *, #16011, .F. ) ;
#42952=VECTOR ( 'NONE', #6457, 1000.000000000000000 ) ;
#42953=DIRECTION ( 'NONE',  ( -1.836970198721029934E-16, -1.836970198721010706E-16, 1.000000000000000000 ) ) ;
#42969=EDGE_CURVE ( 'NONE', #11541, #13296, #35299, .T. ) ;
#42976=FACE_OUTER_BOUND ( 'NONE', #68585, .T. ) ;
#42981=AXIS2_PLACEMENT_3D ( 'NONE', #43489, #37170, #4636 ) ;
#42982=ORIENTED_EDGE ( 'NONE', *, *, #18044, .F. ) ;
#42988=AXIS2_PLACEMENT_3D ( 'NONE', #4928, #63989, #64663 ) ;
#43016=LINE ( 'NONE', #10152, #34934 ) ;
#43029=ORIENTED_EDGE ( 'NONE', *, *, #41442, .F. ) ;
#43030=CARTESIAN_POINT ( 'NONE',  ( 2.544523737882815162, 8.821682069070730492, 54.00000000000000711 ) ) ;
#43033=VECTOR ( 'NONE', #49075, 1000.000000000000000 ) ;
#43041=LINE ( 'NONE', #9837, #36757 ) ;
#43047=ORIENTED_EDGE ( 'NONE', *, *, #27708, .T. ) ;
#43052=EDGE_CURVE ( 'NONE', #60243, #16269, #639, .T. ) ;
#43057=ORIENTED_EDGE ( 'NONE', *, *, #34829, .T. ) ;
#43068=ORIENTED_EDGE ( 'NONE', *, *, #46161, .F. ) ;
#43070=DIRECTION ( 'NONE',  ( 1.000000000000000000, 0.000000000000000000, 0.000000000000000000 ) ) ;
#43076=DIRECTION ( 'NONE',  ( 1.836970198721029934E-16, 1.836970198721010706E-16, -1.000000000000000000 ) ) ;
#43080=ORIENTED_EDGE ( 'NONE', *, *, #3720, .F. ) ;
#43081=DIRECTION ( 'NONE',  ( 0.000000000000000000, -1.000000000000000000, 0.000000000000000000 ) ) ;
#43087=CARTESIAN_POINT ( 'NONE',  ( 7.357023737882817827, -5.552858015815577808, 26.00000000000000711 ) ) ;
#43088=LINE ( 'NONE', #16219, #63516 ) ;
#43091=DIRECTION ( 'NONE',  ( -1.000000000000000000, 0.000000000000000000, 0.000000000000000000 ) ) ;
#43092=CARTESIAN_POINT ( 'NONE',  ( -6.817976262117261044, 9.897976262117179402, 54.00000000000000711 ) ) ;
#43098=DIRECTION ( 'NONE',  ( -1.836970198721029934E-16, 1.836970198721036590E-16, -1.000000000000000000 ) ) ;
#43101=VERTEX_POINT ( 'NONE', #64637 ) ;
#43108=ADVANCED_FACE ( 'NONE', ( #59686 ), #43411, .F. ) ;
#43109=DIRECTION ( 'NONE',  ( 0.6414496315691473605, 0.7671651518153083105, 0.000000000000000000 ) ) ;
#43115=VERTEX_POINT ( 'NONE', #23927 ) ;
#43125=CARTESIAN_POINT ( 'NONE',  ( 6.364920264886846368, 3.663616288756996298, 26.00000000000000711 ) ) ;
#43128=CARTESIAN_POINT ( 'NONE',  ( 3.848229544836325289, 7.517976262117209707, 26.00000000000000711 ) ) ;
#43133=CIRCLE ( 'NONE', #9225, 0.5249999999999994671 ) ;
#43142=VERTEX_POINT ( 'NONE', #6625 ) ;
#43157=VECTOR ( 'NONE', #36755, 1000.000000000000000 ) ;
#43159=LINE ( 'NONE', #42470, #54400 ) ;
#43162=LINE ( 'NONE', #64736, #13211 ) ;
#43177=VERTEX_POINT ( 'NONE', #28871 ) ;
#43184=EDGE_LOOP ( 'NONE', ( #65219, #11734, #34478, #10670 ) ) ;
#43185=DIRECTION ( 'NONE',  ( -0.7071067811865391350, 0.7071067811865560104, 1.750285133459120294E-30 ) ) ;
#43187=ADVANCED_FACE ( 'NONE', ( #18261 ), #56109, .T. ) ;
#43196=LINE ( 'NONE', #21983, #57780 ) ;
#43203=VECTOR ( 'NONE', #52235, 999.9999999999998863 ) ;
#43205=LINE ( 'NONE', #53487, #7093 ) ;
#43208=CIRCLE ( 'NONE', #15001, 1.224999999999997868 ) ;
#43210=FACE_OUTER_BOUND ( 'NONE', #30153, .T. ) ;
#43217=VERTEX_POINT ( 'NONE', #36289 ) ;
#43219=ADVANCED_FACE ( 'NONE', ( #13317 ), #25333, .F. ) ;
#43220=DIRECTION ( 'NONE',  ( 1.000000000000000000, -8.728482790395504563E-15, 0.000000000000000000 ) ) ;
#43236=EDGE_CURVE ( 'NONE', #4021, #43477, #56794, .T. ) ;
#43241=CIRCLE ( 'NONE', #347, 0.3499999999999996447 ) ;
#43242=DIRECTION ( 'NONE',  ( 0.000000000000000000, 0.000000000000000000, 1.000000000000000000 ) ) ;
#43250=ORIENTED_EDGE ( 'NONE', *, *, #30977, .T. ) ;
#43264=CARTESIAN_POINT ( 'NONE',  ( -4.947141984184539432, -7.357023737882807168, 54.00000000000000711 ) ) ;
#43272=EDGE_LOOP ( 'NONE', ( #12974, #19904, #36524, #59397 ) ) ;
#43284=EDGE_CURVE ( 'NONE', #63336, #56487, #27689, .T. ) ;
#43289=LINE ( 'NONE', #27383, #65505 ) ;
#43292=VERTEX_POINT ( 'NONE', #28038 ) ;
#43295=CARTESIAN_POINT ( 'NONE',  ( 10.50702373788278265, 3.650476262117142934, 54.00000000000000711 ) ) ;
#43328=FACE_OUTER_BOUND ( 'NONE', #47109, .T. ) ;
#43332=LINE ( 'NONE', #53273, #6468 ) ;
#43335=CARTESIAN_POINT ( 'NONE',  ( 10.50702373788281996, -3.664523737882826815, 54.00000000000000711 ) ) ;
#43337=DIRECTION ( 'NONE',  ( -1.047444401652940007E-14, -1.000000000000000000, -1.836970198721029934E-16 ) ) ;
#43338=CARTESIAN_POINT ( 'NONE',  ( -4.135079735113209587, -6.836383711242997485, 26.00000000000000711 ) ) ;
#43340=VECTOR ( 'NONE', #29594, 1000.000000000000000 ) ;
#43342=ORIENTED_EDGE ( 'NONE', *, *, #59513, .F. ) ;
#43352=ADVANCED_FACE ( 'NONE', ( #68819 ), #63524, .F. ) ;
#43356=VECTOR ( 'NONE', #1529, 1000.000000000000000 ) ;
#43357=DIRECTION ( 'NONE',  ( 1.836970198721029934E-16, 1.836970198721010706E-16, -1.000000000000000000 ) ) ;
#43358=VECTOR ( 'NONE', #9982, 1000.000000000000114 ) ;
#43365=LINE ( 'NONE', #5894, #57513 ) ;
#43370=CARTESIAN_POINT ( 'NONE',  ( 6.849523737882818430, 10.49297626211719603, 54.00000000000000711 ) ) ;
#43377=DIRECTION ( 'NONE',  ( 0.6414496315691617934, 0.7671651518152962090, 0.000000000000000000 ) ) ;
#43382=ORIENTED_EDGE ( 'NONE', *, *, #21976, .F. ) ;
#43384=CARTESIAN_POINT ( 'NONE',  ( 7.357023737882817827, -6.665817930929295088, 26.00000000000000000 ) ) ;
#43390=ORIENTED_EDGE ( 'NONE', *, *, #16010, .T. ) ;
#43395=CIRCLE ( 'NONE', #67110, 0.7112000000000124889 ) ;
#43396=CIRCLE ( 'NONE', #12884, 1.224999999999999423 ) ;
#43411=CYLINDRICAL_SURFACE ( 'NONE', #50064, 0.1749999999999993783 ) ;
#43421=LINE ( 'NONE', #11242, #55014 ) ;
#43426=CARTESIAN_POINT ( 'NONE',  ( -10.49297626211729551, -6.849523737882748264, 54.00000000000000711 ) ) ;
#43430=FACE_OUTER_BOUND ( 'NONE', #442, .T. ) ;
#43436=CARTESIAN_POINT ( 'NONE',  ( -1.466476262117315743, -8.612468434717266419, 54.00000000000000711 ) ) ;
#43440=EDGE_CURVE ( 'NONE', #21439, #25606, #64932, .T. ) ;
#43443=AXIS2_PLACEMENT_3D ( 'NONE', #25134, #62599, #57657 ) ;
#43446=EDGE_LOOP ( 'NONE', ( #60484, #24150, #65418, #59623 ) ) ;
#43449=CARTESIAN_POINT ( 'NONE',  ( 7.357023737882802727, 5.538810540049955655, 54.00000000000000711 ) ) ;
#43454=EDGE_CURVE ( 'NONE', #20164, #32475, #23065, .T. ) ;
#43459=ADVANCED_FACE ( 'NONE', ( #39666 ), #12787, .F. ) ;
#43467=LINE ( 'NONE', #10954, #3902 ) ;
#43477=VERTEX_POINT ( 'NONE', #39332 ) ;
#43489=CARTESIAN_POINT ( 'NONE',  ( 5.257023737882795977, 5.242976262117205799, 26.00000000000000711 ) ) ;
#43503=EDGE_CURVE ( 'NONE', #66440, #68576, #23766, .T. ) ;
#43505=CARTESIAN_POINT ( 'NONE',  ( 5.552858015815571591, 7.342976262117199227, 54.00000000000000711 ) ) ;
#43517=AXIS2_PLACEMENT_3D ( 'NONE', #44369, #39760, #50381 ) ;
#43519=LINE ( 'NONE', #11007, #69106 ) ;
#43529=ORIENTED_EDGE ( 'NONE', *, *, #33550, .F. ) ;
#43536=CARTESIAN_POINT ( 'NONE',  ( -5.242976262117275077, -5.257023737882800418, 26.00000000000000711 ) ) ;
#43547=EDGE_CURVE ( 'NONE', #45109, #27729, #62285, .T. ) ;
#43550=VECTOR ( 'NONE', #9082, 1000.000000000000000 ) ;
#43560=EDGE_LOOP ( 'NONE', ( #33475, #57315, #34305, #67388 ) ) ;
#43563=ADVANCED_FACE ( 'NONE', ( #56978 ), #25172, .F. ) ;
#43567=CARTESIAN_POINT ( 'NONE',  ( 3.664523737882778853, -10.50702373788281285, 54.00000000000000711 ) ) ;
#43575=VECTOR ( 'NONE', #10562, 1000.000000000000114 ) ;
#43577=CARTESIAN_POINT ( 'NONE',  ( 9.929523737882751888, 0.9414762621171479662, 54.00000000000000711 ) ) ;
#43606=DIRECTION ( 'NONE',  ( 3.491481338843133355E-15, 1.000000000000000000, 1.836970198721029934E-16 ) ) ;
#43609=EDGE_CURVE ( 'NONE', #61431, #4997, #17565, .T. ) ;
#43610=CARTESIAN_POINT ( 'NONE',  ( -9.781776262117324094, -10.50702373788275779, 54.00000000000000711 ) ) ;
#43611=AXIS2_PLACEMENT_3D ( 'NONE', #3065, #24632, #67752 ) ;
#43616=EDGE_CURVE ( 'NONE', #38860, #10751, #60471, .T. ) ;
#43617=EDGE_CURVE ( 'NONE', #14797, #37068, #9611, .T. ) ;
#43624=VERTEX_POINT ( 'NONE', #8897 ) ;
#43632=DIRECTION ( 'NONE',  ( 1.836970198721029934E-16, 1.836970198721010706E-16, -1.000000000000000000 ) ) ;
#43633=ORIENTED_EDGE ( 'NONE', *, *, #1700, .F. ) ;
#43639=EDGE_LOOP ( 'NONE', ( #16104, #41986, #34353, #51955 ) ) ;
#43645=DIRECTION ( 'NONE',  ( -1.000000000000000000, 0.000000000000000000, 0.000000000000000000 ) ) ;
#43647=AXIS2_PLACEMENT_3D ( 'NONE', #54232, #43606, #44284 ) ;
#43655=ORIENTED_EDGE ( 'NONE', *, *, #42056, .T. ) ;
#43657=DIRECTION ( 'NONE',  ( 1.000000000000000000, -1.952517519553884087E-14, 1.836970198720994435E-16 ) ) ;
#43658=CARTESIAN_POINT ( 'NONE',  ( 5.257023737882819070, -5.257023737882815517, 26.00000000000000711 ) ) ;
#43691=DIRECTION ( 'NONE',  ( -1.000000000000000000, 0.000000000000000000, 0.000000000000000000 ) ) ;
#43708=CARTESIAN_POINT ( 'NONE',  ( 7.357023737882817827, -3.848229544836335947, 26.00000000000000711 ) ) ;
#43709=VECTOR ( 'NONE', #37184, 1000.000000000000000 ) ;
#43710=CARTESIAN_POINT ( 'NONE',  ( 10.50702373788281996, -3.664523737882816157, 26.00000000000000711 ) ) ;
#43711=AXIS2_PLACEMENT_3D ( 'NONE', #28241, #60074, #32866 ) ;
#43723=EDGE_CURVE ( 'NONE', #28927, #32858, #1088, .T. ) ;
#43724=VECTOR ( 'NONE', #53012, 1000.000000000000114 ) ;
#43731=VERTEX_POINT ( 'NONE', #16663 ) ;
#43738=CARTESIAN_POINT ( 'NONE',  ( 8.580623737882849156, 9.689726262117156708, 54.00000000000000711 ) ) ;
#43740=ORIENTED_EDGE ( 'NONE', *, *, #51847, .T. ) ;
#43741=VERTEX_POINT ( 'NONE', #16999 ) ;
#43762=EDGE_CURVE ( 'NONE', #49997, #37598, #61861, .T. ) ;
#43771=ADVANCED_FACE ( 'NONE', ( #34270 ), #56552, .T. ) ;
#43773=DIRECTION ( 'NONE',  ( -1.000000000000000000, 0.000000000000000000, 0.000000000000000000 ) ) ;
#43776=CARTESIAN_POINT ( 'NONE',  ( 10.31452373788281562, -6.849523737882814878, 26.00000000000000000 ) ) ;
#43778=LINE ( 'NONE', #65349, #41549 ) ;
#43783=CARTESIAN_POINT ( 'NONE',  ( 7.357023737882802727, 5.538810540049955655, 54.00000000000000711 ) ) ;
#43784=CARTESIAN_POINT ( 'NONE',  ( -2.530476262117313357, -8.835729544836349092, 26.00000000000000711 ) ) ;
#43785=DIRECTION ( 'NONE',  ( -0.7071067811865451302, 0.7071067811865500152, 2.597868168706484541E-16 ) ) ;
#43786=VERTEX_POINT ( 'NONE', #7407 ) ;
#43800=CARTESIAN_POINT ( 'NONE',  ( -7.394232575409600550, -3.724485858128637084, 26.00000000000000711 ) ) ;
#43804=CARTESIAN_POINT ( 'NONE',  ( 2.632023737882809744, -6.501044194225475081, 54.00000000000000711 ) ) ;
#43805=DIRECTION ( 'NONE',  ( 0.5000000000000068834, 0.8660254037844345998, 6.723777587268309839E-17 ) ) ;
#43807=EDGE_CURVE ( 'NONE', #16156, #33225, #24382, .T. ) ;
#43809=ADVANCED_FACE ( 'NONE', ( #34627 ), #39582, .F. ) ;
#43817=ORIENTED_EDGE ( 'NONE', *, *, #30269, .F. ) ;
#43830=ORIENTED_EDGE ( 'NONE', *, *, #59245, .F. ) ;
#43831=VERTEX_POINT ( 'NONE', #2116 ) ;
#43835=ORIENTED_EDGE ( 'NONE', *, *, #43993, .T. ) ;
#43841=DIRECTION ( 'NONE',  ( -4.956352788505168198E-15, -1.000000000000000000, 0.000000000000000000 ) ) ;
#43844=ORIENTED_EDGE ( 'NONE', *, *, #4743, .F. ) ;
#43846=EDGE_CURVE ( 'NONE', #35523, #1729, #19842, .T. ) ;
#43849=CARTESIAN_POINT ( 'NONE',  ( -6.350872789121319251, -3.677663764522589140, 54.00000000000000711 ) ) ;
#43852=CARTESIAN_POINT ( 'NONE',  ( 9.703773737882785966, -8.580623737882856261, 54.00000000000000711 ) ) ;
#43863=EDGE_LOOP ( 'NONE', ( #38020, #44734, #2930, #12004 ) ) ;
#43869=CARTESIAN_POINT ( 'NONE',  ( 5.257023737882801306, 5.242976262117200470, 54.00000000000000711 ) ) ;
#43872=CYLINDRICAL_SURFACE ( 'NONE', #31753, 0.5249999999999990230 ) ;
#43880=LINE ( 'NONE', #5019, #55221 ) ;
#43881=ORIENTED_EDGE ( 'NONE', *, *, #57607, .F. ) ;
#43886=EDGE_CURVE ( 'NONE', #60715, #20779, #62203, .T. ) ;
#43891=EDGE_LOOP ( 'NONE', ( #48842, #67748, #24704, #65951 ) ) ;
#43899=AXIS2_PLACEMENT_3D ( 'NONE', #41152, #58125, #2988 ) ;
#43901=CARTESIAN_POINT ( 'NONE',  ( -6.651770455163739548, 7.342976262117183239, 54.00000000000000711 ) ) ;
#43910=DIRECTION ( 'NONE',  ( 1.000000000000000000, 2.135044278125301343E-15, -0.000000000000000000 ) ) ;
#43912=VECTOR ( 'NONE', #25716, 1000.000000000000000 ) ;
#43915=ORIENTED_EDGE ( 'NONE', *, *, #29385, .F. ) ;
#43921=ORIENTED_EDGE ( 'NONE', *, *, #26747, .F. ) ;
#43935=DIRECTION ( 'NONE',  ( 0.000000000000000000, 0.000000000000000000, 1.000000000000000000 ) ) ;
#43936=CARTESIAN_POINT ( 'NONE',  ( 7.357023737882817827, -4.961189459950053227, 26.00000000000000711 ) ) ;
#43939=EDGE_CURVE ( 'NONE', #9110, #36010, #9171, .T. ) ;
#43942=EDGE_CURVE ( 'NONE', #15565, #43142, #3170, .T. ) ;
#43950=AXIS2_PLACEMENT_3D ( 'NONE', #14550, #3955, #25526 ) ;
#43952=EDGE_LOOP ( 'NONE', ( #7552, #6995, #18638, #6535 ) ) ;
#43958=EDGE_LOOP ( 'NONE', ( #48010, #48421, #11230, #4774 ) ) ;
#43962=LINE ( 'NONE', #64505, #6141 ) ;
#43971=CARTESIAN_POINT ( 'NONE',  ( 4.155633711806655306, 4.706725378239160484, 54.00000000000000711 ) ) ;
#43974=ORIENTED_EDGE ( 'NONE', *, *, #65796, .T. ) ;
#43978=PLANE ( 'NONE',  #48870 ) ;
#43979=ORIENTED_EDGE ( 'NONE', *, *, #52154, .T. ) ;
#43993=EDGE_CURVE ( 'NONE', #16593, #15802, #11244, .T. ) ;
#43997=ORIENTED_EDGE ( 'NONE', *, *, #40807, .T. ) ;
#44000=EDGE_CURVE ( 'NONE', #18538, #4880, #13064, .T. ) ;
#44008=CARTESIAN_POINT ( 'NONE',  ( 5.793274621760843957, -4.155633711806661523, 26.00000000000000711 ) ) ;
#44014=DIRECTION ( 'NONE',  ( -0.000000000000000000, -0.000000000000000000, -1.000000000000000000 ) ) ;
#44016=EDGE_CURVE ( 'NONE', #28088, #1387, #37102, .T. ) ;
#44018=DIRECTION ( 'NONE',  ( -0.000000000000000000, 0.000000000000000000, -1.000000000000000000 ) ) ;
#44019=EDGE_CURVE ( 'NONE', #55229, #43831, #16912, .T. ) ;
#44024=DIRECTION ( 'NONE',  ( 3.491481338843133355E-15, 1.000000000000000000, 1.836970198721029934E-16 ) ) ;
#44025=CARTESIAN_POINT ( 'NONE',  ( -3.834182069070765309, 7.342976262117171693, 54.00000000000000711 ) ) ;
#44027=APPLICATION_CONTEXT ( 'automotive_design' ) ;
#44028=DIRECTION ( 'NONE',  ( -3.491481338843133355E-15, -1.000000000000000000, -1.836970198721029934E-16 ) ) ;
#44030=CYLINDRICAL_SURFACE ( 'NONE', #26045, 1.224999999999999423 ) ;
#44047=EDGE_CURVE ( 'NONE', #46469, #53664, #54056, .T. ) ;
#44053=EDGE_CURVE ( 'NONE', #56837, #26653, #5613, .T. ) ;
#44056=DIRECTION ( 'NONE',  ( 1.000000000000000000, 0.000000000000000000, 0.000000000000000000 ) ) ;
#44057=ORIENTED_EDGE ( 'NONE', *, *, #54874, .T. ) ;
#44077=ORIENTED_EDGE ( 'NONE', *, *, #2548, .F. ) ;
#44078=LINE ( 'NONE', #21137, #38024 ) ;
#44084=EDGE_CURVE ( 'NONE', #10363, #67274, #56125, .T. ) ;
#44086=PLANE ( 'NONE',  #59302 ) ;
#44089=ORIENTED_EDGE ( 'NONE', *, *, #37080, .F. ) ;
#44092=AXIS2_PLACEMENT_3D ( 'NONE', #27793, #11512, #60305 ) ;
#44094=ORIENTED_EDGE ( 'NONE', *, *, #14484, .T. ) ;
#44095=ORIENTED_EDGE ( 'NONE', *, *, #56486, .F. ) ;
#44109=CIRCLE ( 'NONE', #1180, 0.3499999999999996447 ) ;
#44113=CARTESIAN_POINT ( 'NONE',  ( 2.005523737882793256, -8.612468434717211352, 26.00000000000000000 ) ) ;
#44115=CARTESIAN_POINT ( 'NONE',  ( 6.849523737882814878, 10.30047626211719702, 26.00000000000000711 ) ) ;
#44117=LINE ( 'NONE', #65694, #17544 ) ;
#44119=DIRECTION ( 'NONE',  ( 0.7071067811865441310, -0.7071067811865510144, -2.597868168706485034E-16 ) ) ;
#44125=EDGE_LOOP ( 'NONE', ( #40846, #58048, #18331, #3544 ) ) ;
#44133=DIRECTION ( 'NONE',  ( 1.000000000000000000, -1.047444401652940007E-14, 1.836970198721010706E-16 ) ) ;
#44138=ADVANCED_FACE ( 'NONE', ( #65692 ), #6973, .F. ) ;
#44166=CARTESIAN_POINT ( 'NONE',  ( -2.355476262117229158, 9.547976262117156665, 26.00000000000000711 ) ) ;
#44175=CARTESIAN_POINT ( 'NONE',  ( -10.03972626211722918, 9.689726262117183353, 26.00000000000000711 ) ) ;
#44183=CARTESIAN_POINT ( 'NONE',  ( -5.779227145995285753, 4.141586236041028712, 54.00000000000000711 ) ) ;
#44188=CARTESIAN_POINT ( 'NONE',  ( -3.667976262117323305, -9.737023737882815055, 26.00000000000000000 ) ) ;
#44189=CARTESIAN_POINT ( 'NONE',  ( 6.849523737882817542, -10.50702373788281463, 26.00000000000000000 ) ) ;
#44190=DIRECTION ( 'NONE',  ( 1.000000000000000000, 0.000000000000000000, 0.000000000000000000 ) ) ;
#44201=CARTESIAN_POINT ( 'NONE',  ( -1.466476262117318852, -9.404523737882838574, 26.00000000000000711 ) ) ;
#44238=LINE ( 'NONE', #17725, #48921 ) ;
#44240=DIRECTION ( 'NONE',  ( 0.8660254037844510311, 0.4999999999999785727, 1.836970198720951294E-16 ) ) ;
#44243=FACE_OUTER_BOUND ( 'NONE', #34958, .T. ) ;
#44245=ORIENTED_EDGE ( 'NONE', *, *, #31431, .F. ) ;
#44247=VECTOR ( 'NONE', #957, 1000.000000000000000 ) ;
#44250=LINE ( 'NONE', #65825, #15201 ) ;
#44258=DIRECTION ( 'NONE',  ( -1.000000000000000000, 0.000000000000000000, 0.000000000000000000 ) ) ;
#44260=ORIENTED_EDGE ( 'NONE', *, *, #55803, .T. ) ;
#44261=DIRECTION ( 'NONE',  ( 1.000000000000000000, 2.135044278125299371E-15, 7.844025423732057781E-31 ) ) ;
#44263=ORIENTED_EDGE ( 'NONE', *, *, #54480, .F. ) ;
#44280=DIRECTION ( 'NONE',  ( -1.836970198721029934E-16, 1.836970198721036590E-16, -1.000000000000000000 ) ) ;
#44282=ORIENTED_EDGE ( 'NONE', *, *, #64356, .T. ) ;
#44284=DIRECTION ( 'NONE',  ( -1.000000000000000000, 3.491481338843133355E-15, 0.000000000000000000 ) ) ;
#44292=LINE ( 'NONE', #16399, #47179 ) ;
#44294=CIRCLE ( 'NONE', #47746, 0.1749999999999998224 ) ;
#44303=ORIENTED_EDGE ( 'NONE', *, *, #10623, .T. ) ;
#44307=DIRECTION ( 'NONE',  ( -0.000000000000000000, -0.000000000000000000, -1.000000000000000000 ) ) ;
#44308=VERTEX_POINT ( 'NONE', #42653 ) ;
#44313=EDGE_CURVE ( 'NONE', #34946, #24260, #16370, .T. ) ;
#44314=DIRECTION ( 'NONE',  ( 0.7071067811865539010, 0.7071067811865411334, -1.887411345499491136E-30 ) ) ;
#44317=EDGE_CURVE ( 'NONE', #43624, #14837, #48315, .T. ) ;
#44323=ORIENTED_EDGE ( 'NONE', *, *, #24145, .T. ) ;
#44329=EDGE_CURVE ( 'NONE', #56086, #35347, #58922, .T. ) ;
#44334=CARTESIAN_POINT ( 'NONE',  ( -6.344366288193410419, 4.706725378239148050, 54.00000000000000711 ) ) ;
#44336=ORIENTED_EDGE ( 'NONE', *, *, #15675, .F. ) ;
#44344=DIRECTION ( 'NONE',  ( -1.836970198721029934E-16, 1.836970198721036590E-16, -1.000000000000000000 ) ) ;
#44354=CARTESIAN_POINT ( 'NONE',  ( -7.517976262117260333, 3.834182069070703580, 26.00000000000000711 ) ) ;
#44358=ORIENTED_EDGE ( 'NONE', *, *, #36690, .F. ) ;
#44369=CARTESIAN_POINT ( 'NONE',  ( 9.795823737882805915, -9.795823737882811244, 54.00000000000000711 ) ) ;
#44379=DIRECTION ( 'NONE',  ( -0.7071067811865446862, 0.7071067811865503483, -0.000000000000000000 ) ) ;
#44380=EDGE_CURVE ( 'NONE', #16502, #9404, #10821, .T. ) ;
#44392=DIRECTION ( 'NONE',  ( -0.000000000000000000, 1.000000000000000000, -0.000000000000000000 ) ) ;
#44397=VERTEX_POINT ( 'NONE', #16484 ) ;
#44400=DIRECTION ( 'NONE',  ( -1.836970198721029934E-16, -1.836970198721010706E-16, 1.000000000000000000 ) ) ;
#44403=ADVANCED_FACE ( 'NONE', ( #26058 ), #42300, .F. ) ;
#44407=ORIENTED_EDGE ( 'NONE', *, *, #50547, .F. ) ;
#44410=DIRECTION ( 'NONE',  ( 1.000000000000000000, -3.016910393003147986E-15, 0.000000000000000000 ) ) ;
#44411=ORIENTED_EDGE ( 'NONE', *, *, #34647, .F. ) ;
#44413=ORIENTED_EDGE ( 'NONE', *, *, #21979, .F. ) ;
#44420=DIRECTION ( 'NONE',  ( -7.457533623526253657E-15, -1.000000000000000000, -1.836970198721024757E-16 ) ) ;
#44427=CARTESIAN_POINT ( 'NONE',  ( 5.257023737882819070, -5.257023737882815517, 26.00000000000000711 ) ) ;
#44428=CARTESIAN_POINT ( 'NONE',  ( 3.664523737882820598, 10.49297626211720491, 54.00000000000000711 ) ) ;
#44433=VECTOR ( 'NONE', #35909, 1000.000000000000000 ) ;
#44442=LINE ( 'NONE', #38476, #36364 ) ;
#44445=DIRECTION ( 'NONE',  ( -1.000000000000000000, 8.728482790395504563E-15, 0.000000000000000000 ) ) ;
#44447=CIRCLE ( 'NONE', #13979, 1.224999999999999423 ) ;
#44448=EDGE_CURVE ( 'NONE', #48595, #39506, #24278, .T. ) ;
#44451=CYLINDRICAL_SURFACE ( 'NONE', #36954, 1.929199999999998028 ) ;
#44455=LINE ( 'NONE', #60374, #55223 ) ;
#44456=EDGE_CURVE ( 'NONE', #7568, #30669, #54835, .T. ) ;
#44467=EDGE_CURVE ( 'NONE', #51741, #18742, #45419, .T. ) ;
#44480=DIRECTION ( 'NONE',  ( 1.836970198721029934E-16, 1.836970198721010706E-16, -1.000000000000000000 ) ) ;
#44486=ORIENTED_EDGE ( 'NONE', *, *, #9778, .F. ) ;
#44490=AXIS2_PLACEMENT_3D ( 'NONE', #6647, #49784, #43091 ) ;
#44492=CARTESIAN_POINT ( 'NONE',  ( 3.677663764522614454, -4.149127210878770455, 54.00000000000000711 ) ) ;
#44495=DIRECTION ( 'NONE',  ( -1.000000000000000000, 3.491481338843133355E-15, 1.836970198721036344E-16 ) ) ;
#44496=CARTESIAN_POINT ( 'NONE',  ( 9.562023737882766383, 2.530476262117153485, 54.00000000000000711 ) ) ;
#44504=AXIS2_PLACEMENT_3D ( 'NONE', #17630, #39203, #51198 ) ;
#44507=EDGE_LOOP ( 'NONE', ( #24073, #4425, #1878, #39210 ) ) ;
#44510=LINE ( 'NONE', #45557, #42548 ) ;
#44516=VERTEX_POINT ( 'NONE', #51435 ) ;
#44523=FACE_OUTER_BOUND ( 'NONE', #22925, .T. ) ;
#44524=VERTEX_POINT ( 'NONE', #3345 ) ;
#44532=DIRECTION ( 'NONE',  ( 1.671920889371702854E-15, -1.000000000000000000, 0.000000000000000000 ) ) ;
#44538=CARTESIAN_POINT ( 'NONE',  ( 8.835729544836325999, 7.955476262117193720, 26.00000000000000711 ) ) ;
#44540=ORIENTED_EDGE ( 'NONE', *, *, #5863, .T. ) ;
#44554=CARTESIAN_POINT ( 'NONE',  ( -7.517976262117260333, 3.834182069070703580, 54.00000000000000711 ) ) ;
#44565=DIRECTION ( 'NONE',  ( -1.000000000000000000, 1.920885163218982051E-15, 1.836970198721033385E-16 ) ) ;
#44567=ORIENTED_EDGE ( 'NONE', *, *, #25487, .T. ) ;
#44579=CARTESIAN_POINT ( 'NONE',  ( 8.930623737882839919, 8.916576262117192897, 26.00000000000000711 ) ) ;
#44581=DIRECTION ( 'NONE',  ( -1.000000000000000000, 0.000000000000000000, 0.000000000000000000 ) ) ;
#44588=CARTESIAN_POINT ( 'NONE',  ( -0.9414762621172296786, 9.390476262117148920, 26.00000000000000711 ) ) ;
#44595=CARTESIAN_POINT ( 'NONE',  ( 10.31452373788281562, -3.857023737882824932, 54.00000000000000711 ) ) ;
#44599=DIRECTION ( 'NONE',  ( -1.034072152899300274E-14, -1.000000000000000000, 0.000000000000000000 ) ) ;
#44600=CARTESIAN_POINT ( 'NONE',  ( 4.149127210878725158, -3.677663764522648648, 54.00000000000000711 ) ) ;
#44607=EDGE_LOOP ( 'NONE', ( #12054, #31261, #61390, #64546 ) ) ;
#44617=ADVANCED_FACE ( 'NONE', ( #32663 ), #21004, .F. ) ;
#44625=LINE ( 'NONE', #50290, #30234 ) ;
#44627=DIRECTION ( 'NONE',  ( -1.836970198721029934E-16, 1.836970198721036590E-16, -1.000000000000000000 ) ) ;
#44629=EDGE_LOOP ( 'NONE', ( #12816, #64893, #23900, #33291 ) ) ;
#44634=VECTOR ( 'NONE', #40640, 1000.000000000000000 ) ;
#44641=ORIENTED_EDGE ( 'NONE', *, *, #10808, .F. ) ;
#44643=CARTESIAN_POINT ( 'NONE',  ( 2.369523737882786918, -9.562023737882798358, 54.00000000000000711 ) ) ;
#44654=DIRECTION ( 'NONE',  ( 0.000000000000000000, 1.000000000000000000, 3.673940397442059868E-16 ) ) ;
#44671=LINE ( 'NONE', #1549, #63199 ) ;
#44686=CARTESIAN_POINT ( 'NONE',  ( -3.142976262117251451, 6.486996718459839606, 26.00000000000000711 ) ) ;
#44699=AXIS2_PLACEMENT_3D ( 'NONE', #27412, #17141, #48987 ) ;
#44704=PLANE ( 'NONE',  #34297 ) ;
#44720=CARTESIAN_POINT ( 'NONE',  ( 10.50702373788280752, 6.835476262117182067, 54.00000000000000711 ) ) ;
#44731=AXIS2_PLACEMENT_3D ( 'NONE', #58733, #15608, #19838 ) ;
#44734=ORIENTED_EDGE ( 'NONE', *, *, #54954, .F. ) ;
#44736=AXIS2_PLACEMENT_3D ( 'NONE', #63596, #3149, #9146 ) ;
#44738=CARTESIAN_POINT ( 'NONE',  ( -6.642976262117260333, 10.30047626211718104, 54.00000000000000711 ) ) ;
#44739=VERTEX_POINT ( 'NONE', #5800 ) ;
#44740=VECTOR ( 'NONE', #65186, 1000.000000000000000 ) ;
#44743=ORIENTED_EDGE ( 'NONE', *, *, #46630, .F. ) ;
#44746=DIRECTION ( 'NONE',  ( 0.000000000000000000, 0.000000000000000000, 1.000000000000000000 ) ) ;
#44753=AXIS2_PLACEMENT_3D ( 'NONE', #13226, #34788, #61295 ) ;
#44755=EDGE_LOOP ( 'NONE', ( #64545, #15684, #57747, #12583 ) ) ;
#44759=ADVANCED_FACE ( 'NONE', ( #65870 ), #4413, .F. ) ;
#44762=VERTEX_POINT ( 'NONE', #38322 ) ;
#44766=EDGE_LOOP ( 'NONE', ( #12476, #24600, #55395, #65637 ) ) ;
#44768=DIRECTION ( 'NONE',  ( 0.000000000000000000, 1.000000000000000000, 0.000000000000000000 ) ) ;
#44782=( GEOMETRIC_REPRESENTATION_CONTEXT ( 3 ) GLOBAL_UNCERTAINTY_ASSIGNED_CONTEXT ( ( #47928 ) ) GLOBAL_UNIT_ASSIGNED_CONTEXT ( ( #55997, #24164, #50680 ) ) REPRESENTATION_CONTEXT ( 'NONE', 'WORKASPACE' ) );
#44785=EDGE_CURVE ( 'NONE', #51180, #61547, #59877, .T. ) ;
#44788=VERTEX_POINT ( 'NONE', #54588 ) ;
#44793=EDGE_CURVE ( 'NONE', #15217, #22970, #17782, .T. ) ;
#44795=LINE ( 'NONE', #49078, #39609 ) ;
#44796=EDGE_CURVE ( 'NONE', #48238, #34255, #38996, .T. ) ;
#44797=VECTOR ( 'NONE', #27497, 1000.000000000000114 ) ;
#44804=ADVANCED_FACE ( 'NONE', ( #7513 ), #12120, .F. ) ;
#44811=ORIENTED_EDGE ( 'NONE', *, *, #48560, .T. ) ;
#44817=DIRECTION ( 'NONE',  ( -1.836970198721029934E-16, 1.836970198721036344E-16, -1.000000000000000000 ) ) ;
#44822=ORIENTED_EDGE ( 'NONE', *, *, #32760, .F. ) ;
#44827=DIRECTION ( 'NONE',  ( 1.000000000000000000, -5.120954910632640039E-15, 0.000000000000000000 ) ) ;
#44830=CIRCLE ( 'NONE', #14371, 0.1749999999999989342 ) ;
#44832=CARTESIAN_POINT ( 'NONE',  ( -6.775514141871427753, -7.408280051175141878, 54.00000000000000711 ) ) ;
#44835=LINE ( 'NONE', #65727, #61037 ) ;
#44842=DIRECTION ( 'NONE',  ( 1.000000000000000000, 0.000000000000000000, 0.000000000000000000 ) ) ;
#44843=CARTESIAN_POINT ( 'NONE',  ( -9.689726262117227762, 8.566576262117216345, 54.00000000000000711 ) ) ;
#44845=EDGE_LOOP ( 'NONE', ( #54457, #35983, #62546, #25130 ) ) ;
#44846=FACE_OUTER_BOUND ( 'NONE', #23903, .T. ) ;
#44858=ORIENTED_EDGE ( 'NONE', *, *, #29939, .F. ) ;
#44859=VECTOR ( 'NONE', #25788, 1000.000000000000000 ) ;
#44862=ORIENTED_EDGE ( 'NONE', *, *, #44016, .F. ) ;
#44865=ADVANCED_FACE ( 'NONE', ( #68931 ), #13517, .F. ) ;
#44872=LINE ( 'NONE', #38876, #68099 ) ;
#44875=ORIENTED_EDGE ( 'NONE', *, *, #26941, .T. ) ;
#44879=EDGE_CURVE ( 'NONE', #19218, #28927, #42405, .T. ) ;
#44890=DIRECTION ( 'NONE',  ( -0.7071067811865503483, 0.7071067811865446862, 0.000000000000000000 ) ) ;
#44900=AXIS2_PLACEMENT_3D ( 'NONE', #4678, #32238, #68321 ) ;
#44902=DIRECTION ( 'NONE',  ( -1.000000000000000000, 0.000000000000000000, 0.000000000000000000 ) ) ;
#44904=DIRECTION ( 'NONE',  ( -1.000000000000000000, 0.000000000000000000, 0.000000000000000000 ) ) ;
#44912=ADVANCED_FACE ( 'NONE', ( #17257 ), #11940, .F. ) ;
#44918=VECTOR ( 'NONE', #10554, 1000.000000000000114 ) ;
#44921=CARTESIAN_POINT ( 'NONE',  ( -3.663616288757055806, 6.350872789121238426, 54.00000000000000711 ) ) ;
#44931=VERTEX_POINT ( 'NONE', #16225 ) ;
#44932=EDGE_CURVE ( 'NONE', #36248, #16269, #22577, .T. ) ;
#44958=ORIENTED_EDGE ( 'NONE', *, *, #68169, .F. ) ;
#44961=CARTESIAN_POINT ( 'NONE',  ( -5.242976262117280406, -5.257023737882805747, 54.00000000000000711 ) ) ;
#44994=LINE ( 'NONE', #1514, #33849 ) ;
#45005=DIRECTION ( 'NONE',  ( -0.7071067811865348052, 0.7071067811865602293, 0.000000000000000000 ) ) ;
#45009=DIRECTION ( 'NONE',  ( 1.000000000000000000, 0.000000000000000000, 0.000000000000000000 ) ) ;
#45020=ORIENTED_EDGE ( 'NONE', *, *, #54846, .T. ) ;
#45022=EDGE_CURVE ( 'NONE', #52921, #47907, #21878, .T. ) ;
#45027=EDGE_CURVE ( 'NONE', #51768, #23407, #65371, .T. ) ;
#45030=ORIENTED_EDGE ( 'NONE', *, *, #58554, .F. ) ;
#45033=VERTEX_POINT ( 'NONE', #11596 ) ;
#45043=DIRECTION ( 'NONE',  ( 1.836970198721029934E-16, -1.836970198721036344E-16, 1.000000000000000000 ) ) ;
#45054=AXIS2_PLACEMENT_3D ( 'NONE', #47615, #9433, #58584 ) ;
#45057=DIRECTION ( 'NONE',  ( -0.8660254037844375974, 0.5000000000000019984, 1.836970198721037330E-16 ) ) ;
#45061=FACE_OUTER_BOUND ( 'NONE', #28391, .T. ) ;
#45075=DIRECTION ( 'NONE',  ( 9.912705577010312730E-15, 1.000000000000000000, 0.000000000000000000 ) ) ;
#45100=ORIENTED_EDGE ( 'NONE', *, *, #14568, .F. ) ;
#45109=VERTEX_POINT ( 'NONE', #1683 ) ;
#45113=ORIENTED_EDGE ( 'NONE', *, *, #21945, .F. ) ;
#45115=VERTEX_POINT ( 'NONE', #55106 ) ;
#45116=CARTESIAN_POINT ( 'NONE',  ( 9.562023737882766383, 2.530476262117153485, 54.00000000000000711 ) ) ;
#45122=VERTEX_POINT ( 'NONE', #28903 ) ;
#45123=VERTEX_POINT ( 'NONE', #40560 ) ;
#45127=VECTOR ( 'NONE', #6517, 1000.000000000000000 ) ;
#45130=CARTESIAN_POINT ( 'NONE',  ( -3.142976262117267883, -4.046023737882828542, 54.00000000000000711 ) ) ;
#45141=CARTESIAN_POINT ( 'NONE',  ( 10.31452373788281562, -3.857023737882824932, 54.00000000000000711 ) ) ;
#45145=ORIENTED_EDGE ( 'NONE', *, *, #53912, .F. ) ;
#45146=CARTESIAN_POINT ( 'NONE',  ( -4.141586236041100655, 4.706725378239165813, 26.00000000000000711 ) ) ;
#45160=CARTESIAN_POINT ( 'NONE',  ( -9.722976262117258628, 3.667976262117184749, 26.00000000000000711 ) ) ;
#45166=VERTEX_POINT ( 'NONE', #61071 ) ;
#45177=EDGE_LOOP ( 'NONE', ( #30282, #2517, #23018, #44260 ) ) ;
#45178=VERTEX_POINT ( 'NONE', #1351 ) ;
#45181=DIRECTION ( 'NONE',  ( -0.8660254037844510311, -0.4999999999999785727, 0.000000000000000000 ) ) ;
#45182=VECTOR ( 'NONE', #44379, 1000.000000000000114 ) ;
#45192=PLANE ( 'NONE',  #36477 ) ;
#45202=EDGE_CURVE ( 'NONE', #59591, #7598, #46559, .T. ) ;
#45215=CARTESIAN_POINT ( 'NONE',  ( 9.737023737882816832, -6.832023737882823688, 54.00000000000000711 ) ) ;
#45225=LINE ( 'NONE', #66795, #17181 ) ;
#45231=CARTESIAN_POINT ( 'NONE',  ( 5.257023737882795977, 5.242976262117205799, 26.00000000000000711 ) ) ;
#45239=CIRCLE ( 'NONE', #55459, 0.1749999999999998224 ) ;
#45241=ORIENTED_EDGE ( 'NONE', *, *, #59327, .T. ) ;
#45242=CARTESIAN_POINT ( 'NONE',  ( -2.989207322240233555, -6.872275254348434892, 54.00000000000000711 ) ) ;
#45243=CARTESIAN_POINT ( 'NONE',  ( 7.408280051175138325, 3.710438382363051790, 54.00000000000000711 ) ) ;
#45244=ORIENTED_EDGE ( 'NONE', *, *, #62391, .T. ) ;
#45249=FACE_BOUND ( 'NONE', #63740, .T. ) ;
#45252=AXIS2_PLACEMENT_3D ( 'NONE', #51361, #29100, #45005 ) ;
#45258=ORIENTED_EDGE ( 'NONE', *, *, #44317, .F. ) ;
#45259=CARTESIAN_POINT ( 'NONE',  ( 6.501044194225450212, 3.142976262117187058, 54.00000000000000711 ) ) ;
#45261=EDGE_CURVE ( 'NONE', #39983, #65543, #13691, .T. ) ;
#45276=ORIENTED_EDGE ( 'NONE', *, *, #51806, .T. ) ;
#45278=EDGE_LOOP ( 'NONE', ( #29130, #10812, #19179, #18039 ) ) ;
#45281=EDGE_CURVE ( 'NONE', #38702, #7725, #52225, .T. ) ;
#45290=LINE ( 'NONE', #44595, #18458 ) ;
#45300=CARTESIAN_POINT ( 'NONE',  ( 3.677663764522608680, 6.350872789121272177, 54.00000000000000711 ) ) ;
#45308=CARTESIAN_POINT ( 'NONE',  ( 9.737023737882815055, -2.544523737882825820, 54.00000000000000711 ) ) ;
#45310=LINE ( 'NONE', #39328, #57176 ) ;
#45333=DIRECTION ( 'NONE',  ( -9.799566706031580591E-15, -1.000000000000000000, 0.000000000000000000 ) ) ;
#45335=CARTESIAN_POINT ( 'NONE',  ( 5.257023737882798642, 6.467976262117199227, 54.00000000000000711 ) ) ;
#45336=ORIENTED_EDGE ( 'NONE', *, *, #64367, .F. ) ;
#45341=DIRECTION ( 'NONE',  ( 1.836970198721029934E-16, 1.836970198721010706E-16, -1.000000000000000000 ) ) ;
#45342=ORIENTED_EDGE ( 'NONE', *, *, #60966, .F. ) ;
#45352=CARTESIAN_POINT ( 'NONE',  ( 7.357023737882817827, -6.665817930929303969, 54.00000000000000711 ) ) ;
#45361=LINE ( 'NONE', #24156, #52226 ) ;
#45362=VERTEX_POINT ( 'NONE', #34423 ) ;
#45363=VERTEX_POINT ( 'NONE', #62358 ) ;
#45373=CARTESIAN_POINT ( 'NONE',  ( -5.242976262117259978, 5.242976262117182706, 54.00000000000000711 ) ) ;
#45374=VECTOR ( 'NONE', #19932, 1000.000000000000000 ) ;
#45380=VERTEX_POINT ( 'NONE', #1928 ) ;
#45383=EDGE_LOOP ( 'NONE', ( #8561, #5272, #64543, #61760 ) ) ;
#45385=CIRCLE ( 'NONE', #12666, 1.224999999999997868 ) ;
#45386=CARTESIAN_POINT ( 'NONE',  ( -8.130476262117259267, 9.547976262117177981, 26.00000000000000711 ) ) ;
#45391=CARTESIAN_POINT ( 'NONE',  ( -5.779227145995322168, -6.358413763958943754, 26.00000000000000711 ) ) ;
#45402=FACE_BOUND ( 'NONE', #31487, .T. ) ;
#45406=CYLINDRICAL_SURFACE ( 'NONE', #25585, 0.1749999999999998224 ) ;
#45407=VERTEX_POINT ( 'NONE', #12519 ) ;
#45413=ADVANCED_FACE ( 'NONE', ( #18521 ), #56712, .F. ) ;
#45415=PLANE ( 'NONE',  #69698 ) ;
#45417=EDGE_CURVE ( 'NONE', #62878, #39983, #11999, .T. ) ;
#45419=LINE ( 'NONE', #17165, #36773 ) ;
#45424=CARTESIAN_POINT ( 'NONE',  ( -9.547976262117222390, -2.544523737882724124, 26.00000000000000711 ) ) ;
#45425=FACE_OUTER_BOUND ( 'NONE', #12762, .T. ) ;
#45427=VERTEX_POINT ( 'NONE', #13578 ) ;
#45433=LINE ( 'NONE', #18566, #5765 ) ;
#45463=ORIENTED_EDGE ( 'NONE', *, *, #50142, .F. ) ;
#45476=AXIS2_PLACEMENT_3D ( 'NONE', #24699, #23034, #65494 ) ;
#45493=ORIENTED_EDGE ( 'NONE', *, *, #29625, .F. ) ;
#45498=LINE ( 'NONE', #18276, #10841 ) ;
#45512=CARTESIAN_POINT ( 'NONE',  ( -8.566576262117349572, -8.930623737882770641, 54.00000000000000711 ) ) ;
#45513=DIRECTION ( 'NONE',  ( 1.000000000000000000, 0.000000000000000000, 0.000000000000000000 ) ) ;
#45514=AXIS2_PLACEMENT_3D ( 'NONE', #58918, #15439, #64232 ) ;
#45516=ORIENTED_EDGE ( 'NONE', *, *, #60394, .F. ) ;
#45518=ORIENTED_EDGE ( 'NONE', *, *, #55458, .T. ) ;
#45519=CARTESIAN_POINT ( 'NONE',  ( 9.912023737882783792, 3.842976262117149044, 54.00000000000000711 ) ) ;
#45528=VECTOR ( 'NONE', #21873, 1000.000000000000114 ) ;
#45529=DIRECTION ( 'NONE',  ( 1.000000000000000000, 0.000000000000000000, 0.000000000000000000 ) ) ;
#45534=DIRECTION ( 'NONE',  ( -1.000000000000000000, 1.813998472013049822E-14, -1.836970198720996654E-16 ) ) ;
#45536=VECTOR ( 'NONE', #58513, 1000.000000000000000 ) ;
#45549=ORIENTED_EDGE ( 'NONE', *, *, #33423, .F. ) ;
#45557=CARTESIAN_POINT ( 'NONE',  ( 3.857023737882817827, 10.30047626211720413, 54.00000000000000711 ) ) ;
#45565=LINE ( 'NONE', #18698, #13645 ) ;
#45567=CARTESIAN_POINT ( 'NONE',  ( 6.836383711242997485, 6.350872789121265960, 26.00000000000000711 ) ) ;
#45571=CARTESIAN_POINT ( 'NONE',  ( 6.501044194225490180, -2.632023737882815517, 26.00000000000000711 ) ) ;
#45572=VERTEX_POINT ( 'NONE', #63777 ) ;
#45575=DIRECTION ( 'NONE',  ( 1.203165845134433084E-14, 1.000000000000000000, 0.000000000000000000 ) ) ;
#45582=EDGE_CURVE ( 'NONE', #43101, #55737, #59476, .T. ) ;
#45584=CARTESIAN_POINT ( 'NONE',  ( -4.706725378239251967, -4.155633711806651753, 54.00000000000000711 ) ) ;
#45585=VERTEX_POINT ( 'NONE', #41504 ) ;
#45592=DIRECTION ( 'NONE',  ( -0.000000000000000000, -0.000000000000000000, -1.000000000000000000 ) ) ;
#45611=CARTESIAN_POINT ( 'NONE',  ( 10.31452373788280674, 6.835476262117182067, 54.00000000000000711 ) ) ;
#45615=DIRECTION ( 'NONE',  ( 1.349135440953254805E-14, 1.000000000000000000, 1.836970198721035604E-16 ) ) ;
#45618=CARTESIAN_POINT ( 'NONE',  ( 3.848229544836323512, -7.357023737882803616, 26.00000000000000000 ) ) ;
#45619=CARTESIAN_POINT ( 'NONE',  ( -8.130476262117319664, -9.562023737882764607, 26.00000000000000000 ) ) ;
#45621=ORIENTED_EDGE ( 'NONE', *, *, #11771, .T. ) ;
#45622=AXIS2_PLACEMENT_3D ( 'NONE', #6085, #48876, #27997 ) ;
#45632=LINE ( 'NONE', #34319, #61439 ) ;
#45644=EDGE_CURVE ( 'NONE', #961, #35523, #50978, .T. ) ;
#45648=VECTOR ( 'NONE', #68003, 1000.000000000000114 ) ;
#45657=AXIS2_PLACEMENT_3D ( 'NONE', #1115, #44565, #22344 ) ;
#45659=CARTESIAN_POINT ( 'NONE',  ( -4.135079735113210475, -6.836383711242997485, 26.00000000000000711 ) ) ;
#45668=DIRECTION ( 'NONE',  ( 1.000000000000000000, 0.000000000000000000, 0.000000000000000000 ) ) ;
#45670=DIRECTION ( 'NONE',  ( -1.836970198721029934E-16, 1.836970198721036590E-16, -1.000000000000000000 ) ) ;
#45678=ORIENTED_EDGE ( 'NONE', *, *, #46433, .F. ) ;
#45684=EDGE_CURVE ( 'NONE', #47684, #26595, #46367, .T. ) ;
#45686=VERTEX_POINT ( 'NONE', #19148 ) ;
#45688=ORIENTED_EDGE ( 'NONE', *, *, #37024, .T. ) ;
#45692=CARTESIAN_POINT ( 'NONE',  ( -6.642976262117260333, 9.897976262117179402, 54.00000000000000711 ) ) ;
#45702=EDGE_LOOP ( 'NONE', ( #4981, #22745, #42982, #23808 ) ) ;
#45723=VERTEX_POINT ( 'NONE', #18433 ) ;
#45734=EDGE_CURVE ( 'NONE', #58511, #45115, #28966, .T. ) ;
#45735=CARTESIAN_POINT ( 'NONE',  ( -9.390476262117203987, -1.480523737882726731, 26.00000000000000711 ) ) ;
#45743=ORIENTED_EDGE ( 'NONE', *, *, #68169, .T. ) ;
#45749=EDGE_CURVE ( 'NONE', #5714, #24664, #41761, .T. ) ;
#45752=CARTESIAN_POINT ( 'NONE',  ( 10.31452373788281562, -3.664523737882826815, 54.00000000000000711 ) ) ;
#45764=CYLINDRICAL_SURFACE ( 'NONE', #65228, 0.3499999999999996447 ) ;
#45767=AXIS2_PLACEMENT_3D ( 'NONE', #66247, #6836, #28405 ) ;
#45769=DIRECTION ( 'NONE',  ( -1.280238727658158432E-15, -1.000000000000000000, 0.000000000000000000 ) ) ;
#45778=DIRECTION ( 'NONE',  ( -1.000000000000000000, 0.000000000000000000, 0.000000000000000000 ) ) ;
#45780=CARTESIAN_POINT ( 'NONE',  ( -9.390476262117259054, 1.466476262117183627, 54.00000000000000711 ) ) ;
#45786=CARTESIAN_POINT ( 'NONE',  ( -5.779227145995281312, -4.155633711806634878, 26.00000000000000711 ) ) ;
#45791=ORIENTED_EDGE ( 'NONE', *, *, #55799, .T. ) ;
#45794=DIRECTION ( 'NONE',  ( -1.836970198721029934E-16, 1.836970198721036590E-16, -1.000000000000000000 ) ) ;
#45799=VECTOR ( 'NONE', #56150, 1000.000000000000114 ) ;
#45802=DIRECTION ( 'NONE',  ( -1.000000000000000000, 3.491481338843133355E-15, 1.836970198721036590E-16 ) ) ;
#45809=LINE ( 'NONE', #67394, #51734 ) ;
#45812=CIRCLE ( 'NONE', #69552, 0.1749999999999998224 ) ;
#45817=CARTESIAN_POINT ( 'NONE',  ( -8.130476262117259267, 8.821682069070703847, 54.00000000000000711 ) ) ;
#45822=ORIENTED_EDGE ( 'NONE', *, *, #49222, .F. ) ;
#45832=VERTEX_POINT ( 'NONE', #31530 ) ;
#45833=VECTOR ( 'NONE', #59349, 1000.000000000000114 ) ;
#45843=ORIENTED_EDGE ( 'NONE', *, *, #16883, .F. ) ;
#45846=LINE ( 'NONE', #18620, #5325 ) ;
#45847=DIRECTION ( 'NONE',  ( 1.836970198721029934E-16, 1.836970198721010706E-16, -1.000000000000000000 ) ) ;
#45849=CARTESIAN_POINT ( 'NONE',  ( 8.144523737882815695, 9.547976262117185087, 54.00000000000000711 ) ) ;
#45862=AXIS2_PLACEMENT_3D ( 'NONE', #18799, #1843, #23420 ) ;
#45873=CARTESIAN_POINT ( 'NONE',  ( 7.357023737882817827, -4.961189459950063885, 54.00000000000000711 ) ) ;
#45876=CARTESIAN_POINT ( 'NONE',  ( -6.835476262117330393, -10.50702373788278265, 26.00000000000000000 ) ) ;
#45881=ORIENTED_EDGE ( 'NONE', *, *, #43939, .F. ) ;
#45885=ORIENTED_EDGE ( 'NONE', *, *, #53323, .T. ) ;
#45886=ORIENTED_EDGE ( 'NONE', *, *, #49358, .T. ) ;
#45891=DIRECTION ( 'NONE',  ( -1.000000000000000000, 0.000000000000000000, 0.000000000000000000 ) ) ;
#45909=EDGE_CURVE ( 'NONE', #62934, #63019, #39169, .T. ) ;
#45911=DIRECTION ( 'NONE',  ( 0.000000000000000000, 0.000000000000000000, 1.000000000000000000 ) ) ;
#45916=ADVANCED_FACE ( 'NONE', ( #22303 ), #6710, .F. ) ;
#45918=AXIS2_PLACEMENT_3D ( 'NONE', #22775, #53934, #32355 ) ;
#45929=CARTESIAN_POINT ( 'NONE',  ( 6.501044194225490180, -2.632023737882825287, 54.00000000000000711 ) ) ;
#45930=EDGE_LOOP ( 'NONE', ( #34653, #51254, #13043, #63590 ) ) ;
#45948=ORIENTED_EDGE ( 'NONE', *, *, #69535, .T. ) ;
#45959=EDGE_CURVE ( 'NONE', #47586, #61728, #38893, .T. ) ;
#45963=VECTOR ( 'NONE', #53693, 1000.000000000000000 ) ;
#45964=DIRECTION ( 'NONE',  ( -1.000000000000000000, 0.000000000000000000, 0.000000000000000000 ) ) ;
#45965=DIRECTION ( 'NONE',  ( -1.836970198721029934E-16, 1.836970198721036590E-16, -1.000000000000000000 ) ) ;
#45967=AXIS2_PLACEMENT_3D ( 'NONE', #28780, #45043, #12517 ) ;
#45970=CARTESIAN_POINT ( 'NONE',  ( 6.849523737882817542, -10.50702373788282529, 54.00000000000000711 ) ) ;
#45981=VERTEX_POINT ( 'NONE', #65433 ) ;
#45984=LINE ( 'NONE', #8135, #60839 ) ;
#45987=CARTESIAN_POINT ( 'NONE',  ( -8.598420958951637161, -2.005523737882740409, 26.00000000000000711 ) ) ;
#46007=VERTEX_POINT ( 'NONE', #22639 ) ;
#46010=VECTOR ( 'NONE', #13498, 1000.000000000000000 ) ;
#46016=CARTESIAN_POINT ( 'NONE',  ( 10.50702373788280752, 6.835476262117182067, 54.00000000000000711 ) ) ;
#46021=VERTEX_POINT ( 'NONE', #35668 ) ;
#46026=DIRECTION ( 'NONE',  ( -1.000000000000000000, 0.000000000000000000, 0.000000000000000000 ) ) ;
#46042=ORIENTED_EDGE ( 'NONE', *, *, #54380, .F. ) ;
#46047=CARTESIAN_POINT ( 'NONE',  ( 6.501044194225490180, -3.157023737882824754, 54.00000000000000711 ) ) ;
#46048=CARTESIAN_POINT ( 'NONE',  ( 5.793274621760835963, 6.344366288193353576, 26.00000000000000711 ) ) ;
#46049=ORIENTED_EDGE ( 'NONE', *, *, #48994, .T. ) ;
#46060=ORIENTED_EDGE ( 'NONE', *, *, #46818, .T. ) ;
#46064=ORIENTED_EDGE ( 'NONE', *, *, #67241, .F. ) ;
#46068=DIRECTION ( 'NONE',  ( 1.836970198721029934E-16, -1.836970198721036344E-16, 1.000000000000000000 ) ) ;
#46070=CIRCLE ( 'NONE', #55119, 0.1749999999999980738 ) ;
#46071=AXIS2_PLACEMENT_3D ( 'NONE', #10095, #41909, #37662 ) ;
#46072=CARTESIAN_POINT ( 'NONE',  ( -7.517976262117260333, 3.834182069070703580, 54.00000000000000711 ) ) ;
#46084=EDGE_CURVE ( 'NONE', #48981, #29034, #66796, .T. ) ;
#46086=VERTEX_POINT ( 'NONE', #13051 ) ;
#46087=ADVANCED_FACE ( 'NONE', ( #19411 ), #18349, .F. ) ;
#46091=ADVANCED_FACE ( 'NONE', ( #46283 ), #67153, .F. ) ;
#46093=LINE ( 'NONE', #67660, #7337 ) ;
#46102=EDGE_CURVE ( 'NONE', #55318, #61234, #61483, .T. ) ;
#46109=ORIENTED_EDGE ( 'NONE', *, *, #11141, .T. ) ;
#46113=ORIENTED_EDGE ( 'NONE', *, *, #1028, .F. ) ;
#46114=CARTESIAN_POINT ( 'NONE',  ( 7.969523737882818537, -9.562023737882809016, 26.00000000000000000 ) ) ;
#46122=AXIS2_PLACEMENT_3D ( 'NONE', #34094, #29496, #50370 ) ;
#46123=CARTESIAN_POINT ( 'NONE',  ( -8.916576262117345664, -8.580623737882765667, 54.00000000000000711 ) ) ;
#46125=CARTESIAN_POINT ( 'NONE',  ( 6.657023737882816761, 9.897976262117193613, 54.00000000000000711 ) ) ;
#46130=DIRECTION ( 'NONE',  ( 5.120954910632640039E-15, 1.000000000000000000, -0.000000000000000000 ) ) ;
#46145=CARTESIAN_POINT ( 'NONE',  ( -9.897976262117257562, 6.817976262117182884, 26.00000000000000711 ) ) ;
#46146=CARTESIAN_POINT ( 'NONE',  ( -3.834182069070823040, -7.357023737882818715, 54.00000000000000711 ) ) ;
#46153=EDGE_CURVE ( 'NONE', #42109, #23844, #55850, .T. ) ;
#46161=EDGE_CURVE ( 'NONE', #54627, #22368, #15532, .T. ) ;
#46169=EDGE_LOOP ( 'NONE', ( #47992, #55584, #47634, #5315 ) ) ;
#46170=VECTOR ( 'NONE', #35694, 1000.000000000000000 ) ;
#46189=DIRECTION ( 'NONE',  ( 4.121462285523434951E-16, 1.000000000000000000, 3.673940397442059868E-16 ) ) ;
#46197=LINE ( 'NONE', #62820, #26803 ) ;
#46205=EDGE_CURVE ( 'NONE', #51302, #59628, #52665, .T. ) ;
#46216=CARTESIAN_POINT ( 'NONE',  ( -8.079219948824961861, -8.711985858128649340, 54.00000000000000711 ) ) ;
#46219=LINE ( 'NONE', #14041, #47442 ) ;
#46236=ORIENTED_EDGE ( 'NONE', *, *, #36628, .T. ) ;
#46239=EDGE_LOOP ( 'NONE', ( #31696, #12500, #43068, #1539 ) ) ;
#46245=ORIENTED_EDGE ( 'NONE', *, *, #23325, .F. ) ;
#46254=LINE ( 'NONE', #62503, #6253 ) ;
#46256=AXIS2_PLACEMENT_3D ( 'NONE', #39117, #2674, #29894 ) ;
#46258=ORIENTED_EDGE ( 'NONE', *, *, #37009, .T. ) ;
#46261=DIRECTION ( 'NONE',  ( 3.540251991789405856E-15, 1.000000000000000000, 0.000000000000000000 ) ) ;
#46262=ORIENTED_EDGE ( 'NONE', *, *, #67515, .T. ) ;
#46270=CARTESIAN_POINT ( 'NONE',  ( -8.566576262117358453, -9.703773737882738004, 54.00000000000000711 ) ) ;
#46274=CARTESIAN_POINT ( 'NONE',  ( -8.916576262117258622, 10.03972626211718477, 26.00000000000000711 ) ) ;
#46275=DIRECTION ( 'NONE',  ( 0.000000000000000000, 1.000000000000000000, 0.000000000000000000 ) ) ;
#46279=ORIENTED_EDGE ( 'NONE', *, *, #23521, .F. ) ;
#46281=VECTOR ( 'NONE', #16382, 1000.000000000000000 ) ;
#46283=FACE_OUTER_BOUND ( 'NONE', #59024, .T. ) ;
#46284=DIRECTION ( 'NONE',  ( 1.819560449471430698E-15, 1.000000000000000000, 1.836970198721032892E-16 ) ) ;
#46293=DIRECTION ( 'NONE',  ( 1.000000000000000000, 0.000000000000000000, 0.000000000000000000 ) ) ;
#46304=DIRECTION ( 'NONE',  ( 1.000000000000000000, -7.808916176531286882E-15, -2.868949260119708725E-30 ) ) ;
#46311=ORIENTED_EDGE ( 'NONE', *, *, #60597, .F. ) ;
#46312=DIRECTION ( 'NONE',  ( 1.836970198721029934E-16, 1.836970198721010706E-16, -1.000000000000000000 ) ) ;
#46314=VERTEX_POINT ( 'NONE', #37781 ) ;
#46320=DIRECTION ( 'NONE',  ( 0.000000000000000000, -1.000000000000000000, 0.000000000000000000 ) ) ;
#46322=ORIENTED_EDGE ( 'NONE', *, *, #16939, .T. ) ;
#46323=CARTESIAN_POINT ( 'NONE',  ( 8.580623737882818958, -9.703773737882825046, 54.00000000000000711 ) ) ;
#46333=AXIS2_PLACEMENT_3D ( 'NONE', #42473, #58033, #31877 ) ;
#46335=DIRECTION ( 'NONE',  ( 9.912705577010336396E-15, 1.000000000000000000, 0.000000000000000000 ) ) ;
#46340=VERTEX_POINT ( 'NONE', #17235 ) ;
#46343=ADVANCED_FACE ( 'NONE', ( #22216 ), #38140, .F. ) ;
#46344=CARTESIAN_POINT ( 'NONE',  ( 6.836383711243005479, -4.149127210878743810, 54.00000000000000711 ) ) ;
#46346=ORIENTED_EDGE ( 'NONE', *, *, #46390, .F. ) ;
#46364=CARTESIAN_POINT ( 'NONE',  ( -2.355476262117320640, -9.562023737882825003, 26.00000000000000711 ) ) ;
#46365=LINE ( 'NONE', #64635, #16603 ) ;
#46367=LINE ( 'NONE', #41061, #27872 ) ;
#46369=VECTOR ( 'NONE', #52875, 1000.000000000000000 ) ;
#46375=DIRECTION ( 'NONE',  ( 0.000000000000000000, -3.673940397442059868E-16, 1.000000000000000000 ) ) ;
#46384=DIRECTION ( 'NONE',  ( 0.000000000000000000, -1.000000000000000000, -3.673940397442059868E-16 ) ) ;
#46387=ORIENTED_EDGE ( 'NONE', *, *, #48964, .F. ) ;
#46390=EDGE_CURVE ( 'NONE', #10200, #37820, #10906, .T. ) ;
#46391=LINE ( 'NONE', #53125, #30795 ) ;
#46406=CARTESIAN_POINT ( 'NONE',  ( 5.257023737882819070, -5.257023737882815517, 26.00000000000000711 ) ) ;
#46413=CARTESIAN_POINT ( 'NONE',  ( 6.364920264886851697, 3.663616288756991413, 54.00000000000000711 ) ) ;
#46419=ORIENTED_EDGE ( 'NONE', *, *, #60240, .T. ) ;
#46425=VECTOR ( 'NONE', #35799, 1000.000000000000000 ) ;
#46433=EDGE_CURVE ( 'NONE', #23129, #55364, #43778, .T. ) ;
#46434=AXIS2_PLACEMENT_3D ( 'NONE', #59183, #142, #48576 ) ;
#46451=VERTEX_POINT ( 'NONE', #2708 ) ;
#46453=CARTESIAN_POINT ( 'NONE',  ( 6.501044194225438666, 2.617976262117192032, 26.00000000000000711 ) ) ;
#46460=FACE_OUTER_BOUND ( 'NONE', #18769, .T. ) ;
#46462=FACE_OUTER_BOUND ( 'NONE', #62235, .T. ) ;
#46464=DIRECTION ( 'NONE',  ( -0.7071067811865451302, 0.7071067811865500152, 2.597868168706484541E-16 ) ) ;
#46469=VERTEX_POINT ( 'NONE', #51152 ) ;
#46470=FACE_OUTER_BOUND ( 'NONE', #21021, .T. ) ;
#46475=ORIENTED_EDGE ( 'NONE', *, *, #33309, .T. ) ;
#46476=CARTESIAN_POINT ( 'NONE',  ( -3.142976262117267883, -4.046023737882828542, 54.00000000000000711 ) ) ;
#46477=LINE ( 'NONE', #4063, #61425 ) ;
#46481=CARTESIAN_POINT ( 'NONE',  ( 0.9555237378828128625, 9.915476262117220330, 26.00000000000000711 ) ) ;
#46490=ORIENTED_EDGE ( 'NONE', *, *, #27397, .F. ) ;
#46493=ADVANCED_FACE ( 'NONE', ( #55765 ), #18266, .F. ) ;
#46496=CARTESIAN_POINT ( 'NONE',  ( 7.532023737882817649, -3.848229544836346605, 54.00000000000000711 ) ) ;
#46504=DIRECTION ( 'NONE',  ( -1.185108578570163560E-14, -1.000000000000000000, -1.836970198721014650E-16 ) ) ;
#46509=FACE_OUTER_BOUND ( 'NONE', #24216, .T. ) ;
#46520=CARTESIAN_POINT ( 'NONE',  ( -8.821682069070829968, -8.144523737882765957, 54.00000000000000711 ) ) ;
#46521=ORIENTED_EDGE ( 'NONE', *, *, #69316, .F. ) ;
#46528=EDGE_CURVE ( 'NONE', #32475, #31391, #39266, .T. ) ;
#46537=ORIENTED_EDGE ( 'NONE', *, *, #56486, .T. ) ;
#46544=CARTESIAN_POINT ( 'NONE',  ( 6.836383711243005479, -4.149127210878734040, 26.00000000000000711 ) ) ;
#46546=PLANE ( 'NONE',  #65215 ) ;
#46559=LINE ( 'NONE', #9445, #6373 ) ;
#46560=AXIS2_PLACEMENT_3D ( 'NONE', #43295, #59568, #59218 ) ;
#46561=DIRECTION ( 'NONE',  ( -1.836970198721029934E-16, 1.836970198721036590E-16, -1.000000000000000000 ) ) ;
#46566=ORIENTED_EDGE ( 'NONE', *, *, #66489, .T. ) ;
#46568=CARTESIAN_POINT ( 'NONE',  ( 6.665817930929297752, -7.357023737882824044, 54.00000000000000711 ) ) ;
#46573=ORIENTED_EDGE ( 'NONE', *, *, #45281, .T. ) ;
#46576=AXIS2_PLACEMENT_3D ( 'NONE', #7157, #55958, #51345 ) ;
#46582=PLANE ( 'NONE',  #38512 ) ;
#46587=FACE_OUTER_BOUND ( 'NONE', #54386, .T. ) ;
#46591=CARTESIAN_POINT ( 'NONE',  ( 4.720772854004780861, 4.141586236041042923, 54.00000000000000711 ) ) ;
#46593=ORIENTED_EDGE ( 'NONE', *, *, #27808, .T. ) ;
#46595=ORIENTED_EDGE ( 'NONE', *, *, #8605, .T. ) ;
#46598=EDGE_CURVE ( 'NONE', #66948, #3798, #67766, .T. ) ;
#46603=EDGE_CURVE ( 'NONE', #45572, #26595, #57855, .T. ) ;
#46612=FACE_OUTER_BOUND ( 'NONE', #5584, .T. ) ;
#46617=CIRCLE ( 'NONE', #64710, 0.1749999999999989342 ) ;
#46618=CARTESIAN_POINT ( 'NONE',  ( -3.650476262117331228, -10.50702373788281641, 26.00000000000000000 ) ) ;
#46621=DIRECTION ( 'NONE',  ( 1.836970198721029934E-16, 1.836970198721010706E-16, -1.000000000000000000 ) ) ;
#46623=CARTESIAN_POINT ( 'NONE',  ( 5.257023737882819070, -5.257023737882815517, 26.00000000000000711 ) ) ;
#46625=EDGE_CURVE ( 'NONE', #14276, #55844, #25707, .T. ) ;
#46630=EDGE_CURVE ( 'NONE', #7067, #56499, #41598, .T. ) ;
#46635=AXIS2_PLACEMENT_3D ( 'NONE', #27779, #53972, #49362 ) ;
#46673=ORIENTED_EDGE ( 'NONE', *, *, #7771, .F. ) ;
#46684=PLANE ( 'NONE',  #52549 ) ;
#46688=DIRECTION ( 'NONE',  ( -0.000000000000000000, 3.673940397442059868E-16, -1.000000000000000000 ) ) ;
#46695=DIRECTION ( 'NONE',  ( 1.000000000000000000, -3.491481338843133355E-15, -1.836970198721036344E-16 ) ) ;
#46710=CARTESIAN_POINT ( 'NONE',  ( 6.501044194225490180, -3.157023737882825198, 54.00000000000000711 ) ) ;
#46714=DIRECTION ( 'NONE',  ( -1.836970198721029934E-16, 1.836970198721036590E-16, -1.000000000000000000 ) ) ;
#46716=DIRECTION ( 'NONE',  ( -1.000000000000000000, 0.000000000000000000, 0.000000000000000000 ) ) ;
#46727=VECTOR ( 'NONE', #34764, 1000.000000000000000 ) ;
#46730=AXIS2_PLACEMENT_3D ( 'NONE', #14816, #31077, #59938 ) ;
#46734=ORIENTED_EDGE ( 'NONE', *, *, #22062, .F. ) ;
#46742=CARTESIAN_POINT ( 'NONE',  ( 3.664523737882778853, -10.50702373788281285, 54.00000000000000711 ) ) ;
#46753=ORIENTED_EDGE ( 'NONE', *, *, #45417, .F. ) ;
#46756=VERTEX_POINT ( 'NONE', #59615 ) ;
#46766=ORIENTED_EDGE ( 'NONE', *, *, #61218, .F. ) ;
#46778=DIRECTION ( 'NONE',  ( 1.000000000000000000, 0.000000000000000000, -0.000000000000000000 ) ) ;
#46789=ADVANCED_FACE ( 'NONE', ( #11159 ), #58917, .F. ) ;
#46792=VERTEX_POINT ( 'NONE', #33078 ) ;
#46807=CARTESIAN_POINT ( 'NONE',  ( 6.364920264886889001, 6.822336235477383326, 54.00000000000000711 ) ) ;
#46816=DIRECTION ( 'NONE',  ( 3.596772705736698833E-15, 1.000000000000000000, 0.000000000000000000 ) ) ;
#46818=EDGE_CURVE ( 'NONE', #46841, #64891, #55129, .T. ) ;
#46826=EDGE_CURVE ( 'NONE', #45033, #20832, #22484, .T. ) ;
#46830=AXIS2_PLACEMENT_3D ( 'NONE', #61428, #40226, #28572 ) ;
#46841=VERTEX_POINT ( 'NONE', #29156 ) ;
#46845=CARTESIAN_POINT ( 'NONE',  ( 0.9555237378827876604, -9.404523737882790613, 54.00000000000000711 ) ) ;
#46847=AXIS2_PLACEMENT_3D ( 'NONE', #2199, #24472, #1497 ) ;
#46851=VERTEX_POINT ( 'NONE', #40102 ) ;
#46854=CARTESIAN_POINT ( 'NONE',  ( -6.835476262117260227, 10.49297626211718359, 26.00000000000000711 ) ) ;
#46855=VECTOR ( 'NONE', #52929, 1000.000000000000114 ) ;
#46858=VERTEX_POINT ( 'NONE', #23853 ) ;
#46868=CARTESIAN_POINT ( 'NONE',  ( 2.005523737882813240, 8.598420958951633608, 54.00000000000000711 ) ) ;
#46888=DIRECTION ( 'NONE',  ( 1.000000000000000000, -7.665540703601096574E-15, -2.816273965919649962E-30 ) ) ;
#46894=LINE ( 'NONE', #41597, #18376 ) ;
#46895=CARTESIAN_POINT ( 'NONE',  ( 3.848229544836329730, 7.342976262117204556, 54.00000000000000711 ) ) ;
#46896=LINE ( 'NONE', #46544, #62469 ) ;
#46903=CARTESIAN_POINT ( 'NONE',  ( -7.342976262117273833, -4.961189459950004377, 54.00000000000000711 ) ) ;
#46906=ORIENTED_EDGE ( 'NONE', *, *, #21981, .F. ) ;
#46909=VECTOR ( 'NONE', #27891, 1000.000000000000000 ) ;
#46914=DIRECTION ( 'NONE',  ( -0.000000000000000000, 3.673940397442059868E-16, -1.000000000000000000 ) ) ;
#46916=CARTESIAN_POINT ( 'NONE',  ( -6.822336235477489019, -6.364920264886855250, 54.00000000000000711 ) ) ;
#46917=LINE ( 'NONE', #20058, #56513 ) ;
#46920=VECTOR ( 'NONE', #13422, 1000.000000000000114 ) ;
#46922=ORIENTED_EDGE ( 'NONE', *, *, #28816, .T. ) ;
#46923=LINE ( 'NONE', #26418, #14621 ) ;
#46932=ORIENTED_EDGE ( 'NONE', *, *, #1527, .F. ) ;
#46934=ADVANCED_FACE ( 'NONE', ( #56037 ), #39414, .F. ) ;
#46935=DIRECTION ( 'NONE',  ( 0.000000000000000000, 1.000000000000000000, 0.000000000000000000 ) ) ;
#46940=ORIENTED_EDGE ( 'NONE', *, *, #25579, .F. ) ;
#46947=LINE ( 'NONE', #37059, #25553 ) ;
#46949=DIRECTION ( 'NONE',  ( -1.047444401652940007E-14, -1.000000000000000000, -1.836970198721029934E-16 ) ) ;
#46952=VERTEX_POINT ( 'NONE', #7587 ) ;
#46958=ADVANCED_FACE ( 'NONE', ( #8280 ), #66983, .F. ) ;
#46962=VERTEX_POINT ( 'NONE', #17505 ) ;
#46971=DIRECTION ( 'NONE',  ( -0.7071067811865441310, 0.7071067811865510144, 0.000000000000000000 ) ) ;
#46974=CYLINDRICAL_SURFACE ( 'NONE', #33980, 0.1749999999999993783 ) ;
#46975=ORIENTED_EDGE ( 'NONE', *, *, #61737, .F. ) ;
#46978=VECTOR ( 'NONE', #20734, 1000.000000000000000 ) ;
#46980=DIRECTION ( 'NONE',  ( -1.836970198721029934E-16, -1.836970198721010706E-16, 1.000000000000000000 ) ) ;
#46988=VECTOR ( 'NONE', #30782, 1000.000000000000000 ) ;
#46996=FACE_OUTER_BOUND ( 'NONE', #40928, .T. ) ;
#47002=EDGE_CURVE ( 'NONE', #36489, #32081, #33764, .T. ) ;
#47006=FACE_OUTER_BOUND ( 'NONE', #36984, .T. ) ;
#47011=DIRECTION ( 'NONE',  ( 0.000000000000000000, 1.000000000000000000, 0.000000000000000000 ) ) ;
#47016=PLANE ( 'NONE',  #31668 ) ;
#47019=VERTEX_POINT ( 'NONE', #20302 ) ;
#47021=VERTEX_POINT ( 'NONE', #31286 ) ;
#47026=AXIS2_PLACEMENT_3D ( 'NONE', #51679, #67935, #36453 ) ;
#47041=ORIENTED_EDGE ( 'NONE', *, *, #69316, .T. ) ;
#47042=EDGE_CURVE ( 'NONE', #20832, #28438, #41520, .T. ) ;
#47045=CARTESIAN_POINT ( 'NONE',  ( 4.720772854004775532, 4.141586236041047364, 26.00000000000000711 ) ) ;
#47053=EDGE_CURVE ( 'NONE', #6044, #64879, #24564, .T. ) ;
#47054=AXIS2_PLACEMENT_3D ( 'NONE', #7039, #23651, #39561 ) ;
#47055=DIRECTION ( 'NONE',  ( -1.836970198721029934E-16, 1.836970198721036590E-16, -1.000000000000000000 ) ) ;
#47062=DIRECTION ( 'NONE',  ( -9.912705577010336396E-15, -1.000000000000000000, 0.000000000000000000 ) ) ;
#47065=VERTEX_POINT ( 'NONE', #46123 ) ;
#47067=EDGE_CURVE ( 'NONE', #23915, #22764, #40818, .T. ) ;
#47076=ORIENTED_EDGE ( 'NONE', *, *, #53075, .F. ) ;
#47077=PLANE ( 'NONE',  #10180 ) ;
#47089=DIRECTION ( 'NONE',  ( 9.912705577010336396E-15, 1.000000000000000000, 0.000000000000000000 ) ) ;
#47102=EDGE_CURVE ( 'NONE', #49409, #43101, #69092, .T. ) ;
#47109=EDGE_LOOP ( 'NONE', ( #49846, #49264, #44245, #27530, #20557, #46673, #19669, #20718, #50888, #54019, #17832, #33015, #45258, #63356, #42545, #58011, #65676, #57593, #34382, #15897, #2736, #23575, #63932, #54574, #29554, #37750, #65401, #36703, #23826, #48866, #5514, #44077, #32376, #4445, #44641, #33833, #589, #21057, #48919, #63844, #59208, #44413, #51452, #55660, #20464, #10207, #24254, #37295, #17951, #15981, #39348, #37785, #49517, #46932, #54519, #20002, #52066, #26242, #38601, #45493, #12164, #38700, #21424, #48976, #50915, #64461, #21918, #37519, #29559, #451, #20238, #4054, #30281, #50054, #39197, #58756, #22541, #22586, #336, #59956, #31512, #54268, #1118, #57634, #56004, #5903, #36330, #29906, #57296, #9057, #20412, #1615, #10252, #30740, #54798, #32882, #23862, #40646, #55177, #63642, #67584, #68184, #55723, #31060, #58016, #44358, #24172, #10254, #38292, #30695, #52681, #67030, #64975, #52126, #2903, #42692, #2928, #13216, #36159, #50173, #57457, #16244, #10352, #5323, #15067, #65022, #13122, #49578, #49573, #4380, #55397, #36180, #51814, #35377, #30078, #57218, #23333, #57182, #29781, #57536, #50604, #16735, #65653, #24640, #38220, #21171, #28072, #46113, #2105, #21211, #28409, #21835, #33668, #46940, #16555, #30588, #33647, #7421, #50913, #21455, #60275, #17378, #65742, #1019, #64274, #58223, #23821, #37188, #52983, #13378, #42812, #7100, #25760, #13753, #57214, #4586, #38371, #45342, #1329, #26554, #45516, #44858, #22067, #11293, #66354, #34509, #52373, #24210, #6123, #19546, #7736, #46311, #17527, #13499, #59494, #59028, #41669, #66859, #67254, #31679, #18883, #38360, #59206, #56574, #5021, #33986, #60947, #41097, #31730, #12414, #45881, #69288, #37908, #25710 ) ) ;
#47115=FACE_OUTER_BOUND ( 'NONE', #1400, .T. ) ;
#47130=EDGE_CURVE ( 'NONE', #47065, #58190, #64843, .T. ) ;
#47146=VECTOR ( 'NONE', #54645, 1000.000000000000000 ) ;
#47147=DIRECTION ( 'NONE',  ( 0.000000000000000000, 0.000000000000000000, 1.000000000000000000 ) ) ;
#47150=VERTEX_POINT ( 'NONE', #6134 ) ;
#47160=EDGE_CURVE ( 'NONE', #40034, #67224, #22048, .T. ) ;
#47169=VERTEX_POINT ( 'NONE', #59537 ) ;
#47179=VECTOR ( 'NONE', #60566, 1000.000000000000000 ) ;
#47182=CARTESIAN_POINT ( 'NONE',  ( 7.357023737882817827, -5.552858015815587578, 54.00000000000000711 ) ) ;
#47192=ORIENTED_EDGE ( 'NONE', *, *, #2679, .T. ) ;
#47195=CARTESIAN_POINT ( 'NONE',  ( 9.912023737882801555, 6.642976262117184838, 54.00000000000000711 ) ) ;
#47197=EDGE_CURVE ( 'NONE', #65847, #24983, #60759, .T. ) ;
#47201=ORIENTED_EDGE ( 'NONE', *, *, #51981, .T. ) ;
#47202=CARTESIAN_POINT ( 'NONE',  ( -9.689726262117330791, -10.05377373788272699, 54.00000000000000711 ) ) ;
#47209=CARTESIAN_POINT ( 'NONE',  ( 4.149127210878726935, -3.677663764522637546, 26.00000000000000711 ) ) ;
#47226=LINE ( 'NONE', #46854, #5004 ) ;
#47252=DIRECTION ( 'NONE',  ( 1.836970198721029934E-16, 1.836970198721010706E-16, -1.000000000000000000 ) ) ;
#47265=CARTESIAN_POINT ( 'NONE',  ( -8.130476262117259267, 9.547976262117177981, 54.00000000000000711 ) ) ;
#47267=DIRECTION ( 'NONE',  ( -1.000000000000000000, 1.610765207321970913E-14, 1.836970198721059516E-16 ) ) ;
#47270=CARTESIAN_POINT ( 'NONE',  ( 10.31452373788279964, 6.642976262117187503, 26.00000000000000711 ) ) ;
#47273=ORIENTED_EDGE ( 'NONE', *, *, #14059, .F. ) ;
#47275=CARTESIAN_POINT ( 'NONE',  ( -7.342976262117277386, -5.552858015815541393, 26.00000000000000711 ) ) ;
#47277=CARTESIAN_POINT ( 'NONE',  ( -10.49297626211725110, -3.664523737882711352, 54.00000000000000711 ) ) ;
#47278=CARTESIAN_POINT ( 'NONE',  ( -4.706725378239216440, 6.344366288193329595, 54.00000000000000711 ) ) ;
#47286=EDGE_CURVE ( 'NONE', #32555, #63705, #50292, .T. ) ;
#47287=DIRECTION ( 'NONE',  ( -1.836970198721029934E-16, 1.836970198721036590E-16, -1.000000000000000000 ) ) ;
#47300=CARTESIAN_POINT ( 'NONE',  ( 6.849523737882817542, -10.50702373788282529, 54.00000000000000711 ) ) ;
#47302=DIRECTION ( 'NONE',  ( -0.000000000000000000, 3.673940397442059868E-16, -1.000000000000000000 ) ) ;
#47303=ORIENTED_EDGE ( 'NONE', *, *, #17026, .T. ) ;
#47308=ORIENTED_EDGE ( 'NONE', *, *, #10460, .T. ) ;
#47309=ORIENTED_EDGE ( 'NONE', *, *, #11395, .T. ) ;
#47315=PLANE ( 'NONE',  #33369 ) ;
#47319=EDGE_CURVE ( 'NONE', #2487, #61865, #34723, .T. ) ;
#47326=DIRECTION ( 'NONE',  ( 1.836970198721029934E-16, -1.836970198721036344E-16, 1.000000000000000000 ) ) ;
#47335=ORIENTED_EDGE ( 'NONE', *, *, #7685, .T. ) ;
#47336=LINE ( 'NONE', #63255, #39950 ) ;
#47344=CARTESIAN_POINT ( 'NONE',  ( 9.703773737882817940, 10.03972626211715280, 54.00000000000000711 ) ) ;
#47352=CIRCLE ( 'NONE', #54134, 1.224999999999999423 ) ;
#47360=CARTESIAN_POINT ( 'NONE',  ( 9.912023737882815766, -3.857023737882825820, 54.00000000000000711 ) ) ;
#47376=EDGE_CURVE ( 'NONE', #6322, #14837, #49607, .T. ) ;
#47379=VECTOR ( 'NONE', #47287, 1000.000000000000000 ) ;
#47387=VERTEX_POINT ( 'NONE', #63982 ) ;
#47399=DIRECTION ( 'NONE',  ( 1.000000000000000000, 0.000000000000000000, 0.000000000000000000 ) ) ;
#47406=EDGE_LOOP ( 'NONE', ( #3583, #34050, #5125, #46049 ) ) ;
#47407=DIRECTION ( 'NONE',  ( 1.836970198721029934E-16, -1.836970198721036344E-16, 1.000000000000000000 ) ) ;
#47412=CARTESIAN_POINT ( 'NONE',  ( -2.355476262117234931, 8.821682069070680754, 54.00000000000000711 ) ) ;
#47418=DIRECTION ( 'NONE',  ( -1.000000000000000000, 0.000000000000000000, 0.000000000000000000 ) ) ;
#47428=CARTESIAN_POINT ( 'NONE',  ( 3.848229544836323512, -7.357023737882811609, 54.00000000000000711 ) ) ;
#47442=VECTOR ( 'NONE', #35600, 1000.000000000000000 ) ;
#47446=DIRECTION ( 'NONE',  ( -0.000000000000000000, 3.673940397442059868E-16, -1.000000000000000000 ) ) ;
#47451=ORIENTED_EDGE ( 'NONE', *, *, #37499, .T. ) ;
#47452=CARTESIAN_POINT ( 'NONE',  ( -9.897976262117291313, -6.657023737882756365, 54.00000000000000711 ) ) ;
#47458=CARTESIAN_POINT ( 'NONE',  ( 1.480523737882794233, -8.612468434717218457, 54.00000000000000711 ) ) ;
#47469=CARTESIAN_POINT ( 'NONE',  ( -10.30047626211725742, 6.642976262117184838, 54.00000000000000711 ) ) ;
#47501=EDGE_CURVE ( 'NONE', #53417, #27421, #10224, .T. ) ;
#47516=VERTEX_POINT ( 'NONE', #53025 ) ;
#47519=CARTESIAN_POINT ( 'NONE',  ( -8.227189898828745740, 1.620245201994245487, 26.00000000000000711 ) ) ;
#47521=EDGE_CURVE ( 'NONE', #29373, #58489, #69967, .T. ) ;
#47526=EDGE_CURVE ( 'NONE', #28620, #19158, #16579, .T. ) ;
#47532=DIRECTION ( 'NONE',  ( 0.5000000000000111022, 0.8660254037844322683, 2.509347957447867451E-16 ) ) ;
#47534=AXIS2_PLACEMENT_3D ( 'NONE', #58392, #59072, #53091 ) ;
#47548=CIRCLE ( 'NONE', #67882, 0.3499999999999996447 ) ;
#47558=CARTESIAN_POINT ( 'NONE',  ( -6.835476262117260227, 10.30047626211718104, 54.00000000000000711 ) ) ;
#47581=EDGE_CURVE ( 'NONE', #27421, #23856, #65362, .T. ) ;
#47583=VECTOR ( 'NONE', #19488, 1000.000000000000114 ) ;
#47586=VERTEX_POINT ( 'NONE', #16916 ) ;
#47593=EDGE_CURVE ( 'NONE', #25334, #43217, #22903, .T. ) ;
#47595=VERTEX_POINT ( 'NONE', #59702 ) ;
#47600=ORIENTED_EDGE ( 'NONE', *, *, #32900, .F. ) ;
#47606=EDGE_CURVE ( 'NONE', #67667, #34368, #28544, .T. ) ;
#47615=CARTESIAN_POINT ( 'NONE',  ( -9.897976262117293089, -6.832023737882757075, 54.00000000000000711 ) ) ;
#47616=CARTESIAN_POINT ( 'NONE',  ( 2.369523737882811787, 9.547976262117209956, 26.00000000000000711 ) ) ;
#47620=DIRECTION ( 'NONE',  ( -1.000000000000000000, 3.491481338843133355E-15, 1.836970198721036344E-16 ) ) ;
#47622=DIRECTION ( 'NONE',  ( 0.7671651518153105309, 0.6414496315691445849, 0.000000000000000000 ) ) ;
#47623=LINE ( 'NONE', #30664, #32144 ) ;
#47624=DIRECTION ( 'NONE',  ( -0.000000000000000000, 3.673940397442059868E-16, -1.000000000000000000 ) ) ;
#47626=VECTOR ( 'NONE', #46714, 1000.000000000000000 ) ;
#47627=EDGE_CURVE ( 'NONE', #29534, #31249, #44455, .T. ) ;
#47629=EDGE_CURVE ( 'NONE', #42154, #39526, #57486, .T. ) ;
#47630=VECTOR ( 'NONE', #25514, 1000.000000000000000 ) ;
#47634=ORIENTED_EDGE ( 'NONE', *, *, #7850, .F. ) ;
#47638=ORIENTED_EDGE ( 'NONE', *, *, #28010, .T. ) ;
#47639=CIRCLE ( 'NONE', #48809, 0.1749999999999993783 ) ;
#47658=ORIENTED_EDGE ( 'NONE', *, *, #3051, .F. ) ;
#47661=DIRECTION ( 'NONE',  ( 0.000000000000000000, 0.000000000000000000, -1.000000000000000000 ) ) ;
#47671=EDGE_CURVE ( 'NONE', #28065, #18663, #51161, .T. ) ;
#47672=ORIENTED_EDGE ( 'NONE', *, *, #46084, .T. ) ;
#47673=CARTESIAN_POINT ( 'NONE',  ( 6.657023737882815873, 10.30047626211719880, 26.00000000000000711 ) ) ;
#47677=EDGE_CURVE ( 'NONE', #10200, #50705, #56811, .T. ) ;
#47681=DIRECTION ( 'NONE',  ( -0.000000000000000000, -0.000000000000000000, -1.000000000000000000 ) ) ;
#47684=VERTEX_POINT ( 'NONE', #29234 ) ;
#47692=CARTESIAN_POINT ( 'NONE',  ( 7.408280051175172076, -3.724485858128701032, 54.00000000000000711 ) ) ;
#47693=DIRECTION ( 'NONE',  ( -1.000000000000000000, 3.491481338843133355E-15, 1.836970198721036344E-16 ) ) ;
#47694=ORIENTED_EDGE ( 'NONE', *, *, #58690, .T. ) ;
#47701=AXIS2_PLACEMENT_3D ( 'NONE', #14412, #51540, #24667 ) ;
#47703=LINE ( 'NONE', #68925, #43157 ) ;
#47731=EDGE_LOOP ( 'NONE', ( #53246, #48937, #21400, #57715 ) ) ;
#47735=EDGE_LOOP ( 'NONE', ( #19980, #58273, #38799, #30113 ) ) ;
#47745=CARTESIAN_POINT ( 'NONE',  ( 7.357023737882806280, 6.651770455163672935, 54.00000000000000711 ) ) ;
#47746=AXIS2_PLACEMENT_3D ( 'NONE', #24935, #57456, #51458 ) ;
#47749=VECTOR ( 'NONE', #30665, 1000.000000000000000 ) ;
#47750=CARTESIAN_POINT ( 'NONE',  ( -5.538810540050064901, -7.357023737882800951, 54.00000000000000711 ) ) ;
#47770=AXIS2_PLACEMENT_3D ( 'NONE', #867, #11778, #17096 ) ;
#47779=CARTESIAN_POINT ( 'NONE',  ( -7.955476262117311848, -8.835729544836290472, 26.00000000000000000 ) ) ;
#47780=VERTEX_POINT ( 'NONE', #34187 ) ;
#47787=CARTESIAN_POINT ( 'NONE',  ( -6.350872789121327244, 3.663616288756986084, 54.00000000000000711 ) ) ;
#47790=DIRECTION ( 'NONE',  ( -1.047444401652940007E-14, -1.000000000000000000, -1.836970198721029934E-16 ) ) ;
#47795=VERTEX_POINT ( 'NONE', #57174 ) ;
#47815=EDGE_CURVE ( 'NONE', #2345, #14406, #19074, .T. ) ;
#47819=VECTOR ( 'NONE', #2737, 1000.000000000000000 ) ;
#47823=EDGE_CURVE ( 'NONE', #29536, #51293, #21096, .T. ) ;
#47839=ORIENTED_EDGE ( 'NONE', *, *, #12949, .T. ) ;
#47842=AXIS2_PLACEMENT_3D ( 'NONE', #65976, #21818, #43377 ) ;
#47851=DIRECTION ( 'NONE',  ( 0.7671651518153065341, 0.6414496315691495809, -0.000000000000000000 ) ) ;
#47854=EDGE_CURVE ( 'NONE', #47684, #58217, #29204, .T. ) ;
#47862=ORIENTED_EDGE ( 'NONE', *, *, #25767, .T. ) ;
#47866=CARTESIAN_POINT ( 'NONE',  ( 9.703773737882814387, 8.916576262117184015, 54.00000000000000711 ) ) ;
#47868=CARTESIAN_POINT ( 'NONE',  ( -6.835476262117327728, -10.31452373788278187, 26.00000000000000000 ) ) ;
#47877=LINE ( 'NONE', #58144, #6099 ) ;
#47880=DIRECTION ( 'NONE',  ( 9.912705577010386883E-15, 1.000000000000000000, 0.000000000000000000 ) ) ;
#47885=AXIS2_PLACEMENT_3D ( 'NONE', #63995, #24746, #35688 ) ;
#47892=ORIENTED_EDGE ( 'NONE', *, *, #34098, .F. ) ;
#47896=CARTESIAN_POINT ( 'NONE',  ( 3.664523737882815269, 10.49297626211721024, 26.00000000000000711 ) ) ;
#47900=VECTOR ( 'NONE', #16256, 1000.000000000000114 ) ;
#47907=VERTEX_POINT ( 'NONE', #30652 ) ;
#47911=FACE_OUTER_BOUND ( 'NONE', #48456, .T. ) ;
#47912=AXIS2_PLACEMENT_3D ( 'NONE', #50460, #57154, #41236 ) ;
#47917=AXIS2_PLACEMENT_3D ( 'NONE', #2845, #18398, #1807 ) ;
#47918=EDGE_CURVE ( 'NONE', #9024, #17119, #5565, .T. ) ;
#47922=ORIENTED_EDGE ( 'NONE', *, *, #54856, .T. ) ;
#47925=ORIENTED_EDGE ( 'NONE', *, *, #22563, .T. ) ;
#47928=UNCERTAINTY_MEASURE_WITH_UNIT (LENGTH_MEASURE( 1.000000000000000082E-05 ), #55997, 'distance_accuracy_value', 'NONE');
#47935=LINE ( 'NONE', #31348, #24523 ) ;
#47945=AXIS2_PLACEMENT_3D ( 'NONE', #63181, #62461, #42311 ) ;
#47958=DIRECTION ( 'NONE',  ( -1.000000000000000000, 1.214636490590110272E-14, -1.836970198721007747E-16 ) ) ;
#47960=LINE ( 'NONE', #16827, #42632 ) ;
#47966=DIRECTION ( 'NONE',  ( 0.000000000000000000, 0.000000000000000000, 1.000000000000000000 ) ) ;
#47988=ADVANCED_FACE ( 'NONE', ( #11167 ), #27439, .F. ) ;
#47992=ORIENTED_EDGE ( 'NONE', *, *, #55882, .T. ) ;
#47996=VERTEX_POINT ( 'NONE', #37709 ) ;
#48005=DIRECTION ( 'NONE',  ( 0.7071067811865500152, 0.7071067811865451302, -4.683861624749757595E-31 ) ) ;
#48010=ORIENTED_EDGE ( 'NONE', *, *, #3969, .T. ) ;
#48017=CARTESIAN_POINT ( 'NONE',  ( -3.663616288757090445, -4.149127210878730487, 54.00000000000000711 ) ) ;
#48030=ADVANCED_FACE ( 'NONE', ( #11506 ), #53979, .F. ) ;
#48037=VECTOR ( 'NONE', #29965, 1000.000000000000000 ) ;
#48040=AXIS2_PLACEMENT_3D ( 'NONE', #66397, #66732, #49098 ) ;
#48041=CARTESIAN_POINT ( 'NONE',  ( 6.665817930929297752, -7.532023737882814096, 26.00000000000000000 ) ) ;
#48043=DIRECTION ( 'NONE',  ( -1.836970198721029934E-16, 1.836970198721036344E-16, -1.000000000000000000 ) ) ;
#48044=CARTESIAN_POINT ( 'NONE',  ( -3.650476262117333892, -10.31452373788281740, 54.00000000000000711 ) ) ;
#48056=PLANE ( 'NONE',  #1704 ) ;
#48057=ORIENTED_EDGE ( 'NONE', *, *, #41602, .F. ) ;
#48058=LINE ( 'NONE', #52682, #16251 ) ;
#48065=CARTESIAN_POINT ( 'NONE',  ( -3.834182069070763976, 7.517976262117170627, 54.00000000000000711 ) ) ;
#48079=DIRECTION ( 'NONE',  ( 1.000000000000000000, -8.728482790395504563E-15, -3.206792553201184024E-30 ) ) ;
#48082=EDGE_CURVE ( 'NONE', #23904, #55686, #34811, .T. ) ;
#48083=ORIENTED_EDGE ( 'NONE', *, *, #35375, .T. ) ;
#48091=EDGE_CURVE ( 'NONE', #17044, #40228, #13604, .T. ) ;
#48092=AXIS2_PLACEMENT_3D ( 'NONE', #48644, #50019, #27425 ) ;
#48095=DIRECTION ( 'NONE',  ( -8.903847840905249551E-15, -1.000000000000000000, -1.836970198721027222E-16 ) ) ;
#48101=VERTEX_POINT ( 'NONE', #40826 ) ;
#48103=DIRECTION ( 'NONE',  ( 1.836970198721029934E-16, 1.836970198721010706E-16, -1.000000000000000000 ) ) ;
#48108=AXIS2_PLACEMENT_3D ( 'NONE', #69161, #26034, #20715 ) ;
#48123=CARTESIAN_POINT ( 'NONE',  ( 6.657023737882818537, -10.31452373788282095, 54.00000000000000711 ) ) ;
#48134=CARTESIAN_POINT ( 'NONE',  ( 5.552858015815581361, -7.357023737882824044, 54.00000000000000711 ) ) ;
#48137=DIRECTION ( 'NONE',  ( -1.836970198721029934E-16, 1.836970198721036590E-16, -1.000000000000000000 ) ) ;
#48150=EDGE_LOOP ( 'NONE', ( #5277, #62519, #1287, #2690, #18147, #10797, #3464, #44540 ) ) ;
#48155=EDGE_CURVE ( 'NONE', #27113, #2487, #56043, .T. ) ;
#48157=VERTEX_POINT ( 'NONE', #29163 ) ;
#48160=ORIENTED_EDGE ( 'NONE', *, *, #24748, .T. ) ;
#48161=DIRECTION ( 'NONE',  ( 1.836970198721029934E-16, 1.836970198721010706E-16, -1.000000000000000000 ) ) ;
#48162=CIRCLE ( 'NONE', #11986, 1.224999999999998757 ) ;
#48165=CIRCLE ( 'NONE', #10850, 0.3499999999999996447 ) ;
#48166=VECTOR ( 'NONE', #29298, 1000.000000000000000 ) ;
#48170=ORIENTED_EDGE ( 'NONE', *, *, #11062, .T. ) ;
#48176=DIRECTION ( 'NONE',  ( -1.836970198721029934E-16, 1.836970198721036590E-16, -1.000000000000000000 ) ) ;
#48177=CARTESIAN_POINT ( 'NONE',  ( 8.093267424590464998, -8.711985858128699078, 54.00000000000000711 ) ) ;
#48178=EDGE_CURVE ( 'NONE', #32858, #43292, #39455, .T. ) ;
#48183=EDGE_LOOP ( 'NONE', ( #53168, #28373, #50687, #3277 ) ) ;
#48190=ADVANCED_FACE ( 'NONE', ( #51081 ), #61685, .F. ) ;
#48193=ORIENTED_EDGE ( 'NONE', *, *, #36935, .F. ) ;
#48199=AXIS2_PLACEMENT_3D ( 'NONE', #19620, #4081, #15030 ) ;
#48200=CARTESIAN_POINT ( 'NONE',  ( 6.657023737882818537, -10.31452373788282095, 54.00000000000000711 ) ) ;
#48203=VECTOR ( 'NONE', #67525, 1000.000000000000000 ) ;
#48216=CARTESIAN_POINT ( 'NONE',  ( 7.969523737882818537, -9.562023737882819674, 54.00000000000000711 ) ) ;
#48220=CARTESIAN_POINT ( 'NONE',  ( -6.817976262117325881, -9.737023737882786634, 54.00000000000000711 ) ) ;
#48228=VECTOR ( 'NONE', #57680, 1000.000000000000000 ) ;
#48238=VERTEX_POINT ( 'NONE', #36944 ) ;
#48252=CARTESIAN_POINT ( 'NONE',  ( -5.538810540050059572, -7.357023737882796510, 26.00000000000000711 ) ) ;
#48262=ORIENTED_EDGE ( 'NONE', *, *, #21341, .T. ) ;
#48280=VERTEX_POINT ( 'NONE', #52495 ) ;
#48283=EDGE_LOOP ( 'NONE', ( #5576, #29101, #18014, #66231 ) ) ;
#48288=ORIENTED_EDGE ( 'NONE', *, *, #69873, .F. ) ;
#48291=CARTESIAN_POINT ( 'NONE',  ( 5.257023737882819070, -5.257023737882825287, 54.00000000000000711 ) ) ;
#48294=CARTESIAN_POINT ( 'NONE',  ( 8.835729544836331328, 8.130476262117188213, 54.00000000000000711 ) ) ;
#48299=DIRECTION ( 'NONE',  ( -1.034072152899300747E-14, -1.000000000000000000, 0.000000000000000000 ) ) ;
#48310=DIRECTION ( 'NONE',  ( -0.000000000000000000, -0.000000000000000000, -1.000000000000000000 ) ) ;
#48315=LINE ( 'NONE', #31712, #17467 ) ;
#48318=ORIENTED_EDGE ( 'NONE', *, *, #53281, .F. ) ;
#48320=EDGE_CURVE ( 'NONE', #43217, #32555, #68854, .T. ) ;
#48325=LINE ( 'NONE', #27792, #27606 ) ;
#48327=ADVANCED_FACE ( 'NONE', ( #24916 ), #35505, .F. ) ;
#48339=DIRECTION ( 'NONE',  ( -9.050731179009442381E-15, -1.000000000000000000, 0.000000000000000000 ) ) ;
#48345=CARTESIAN_POINT ( 'NONE',  ( 8.835729544836288696, 2.355476262117161657, 54.00000000000000711 ) ) ;
#48367=DIRECTION ( 'NONE',  ( 1.000000000000000000, -8.540177112501197482E-15, 0.000000000000000000 ) ) ;
#48374=DIRECTION ( 'NONE',  ( 1.000000000000000000, 0.000000000000000000, 0.000000000000000000 ) ) ;
#48376=ADVANCED_FACE ( 'NONE', ( #65537 ), #58849, .F. ) ;
#48378=DIRECTION ( 'NONE',  ( -0.8660254037844363761, 0.5000000000000038858, -0.000000000000000000 ) ) ;
#48387=LINE ( 'NONE', #26132, #33159 ) ;
#48400=ORIENTED_EDGE ( 'NONE', *, *, #11302, .F. ) ;
#48406=CIRCLE ( 'NONE', #31508, 0.5249999999999994671 ) ;
#48411=VERTEX_POINT ( 'NONE', #53900 ) ;
#48412=DIRECTION ( 'NONE',  ( 1.836970198721029934E-16, 1.836970198721010706E-16, -1.000000000000000000 ) ) ;
#48415=CARTESIAN_POINT ( 'NONE',  ( 4.046023737882819660, -3.157023737882826087, 54.00000000000000711 ) ) ;
#48419=VECTOR ( 'NONE', #17424, 1000.000000000000000 ) ;
#48421=ORIENTED_EDGE ( 'NONE', *, *, #51806, .F. ) ;
#48423=DIRECTION ( 'NONE',  ( 1.000000000000000000, 0.000000000000000000, 0.000000000000000000 ) ) ;
#48427=CARTESIAN_POINT ( 'NONE',  ( 3.677663764522620227, 4.135079735113113664, 54.00000000000000711 ) ) ;
#48431=DIRECTION ( 'NONE',  ( 1.836970198721029934E-16, 1.836970198721010706E-16, -1.000000000000000000 ) ) ;
#48432=ADVANCED_FACE ( 'NONE', ( #21363 ), #11435, .F. ) ;
#48434=ORIENTED_EDGE ( 'NONE', *, *, #50444, .F. ) ;
#48435=EDGE_CURVE ( 'NONE', #54028, #12647, #32666, .T. ) ;
#48439=ORIENTED_EDGE ( 'NONE', *, *, #50681, .F. ) ;
#48442=CARTESIAN_POINT ( 'NONE',  ( 4.149127210878736705, 3.663616288757004291, 26.00000000000000711 ) ) ;
#48451=CARTESIAN_POINT ( 'NONE',  ( -6.344366288193416636, -4.720772854004745334, 26.00000000000000711 ) ) ;
#48454=DIRECTION ( 'NONE',  ( 0.8660254037844435926, 0.4999999999999913958, 2.509347957447859069E-16 ) ) ;
#48456=EDGE_LOOP ( 'NONE', ( #11984, #55639, #17696, #1541 ) ) ;
#48458=VECTOR ( 'NONE', #32595, 1000.000000000000000 ) ;
#48466=CARTESIAN_POINT ( 'NONE',  ( -8.916576262117258622, 10.03972626211718477, 26.00000000000000711 ) ) ;
#48469=ORIENTED_EDGE ( 'NONE', *, *, #9942, .T. ) ;
#48504=ORIENTED_EDGE ( 'NONE', *, *, #17534, .F. ) ;
#48513=VERTEX_POINT ( 'NONE', #45335 ) ;
#48522=CARTESIAN_POINT ( 'NONE',  ( -7.342976262117259623, 6.651770455163663165, 54.00000000000000711 ) ) ;
#48532=CARTESIAN_POINT ( 'NONE',  ( 8.835729544836338434, -7.969523737882825642, 54.00000000000000711 ) ) ;
#48534=LINE ( 'NONE', #36893, #11642 ) ;
#48539=CARTESIAN_POINT ( 'NONE',  ( 4.720772854004775532, -4.155633711806681063, 54.00000000000000711 ) ) ;
#48548=AXIS2_PLACEMENT_3D ( 'NONE', #35623, #12652, #45891 ) ;
#48550=AXIS2_PLACEMENT_3D ( 'NONE', #66394, #39175, #12625 ) ;
#48558=EDGE_CURVE ( 'NONE', #40825, #28070, #28731, .T. ) ;
#48560=EDGE_CURVE ( 'NONE', #6981, #22970, #44994, .T. ) ;
#48564=LINE ( 'NONE', #64830, #23718 ) ;
#48571=ORIENTED_EDGE ( 'NONE', *, *, #42969, .T. ) ;
#48576=DIRECTION ( 'NONE',  ( 9.912705577010386883E-15, 1.000000000000000000, 0.000000000000000000 ) ) ;
#48579=DIRECTION ( 'NONE',  ( 1.034072152899299800E-14, 1.000000000000000000, 0.000000000000000000 ) ) ;
#48583=ORIENTED_EDGE ( 'NONE', *, *, #47521, .T. ) ;
#48584=CIRCLE ( 'NONE', #24855, 0.1750000000000002387 ) ;
#48595=VERTEX_POINT ( 'NONE', #8206 ) ;
#48596=AXIS2_PLACEMENT_3D ( 'NONE', #33996, #33663, #40355 ) ;
#48599=VECTOR ( 'NONE', #29170, 1000.000000000000000 ) ;
#48612=ADVANCED_FACE ( 'NONE', ( #63727 ), #19520, .F. ) ;
#48631=LINE ( 'NONE', #540, #17607 ) ;
#48644=CARTESIAN_POINT ( 'NONE',  ( 3.682023737882785586, -9.912023737882808661, 54.00000000000000711 ) ) ;
#48645=DIRECTION ( 'NONE',  ( 0.7671651518153105309, 0.6414496315691445849, 2.356647714346206145E-16 ) ) ;
#48657=DIRECTION ( 'NONE',  ( -0.000000000000000000, 3.673940397442059868E-16, -1.000000000000000000 ) ) ;
#48670=EDGE_LOOP ( 'NONE', ( #30465, #746, #18066, #25007 ) ) ;
#48672=DIRECTION ( 'NONE',  ( 9.912705577010336396E-15, 1.000000000000000000, 0.000000000000000000 ) ) ;
#48673=DIRECTION ( 'NONE',  ( 1.836970198721029934E-16, 1.836970198721010706E-16, -1.000000000000000000 ) ) ;
#48681=DIRECTION ( 'NONE',  ( 1.836970198721029934E-16, 1.836970198721010706E-16, -1.000000000000000000 ) ) ;
#48684=CARTESIAN_POINT ( 'NONE',  ( -8.130476262117259267, 9.547976262117177981, 54.00000000000000711 ) ) ;
#48691=VECTOR ( 'NONE', #42558, 1000.000000000000000 ) ;
#48693=PLANE ( 'NONE',  #47842 ) ;
#48707=AXIS2_PLACEMENT_3D ( 'NONE', #34136, #61012, #12917 ) ;
#48716=VERTEX_POINT ( 'NONE', #41446 ) ;
#48729=DIRECTION ( 'NONE',  ( -1.836970198721029934E-16, 1.836970198721036590E-16, -1.000000000000000000 ) ) ;
#48730=ORIENTED_EDGE ( 'NONE', *, *, #23613, .T. ) ;
#48732=DIRECTION ( 'NONE',  ( 0.000000000000000000, 1.000000000000000000, 3.673940397442059868E-16 ) ) ;
#48740=CARTESIAN_POINT ( 'NONE',  ( -5.538810540050023157, 7.342976262117183239, 54.00000000000000711 ) ) ;
#48743=DIRECTION ( 'NONE',  ( 1.836970198721029934E-16, 1.836970198721010706E-16, -1.000000000000000000 ) ) ;
#48752=LINE ( 'NONE', #33521, #45528 ) ;
#48756=ORIENTED_EDGE ( 'NONE', *, *, #37321, .T. ) ;
#48780=EDGE_CURVE ( 'NONE', #67915, #63729, #27623, .T. ) ;
#48783=PLANE ( 'NONE',  #58699 ) ;
#48786=VECTOR ( 'NONE', #40799, 1000.000000000000000 ) ;
#48788=EDGE_CURVE ( 'NONE', #36931, #56714, #42842, .T. ) ;
#48789=DIRECTION ( 'NONE',  ( -1.836970198721029934E-16, 1.836970198721036344E-16, -1.000000000000000000 ) ) ;
#48795=DIRECTION ( 'NONE',  ( -1.000000000000000000, 0.000000000000000000, 0.000000000000000000 ) ) ;
#48801=VECTOR ( 'NONE', #23664, 1000.000000000000000 ) ;
#48809=AXIS2_PLACEMENT_3D ( 'NONE', #58879, #26691, #31661 ) ;
#48810=ADVANCED_FACE ( 'NONE', ( #773 ), #16321, .F. ) ;
#48817=AXIS2_PLACEMENT_3D ( 'NONE', #33542, #39196, #23970 ) ;
#48821=EDGE_CURVE ( 'NONE', #51395, #50609, #43880, .T. ) ;
#48824=ORIENTED_EDGE ( 'NONE', *, *, #56860, .F. ) ;
#48826=VERTEX_POINT ( 'NONE', #64760 ) ;
#48827=EDGE_CURVE ( 'NONE', #49071, #2772, #37899, .T. ) ;
#48831=DIRECTION ( 'NONE',  ( 0.4999999999999974465, -0.8660254037844401509, -2.509347957447879284E-16 ) ) ;
#48842=ORIENTED_EDGE ( 'NONE', *, *, #58859, .T. ) ;
#48851=CYLINDRICAL_SURFACE ( 'NONE', #60880, 1.224999999999998757 ) ;
#48855=DIRECTION ( 'NONE',  ( 1.920885163218982051E-15, 1.000000000000000000, 1.836970198721033139E-16 ) ) ;
#48863=VERTEX_POINT ( 'NONE', #49880 ) ;
#48866=ORIENTED_EDGE ( 'NONE', *, *, #51335, .F. ) ;
#48870=AXIS2_PLACEMENT_3D ( 'NONE', #64524, #17111, #32002 ) ;
#48876=DIRECTION ( 'NONE',  ( -0.000000000000000000, -0.000000000000000000, -1.000000000000000000 ) ) ;
#48882=EDGE_LOOP ( 'NONE', ( #62077, #59970, #26937, #43250 ) ) ;
#48919=ORIENTED_EDGE ( 'NONE', *, *, #30083, .F. ) ;
#48921=VECTOR ( 'NONE', #60843, 1000.000000000000000 ) ;
#48925=AXIS2_PLACEMENT_3D ( 'NONE', #61332, #30233, #51794 ) ;
#48927=CIRCLE ( 'NONE', #28548, 0.1749999999999989342 ) ;
#48930=VECTOR ( 'NONE', #46621, 1000.000000000000000 ) ;
#48937=ORIENTED_EDGE ( 'NONE', *, *, #69912, .F. ) ;
#48943=DIRECTION ( 'NONE',  ( -0.7071067811865550112, -0.7071067811865401342, 0.000000000000000000 ) ) ;
#48948=CARTESIAN_POINT ( 'NONE',  ( -7.342976262117282715, -5.552858015815545834, 54.00000000000000711 ) ) ;
#48954=ORIENTED_EDGE ( 'NONE', *, *, #55593, .T. ) ;
#48962=ADVANCED_FACE ( 'NONE', ( #33621 ), #29341, .T. ) ;
#48964=EDGE_CURVE ( 'NONE', #8868, #1245, #39604, .T. ) ;
#48966=DIRECTION ( 'NONE',  ( -1.000000000000000000, 0.000000000000000000, 0.000000000000000000 ) ) ;
#48976=ORIENTED_EDGE ( 'NONE', *, *, #3969, .F. ) ;
#48978=CIRCLE ( 'NONE', #26358, 0.5250000000000003553 ) ;
#48979=ORIENTED_EDGE ( 'NONE', *, *, #66831, .T. ) ;
#48981=VERTEX_POINT ( 'NONE', #45970 ) ;
#48982=CARTESIAN_POINT ( 'NONE',  ( 5.257023737882819070, -5.257023737882815517, 26.00000000000000711 ) ) ;
#48985=LINE ( 'NONE', #32711, #8505 ) ;
#48987=DIRECTION ( 'NONE',  ( -1.047444401652940007E-14, -1.000000000000000000, 0.000000000000000000 ) ) ;
#48990=ORIENTED_EDGE ( 'NONE', *, *, #53014, .T. ) ;
#48991=LINE ( 'NONE', #918, #22114 ) ;
#48994=EDGE_CURVE ( 'NONE', #32184, #67007, #8835, .T. ) ;
#49007=CARTESIAN_POINT ( 'NONE',  ( 10.31452373788278187, 3.650476262117146042, 54.00000000000000711 ) ) ;
#49010=CARTESIAN_POINT ( 'NONE',  ( 9.912023737882798002, 6.642976262117190167, 26.00000000000000711 ) ) ;
#49018=AXIS2_PLACEMENT_3D ( 'NONE', #60578, #65546, #1198 ) ;
#49039=CARTESIAN_POINT ( 'NONE',  ( 9.703773737882785966, -10.05377373788281403, 26.00000000000000000 ) ) ;
#49040=EDGE_CURVE ( 'NONE', #19647, #42529, #34996, .T. ) ;
#49045=ADVANCED_FACE ( 'NONE', ( #25103 ), #47016, .F. ) ;
#49049=DIRECTION ( 'NONE',  ( -1.836970198721029934E-16, -1.836970198721010706E-16, 1.000000000000000000 ) ) ;
#49053=ORIENTED_EDGE ( 'NONE', *, *, #61803, .T. ) ;
#49058=CARTESIAN_POINT ( 'NONE',  ( -3.710438382363177912, -7.408280051175174741, 54.00000000000000711 ) ) ;
#49059=CYLINDRICAL_SURFACE ( 'NONE', #15928, 0.5249999999999994671 ) ;
#49066=CARTESIAN_POINT ( 'NONE',  ( -8.697938382363135545, 2.406732575409538111, 54.00000000000000711 ) ) ;
#49067=ORIENTED_EDGE ( 'NONE', *, *, #57418, .T. ) ;
#49071=VERTEX_POINT ( 'NONE', #13784 ) ;
#49073=EDGE_CURVE ( 'NONE', #52982, #5963, #8120, .T. ) ;
#49074=AXIS2_PLACEMENT_3D ( 'NONE', #27560, #65056, #65736 ) ;
#49075=DIRECTION ( 'NONE',  ( -1.836970198721029934E-16, 1.836970198721036590E-16, -1.000000000000000000 ) ) ;
#49077=CARTESIAN_POINT ( 'NONE',  ( -8.697938382363135545, 8.079219948824830411, 54.00000000000000711 ) ) ;
#49078=CARTESIAN_POINT ( 'NONE',  ( -4.135079735113167843, 3.663616288757005623, 54.00000000000000711 ) ) ;
#49098=DIRECTION ( 'NONE',  ( 0.000000000000000000, 1.000000000000000000, 0.000000000000000000 ) ) ;
#49107=ORIENTED_EDGE ( 'NONE', *, *, #69362, .F. ) ;
#49111=CARTESIAN_POINT ( 'NONE',  ( 5.257023737882819070, -5.257023737882815517, 26.00000000000000711 ) ) ;
#49115=CARTESIAN_POINT ( 'NONE',  ( -9.390476262117260831, 0.9414762621171833823, 54.00000000000000711 ) ) ;
#49116=EDGE_LOOP ( 'NONE', ( #50857, #58556, #26891, #3586 ) ) ;
#49118=CARTESIAN_POINT ( 'NONE',  ( -6.822336235477446387, -4.149127210878696737, 54.00000000000000711 ) ) ;
#49122=DIRECTION ( 'NONE',  ( -0.7071067811865513475, -0.7071067811865435759, 0.000000000000000000 ) ) ;
#49126=EDGE_CURVE ( 'NONE', #59026, #59587, #40674, .T. ) ;
#49132=LINE ( 'NONE', #42780, #529 ) ;
#49133=DIRECTION ( 'NONE',  ( 0.000000000000000000, 1.000000000000000000, 0.000000000000000000 ) ) ;
#49142=CARTESIAN_POINT ( 'NONE',  ( -6.817976262117327657, -9.912023737882785568, 54.00000000000000711 ) ) ;
#49145=CARTESIAN_POINT ( 'NONE',  ( -8.227189898828745740, 1.620245201994245487, 54.00000000000000711 ) ) ;
#49155=PLANE ( 'NONE',  #31695 ) ;
#49164=PLANE ( 'NONE',  #26742 ) ;
#49173=CARTESIAN_POINT ( 'NONE',  ( -8.821682069070780230, 8.130476262117182884, 54.00000000000000711 ) ) ;
#49175=ORIENTED_EDGE ( 'NONE', *, *, #3136, .F. ) ;
#49178=VERTEX_POINT ( 'NONE', #67054 ) ;
#49181=AXIS2_PLACEMENT_3D ( 'NONE', #17511, #49367, #935 ) ;
#49183=AXIS2_PLACEMENT_3D ( 'NONE', #25878, #46375, #36472 ) ;
#49188=EDGE_LOOP ( 'NONE', ( #57842, #41661, #19513, #2777 ) ) ;
#49191=( NAMED_UNIT ( * ) PLANE_ANGLE_UNIT ( ) SI_UNIT ( $, .RADIAN. ) );
#49195=ORIENTED_EDGE ( 'NONE', *, *, #52380, .T. ) ;
#49199=ORIENTED_EDGE ( 'NONE', *, *, #66324, .F. ) ;
#49202=DIRECTION ( 'NONE',  ( -1.000000000000000000, 3.491481338843133355E-15, 1.836970198721036344E-16 ) ) ;
#49216=AXIS2_PLACEMENT_3D ( 'NONE', #15444, #58582, #10136 ) ;
#49222=EDGE_CURVE ( 'NONE', #8535, #19822, #35211, .T. ) ;
#49231=ORIENTED_EDGE ( 'NONE', *, *, #47593, .F. ) ;
#49248=DIRECTION ( 'NONE',  ( -1.836970198721029934E-16, -1.836970198721010706E-16, 1.000000000000000000 ) ) ;
#49259=CARTESIAN_POINT ( 'NONE',  ( -4.947141984184481700, 7.342976262117180575, 26.00000000000000711 ) ) ;
#49261=EDGE_CURVE ( 'NONE', #54522, #53050, #23923, .T. ) ;
#49264=ORIENTED_EDGE ( 'NONE', *, *, #34273, .F. ) ;
#49265=CARTESIAN_POINT ( 'NONE',  ( -4.135079735113208699, -3.677663764522613121, 54.00000000000000711 ) ) ;
#49267=CARTESIAN_POINT ( 'NONE',  ( 7.357023737882817827, -3.848229544836335947, 26.00000000000000711 ) ) ;
#49270=AXIS2_PLACEMENT_3D ( 'NONE', #23349, #1098, #60818 ) ;
#49274=CARTESIAN_POINT ( 'NONE',  ( -3.834182069070824816, -7.532023737882819425, 54.00000000000000711 ) ) ;
#49277=CIRCLE ( 'NONE', #51525, 0.1749999999999998224 ) ;
#49278=CIRCLE ( 'NONE', #1805, 0.3499999999999996447 ) ;
#49282=ORIENTED_EDGE ( 'NONE', *, *, #51981, .F. ) ;
#49288=EDGE_LOOP ( 'NONE', ( #155, #39213, #61926, #5329 ) ) ;
#49298=DIRECTION ( 'NONE',  ( 0.8660254037844510311, 0.4999999999999785727, 1.836970198720951294E-16 ) ) ;
#49301=LINE ( 'NONE', #43971, #6891 ) ;
#49307=CARTESIAN_POINT ( 'NONE',  ( 4.720772854004775532, -4.155633711806670405, 26.00000000000000711 ) ) ;
#49312=FACE_OUTER_BOUND ( 'NONE', #69679, .T. ) ;
#49325=VECTOR ( 'NONE', #48454, 1000.000000000000000 ) ;
#49330=AXIS2_PLACEMENT_3D ( 'NONE', #52533, #68446, #35544 ) ;
#49334=ORIENTED_EDGE ( 'NONE', *, *, #27331, .F. ) ;
#49335=CIRCLE ( 'NONE', #8630, 1.929199999999998916 ) ;
#49340=AXIS2_PLACEMENT_3D ( 'NONE', #19934, #68024, #36916 ) ;
#49341=PLANE ( 'NONE',  #62239 ) ;
#49343=ORIENTED_EDGE ( 'NONE', *, *, #60643, .F. ) ;
#49345=LINE ( 'NONE', #548, #66160 ) ;
#49350=DIRECTION ( 'NONE',  ( -1.000000000000000000, 0.000000000000000000, 0.000000000000000000 ) ) ;
#49358=EDGE_CURVE ( 'NONE', #63961, #62878, #57846, .T. ) ;
#49361=VECTOR ( 'NONE', #37774, 1000.000000000000000 ) ;
#49362=DIRECTION ( 'NONE',  ( 0.000000000000000000, -3.673940397442059868E-16, 1.000000000000000000 ) ) ;
#49367=DIRECTION ( 'NONE',  ( -0.000000000000000000, -0.000000000000000000, -1.000000000000000000 ) ) ;
#49373=DIRECTION ( 'NONE',  ( 0.000000000000000000, 1.000000000000000000, 0.000000000000000000 ) ) ;
#49376=DIRECTION ( 'NONE',  ( 8.339399738404099512E-15, 1.000000000000000000, 1.836970198721025990E-16 ) ) ;
#49387=ORIENTED_EDGE ( 'NONE', *, *, #36563, .F. ) ;
#49389=DIRECTION ( 'NONE',  ( -0.000000000000000000, 3.673940397442059868E-16, -1.000000000000000000 ) ) ;
#49408=ORIENTED_EDGE ( 'NONE', *, *, #21945, .T. ) ;
#49409=VERTEX_POINT ( 'NONE', #60543 ) ;
#49414=LINE ( 'NONE', #53678, #53342 ) ;
#49419=FACE_OUTER_BOUND ( 'NONE', #65728, .T. ) ;
#49423=AXIS2_PLACEMENT_3D ( 'NONE', #51423, #67687, #63086 ) ;
#49427=LINE ( 'NONE', #989, #33510 ) ;
#49429=AXIS2_PLACEMENT_3D ( 'NONE', #45141, #61395, #62100 ) ;
#49435=CARTESIAN_POINT ( 'NONE',  ( 4.046023737882794791, 3.142976262117205266, 54.00000000000000711 ) ) ;
#49444=FACE_OUTER_BOUND ( 'NONE', #45702, .T. ) ;
#49451=CARTESIAN_POINT ( 'NONE',  ( 8.930623737882818602, -8.930623737882855906, 54.00000000000000711 ) ) ;
#49454=DIRECTION ( 'NONE',  ( 1.000000000000000000, 0.000000000000000000, 0.000000000000000000 ) ) ;
#49457=DIRECTION ( 'NONE',  ( -1.062075597536821678E-14, -1.000000000000000000, 0.000000000000000000 ) ) ;
#49463=ORIENTED_EDGE ( 'NONE', *, *, #69362, .T. ) ;
#49465=VERTEX_POINT ( 'NONE', #37684 ) ;
#49468=LINE ( 'NONE', #16605, #24269 ) ;
#49472=CARTESIAN_POINT ( 'NONE',  ( 4.149127210878736705, 3.663616288757004291, 26.00000000000000711 ) ) ;
#49486=VERTEX_POINT ( 'NONE', #58566 ) ;
#49502=EDGE_LOOP ( 'NONE', ( #10606, #5414, #2385, #20118 ) ) ;
#49516=PLANE ( 'NONE',  #3288 ) ;
#49517=ORIENTED_EDGE ( 'NONE', *, *, #40676, .F. ) ;
#49522=CARTESIAN_POINT ( 'NONE',  ( 8.835729544836338434, -7.969523737882825642, 54.00000000000000711 ) ) ;
#49534=CARTESIAN_POINT ( 'NONE',  ( -5.242976262117259978, 5.242976262117182706, 54.00000000000000711 ) ) ;
#49550=CARTESIAN_POINT ( 'NONE',  ( 7.408280051175156977, 6.775514141871323837, 26.00000000000000711 ) ) ;
#49559=CARTESIAN_POINT ( 'NONE',  ( 4.961189459950039904, -7.357023737882821379, 54.00000000000000711 ) ) ;
#49562=CARTESIAN_POINT ( 'NONE',  ( -7.517976262117260333, 6.651770455163663165, 54.00000000000000711 ) ) ;
#49566=AXIS2_PLACEMENT_3D ( 'NONE', #44921, #66484, #18038 ) ;
#49573=ORIENTED_EDGE ( 'NONE', *, *, #6567, .F. ) ;
#49578=ORIENTED_EDGE ( 'NONE', *, *, #58690, .F. ) ;
#49579=ORIENTED_EDGE ( 'NONE', *, *, #34864, .T. ) ;
#49580=DIRECTION ( 'NONE',  ( -2.135044278125299371E-15, 1.000000000000000000, 0.000000000000000000 ) ) ;
#49582=CARTESIAN_POINT ( 'NONE',  ( -3.834182069070817711, -7.357023737882814274, 26.00000000000000711 ) ) ;
#49594=VECTOR ( 'NONE', #60605, 1000.000000000000000 ) ;
#49603=EDGE_CURVE ( 'NONE', #67007, #41511, #68403, .T. ) ;
#49604=CARTESIAN_POINT ( 'NONE',  ( -9.722976262117258628, 3.667976262117184749, 54.00000000000000711 ) ) ;
#49605=CYLINDRICAL_SURFACE ( 'NONE', #22765, 0.3499999999999996447 ) ;
#49607=LINE ( 'NONE', #22734, #57438 ) ;
#49613=CARTESIAN_POINT ( 'NONE',  ( -8.598420958951633608, -1.480523737882746271, 54.00000000000000711 ) ) ;
#49623=EDGE_LOOP ( 'NONE', ( #64542, #15989, #41748, #37133 ) ) ;
#49625=EDGE_CURVE ( 'NONE', #1811, #18679, #5607, .T. ) ;
#49634=CARTESIAN_POINT ( 'NONE',  ( 4.046023737882789462, 3.142976262117210151, 26.00000000000000711 ) ) ;
#49637=CARTESIAN_POINT ( 'NONE',  ( 5.257023737882807524, 7.172176262117201162, 54.00000000000000711 ) ) ;
#49638=ORIENTED_EDGE ( 'NONE', *, *, #42269, .F. ) ;
#49644=VECTOR ( 'NONE', #51103, 1000.000000000000000 ) ;
#49648=VERTEX_POINT ( 'NONE', #52860 ) ;
#49664=DIRECTION ( 'NONE',  ( 0.6414496315691539108, -0.7671651518153028704, -2.587583378555131256E-16 ) ) ;
#49669=EDGE_CURVE ( 'NONE', #55919, #25422, #1778, .T. ) ;
#49678=PLANE ( 'NONE',  #28108 ) ;
#49681=FACE_OUTER_BOUND ( 'NONE', #62120, .T. ) ;
#49688=CARTESIAN_POINT ( 'NONE',  ( -8.130476262117324993, -9.562023737882769936, 54.00000000000000711 ) ) ;
#49708=CYLINDRICAL_SURFACE ( 'NONE', #1505, 0.1749999999999998224 ) ;
#49711=ORIENTED_EDGE ( 'NONE', *, *, #16855, .T. ) ;
#49728=CARTESIAN_POINT ( 'NONE',  ( 6.789561617636943325, -7.408280051175178293, 54.00000000000000711 ) ) ;
#49751=AXIS2_PLACEMENT_3D ( 'NONE', #68312, #41438, #62646 ) ;
#49752=VERTEX_POINT ( 'NONE', #22665 ) ;
#49756=DIRECTION ( 'NONE',  ( 1.836970198721029934E-16, 1.836970198721010706E-16, -1.000000000000000000 ) ) ;
#49758=VECTOR ( 'NONE', #25995, 1000.000000000000000 ) ;
#49775=CARTESIAN_POINT ( 'NONE',  ( 2.420780051175169145, 8.697938382363084031, 54.00000000000000711 ) ) ;
#49782=DIRECTION ( 'NONE',  ( -0.000000000000000000, 3.673940397442059868E-16, -1.000000000000000000 ) ) ;
#49784=DIRECTION ( 'NONE',  ( 0.000000000000000000, -3.673940397442059868E-16, 1.000000000000000000 ) ) ;
#49786=ORIENTED_EDGE ( 'NONE', *, *, #40550, .F. ) ;
#49797=VERTEX_POINT ( 'NONE', #39598 ) ;
#49798=VECTOR ( 'NONE', #8461, 1000.000000000000000 ) ;
#49801=CIRCLE ( 'NONE', #37408, 0.3499999999999996447 ) ;
#49804=ORIENTED_EDGE ( 'NONE', *, *, #69272, .T. ) ;
#49811=DIRECTION ( 'NONE',  ( 0.7071067811865464625, -0.7071067811865486830, -2.597868168706484048E-16 ) ) ;
#49813=DIRECTION ( 'NONE',  ( -1.000000000000000000, 1.260948829465470062E-14, -1.836970198721007008E-16 ) ) ;
#49816=LINE ( 'NONE', #11289, #9756 ) ;
#49819=FACE_OUTER_BOUND ( 'NONE', #9354, .T. ) ;
#49829=CARTESIAN_POINT ( 'NONE',  ( -3.663616288757094885, -6.364920264886888113, 54.00000000000000711 ) ) ;
#49831=EDGE_CURVE ( 'NONE', #42074, #16599, #13435, .T. ) ;
#49834=ORIENTED_EDGE ( 'NONE', *, *, #63568, .T. ) ;
#49840=CARTESIAN_POINT ( 'NONE',  ( -8.598420958951683346, 1.466476262117183182, 54.00000000000000711 ) ) ;
#49846=ORIENTED_EDGE ( 'NONE', *, *, #18268, .F. ) ;
#49847=DIRECTION ( 'NONE',  ( 1.062075597536821205E-14, 1.000000000000000000, 0.000000000000000000 ) ) ;
#49853=VECTOR ( 'NONE', #25196, 1000.000000000000000 ) ;
#49860=CARTESIAN_POINT ( 'NONE',  ( -8.130476262117324993, -9.562023737882769936, 54.00000000000000711 ) ) ;
#49880=CARTESIAN_POINT ( 'NONE',  ( -6.858227778582867806, 2.989207322240119868, 54.00000000000000711 ) ) ;
#49890=LINE ( 'NONE', #66839, #41941 ) ;
#49898=LINE ( 'NONE', #22687, #23251 ) ;
#49903=EDGE_LOOP ( 'NONE', ( #21326, #21974, #3279, #18167, #9781, #30528, #47638, #15471, #9420, #28097, #5028, #29099, #40157, #44282, #10599, #37127, #36608, #23889, #2987, #2830, #15905, #32094, #3662, #14280, #40753, #16685, #56806, #48979, #60897, #40861, #52537, #13940, #62256, #47335, #2952, #40312, #11131, #13350, #41650, #64951, #35216, #3733, #32222, #21757, #54935, #41974, #34735, #9987, #17576, #31678, #57708, #15992, #10910, #51480, #8898, #15316 ) ) ;
#49906=EDGE_CURVE ( 'NONE', #63123, #8452, #14132, .T. ) ;
#49909=EDGE_CURVE ( 'NONE', #17133, #62878, #8115, .T. ) ;
#49915=CARTESIAN_POINT ( 'NONE',  ( 4.155633711806643760, 5.779227145995235126, 26.00000000000000711 ) ) ;
#49917=ORIENTED_EDGE ( 'NONE', *, *, #32099, .T. ) ;
#49925=ORIENTED_EDGE ( 'NONE', *, *, #47286, .T. ) ;
#49927=CARTESIAN_POINT ( 'NONE',  ( 8.711985858128644011, 2.406732575409517239, 54.00000000000000711 ) ) ;
#49932=CARTESIAN_POINT ( 'NONE',  ( -10.30047626211728939, -6.849523737882745600, 26.00000000000000000 ) ) ;
#49937=DIRECTION ( 'NONE',  ( 0.7671651518153006499, -0.6414496315691565753, -2.356647714346250026E-16 ) ) ;
#49946=ORIENTED_EDGE ( 'NONE', *, *, #24276, .T. ) ;
#49950=EDGE_LOOP ( 'NONE', ( #41734, #49282, #41965, #57351 ) ) ;
#49951=CARTESIAN_POINT ( 'NONE',  ( 3.664523737882778853, -10.50702373788280219, 26.00000000000000000 ) ) ;
#49954=CARTESIAN_POINT ( 'NONE',  ( 6.665817930929297752, -7.532023737882823866, 54.00000000000000711 ) ) ;
#49962=EDGE_CURVE ( 'NONE', #66946, #59628, #50909, .T. ) ;
#49963=VECTOR ( 'NONE', #47693, 1000.000000000000000 ) ;
#49969=AXIS2_PLACEMENT_3D ( 'NONE', #69326, #25506, #31514 ) ;
#49981=VECTOR ( 'NONE', #14018, 1000.000000000000000 ) ;
#49982=CARTESIAN_POINT ( 'NONE',  ( 8.835729544836338434, -8.144523737882813919, 26.00000000000000000 ) ) ;
#49987=ORIENTED_EDGE ( 'NONE', *, *, #34968, .F. ) ;
#49996=EDGE_CURVE ( 'NONE', #24983, #1371, #14848, .T. ) ;
#49997=VERTEX_POINT ( 'NONE', #63279 ) ;
#49998=ORIENTED_EDGE ( 'NONE', *, *, #41200, .F. ) ;
#50001=DIRECTION ( 'NONE',  ( -0.000000000000000000, -0.000000000000000000, -1.000000000000000000 ) ) ;
#50003=EDGE_CURVE ( 'NONE', #52054, #51180, #5669, .T. ) ;
#50019=DIRECTION ( 'NONE',  ( -0.000000000000000000, 3.673940397442059868E-16, -1.000000000000000000 ) ) ;
#50029=LINE ( 'NONE', #17510, #15898 ) ;
#50038=CIRCLE ( 'NONE', #69240, 1.224999999999998757 ) ;
#50054=ORIENTED_EDGE ( 'NONE', *, *, #32369, .F. ) ;
#50059=EDGE_CURVE ( 'NONE', #23915, #57396, #15560, .T. ) ;
#50062=EDGE_CURVE ( 'NONE', #6322, #45033, #9076, .T. ) ;
#50063=FACE_OUTER_BOUND ( 'NONE', #53720, .T. ) ;
#50064=AXIS2_PLACEMENT_3D ( 'NONE', #64995, #22209, #43773 ) ;
#50087=EDGE_CURVE ( 'NONE', #5747, #29034, #12285, .T. ) ;
#50090=VERTEX_POINT ( 'NONE', #43800 ) ;
#50094=LINE ( 'NONE', #44428, #25664 ) ;
#50096=VECTOR ( 'NONE', #66812, 1000.000000000000000 ) ;
#50101=ORIENTED_EDGE ( 'NONE', *, *, #13275, .T. ) ;
#50105=CARTESIAN_POINT ( 'NONE',  ( -2.406732575409589625, 8.697938382363036069, 54.00000000000000711 ) ) ;
#50109=EDGE_CURVE ( 'NONE', #38923, #32604, #14733, .T. ) ;
#50126=DIRECTION ( 'NONE',  ( 1.836970198721029934E-16, 1.836970198721010706E-16, -1.000000000000000000 ) ) ;
#50133=DIRECTION ( 'NONE',  ( -1.000000000000000000, 0.000000000000000000, 0.000000000000000000 ) ) ;
#50135=CARTESIAN_POINT ( 'NONE',  ( -7.342976262117259623, 4.947141984184421304, 54.00000000000000711 ) ) ;
#50142=EDGE_CURVE ( 'NONE', #25334, #1385, #17264, .T. ) ;
#50149=ORIENTED_EDGE ( 'NONE', *, *, #31777, .T. ) ;
#50154=DIRECTION ( 'NONE',  ( -1.000000000000000000, 0.000000000000000000, 0.000000000000000000 ) ) ;
#50155=VERTEX_POINT ( 'NONE', #66400 ) ;
#50157=LINE ( 'NONE', #34224, #69427 ) ;
#50160=VECTOR ( 'NONE', #20639, 1000.000000000000114 ) ;
#50163=EDGE_LOOP ( 'NONE', ( #39796, #39826, #42271, #27807 ) ) ;
#50168=ADVANCED_FACE ( 'NONE', ( #33531 ), #6319, .F. ) ;
#50173=ORIENTED_EDGE ( 'NONE', *, *, #54075, .F. ) ;
#50175=VECTOR ( 'NONE', #67201, 1000.000000000000000 ) ;
#50188=DIRECTION ( 'NONE',  ( 0.000000000000000000, -3.673940397442059868E-16, 1.000000000000000000 ) ) ;
#50197=CARTESIAN_POINT ( 'NONE',  ( 3.682023737882818448, 9.722976262117203561, 54.00000000000000711 ) ) ;
#50201=CARTESIAN_POINT ( 'NONE',  ( -1.620245201994373829, -8.241237374594328813, 54.00000000000000711 ) ) ;
#50205=LINE ( 'NONE', #34631, #38052 ) ;
#50208=CIRCLE ( 'NONE', #58149, 0.5249999999999990230 ) ;
#50216=CARTESIAN_POINT ( 'NONE',  ( 4.155633711806649089, 5.779227145995230686, 54.00000000000000711 ) ) ;
#50219=FACE_BOUND ( 'NONE', #52406, .T. ) ;
#50234=CARTESIAN_POINT ( 'NONE',  ( 2.544523737882785852, -9.737023737882790186, 26.00000000000000000 ) ) ;
#50237=DIRECTION ( 'NONE',  ( -0.000000000000000000, 3.673940397442059868E-16, -1.000000000000000000 ) ) ;
#50245=ORIENTED_EDGE ( 'NONE', *, *, #38186, .F. ) ;
#50253=AXIS2_PLACEMENT_3D ( 'NONE', #49522, #33261, #44902 ) ;
#50256=CARTESIAN_POINT ( 'NONE',  ( 3.857023737882779635, -10.31452373788281029, 54.00000000000000711 ) ) ;
#50267=FACE_OUTER_BOUND ( 'NONE', #29642, .T. ) ;
#50273=ORIENTED_EDGE ( 'NONE', *, *, #52217, .T. ) ;
#50276=DIRECTION ( 'NONE',  ( 1.836970198721029934E-16, 1.836970198721010706E-16, -1.000000000000000000 ) ) ;
#50277=DIRECTION ( 'NONE',  ( 1.000000000000000000, -1.883404846338789915E-14, 1.836970198720995421E-16 ) ) ;
#50286=VERTEX_POINT ( 'NONE', #8747 ) ;
#50289=CARTESIAN_POINT ( 'NONE',  ( -6.835476262117334834, -10.50702373788278798, 54.00000000000000711 ) ) ;
#50290=CARTESIAN_POINT ( 'NONE',  ( -10.03972626211731445, -8.930623737882747548, 26.00000000000000000 ) ) ;
#50292=LINE ( 'NONE', #1863, #14537 ) ;
#50294=EDGE_LOOP ( 'NONE', ( #54717, #960, #42278, #41445 ) ) ;
#50297=FACE_OUTER_BOUND ( 'NONE', #48183, .T. ) ;
#50301=AXIS2_PLACEMENT_3D ( 'NONE', #33740, #56705, #66615 ) ;
#50306=ORIENTED_EDGE ( 'NONE', *, *, #26792, .F. ) ;
#50315=DIRECTION ( 'NONE',  ( 1.000000000000000000, -1.047444401652940007E-14, 1.836970198721010706E-16 ) ) ;
#50327=AXIS2_PLACEMENT_3D ( 'NONE', #55856, #55519, #28631 ) ;
#50335=CARTESIAN_POINT ( 'NONE',  ( -6.344366288193437953, -5.793274621760813758, 54.00000000000000711 ) ) ;
#50336=VERTEX_POINT ( 'NONE', #12980 ) ;
#50341=EDGE_CURVE ( 'NONE', #52963, #15214, #46219, .T. ) ;
#50355=AXIS2_PLACEMENT_3D ( 'NONE', #54661, #28130, #65612 ) ;
#50365=CARTESIAN_POINT ( 'NONE',  ( -10.30047626211729472, -6.849523737882750929, 54.00000000000000711 ) ) ;
#50370=DIRECTION ( 'NONE',  ( 0.000000000000000000, 1.000000000000000000, 0.000000000000000000 ) ) ;
#50372=CARTESIAN_POINT ( 'NONE',  ( 8.835729544836331328, 7.955476262117188391, 54.00000000000000711 ) ) ;
#50381=DIRECTION ( 'NONE',  ( -1.000000000000000000, 0.000000000000000000, 0.000000000000000000 ) ) ;
#50390=DIRECTION ( 'NONE',  ( 1.836970198721029934E-16, 1.836970198721010706E-16, -1.000000000000000000 ) ) ;
#50391=DIRECTION ( 'NONE',  ( -1.000000000000000000, 0.000000000000000000, 0.000000000000000000 ) ) ;
#50394=CARTESIAN_POINT ( 'NONE',  ( -10.49297626211726175, 6.835476262117182955, 54.00000000000000711 ) ) ;
#50396=EDGE_CURVE ( 'NONE', #62286, #45123, #5200, .T. ) ;
#50400=AXIS2_PLACEMENT_3D ( 'NONE', #68212, #24730, #31453 ) ;
#50417=VECTOR ( 'NONE', #63491, 1000.000000000000000 ) ;
#50444=EDGE_CURVE ( 'NONE', #45122, #9220, #46917, .T. ) ;
#50447=LINE ( 'NONE', #6621, #7565 ) ;
#50459=ORIENTED_EDGE ( 'NONE', *, *, #17123, .F. ) ;
#50460=CARTESIAN_POINT ( 'NONE',  ( 6.657023737882818537, -10.31452373788282095, 54.00000000000000711 ) ) ;
#50462=DIRECTION ( 'NONE',  ( -0.000000000000000000, 3.673940397442059868E-16, -1.000000000000000000 ) ) ;
#50472=ADVANCED_FACE ( 'NONE', ( #25727 ), #10492, .T. ) ;
#50473=CARTESIAN_POINT ( 'NONE',  ( 6.832023737882812142, 9.897976262117197166, 26.00000000000000711 ) ) ;
#50488=PLANE ( 'NONE',  #69151 ) ;
#50489=VERTEX_POINT ( 'NONE', #33099 ) ;
#50490=DIRECTION ( 'NONE',  ( 0.000000000000000000, 0.000000000000000000, 1.000000000000000000 ) ) ;
#50494=EDGE_CURVE ( 'NONE', #30798, #57897, #11349, .T. ) ;
#50496=AXIS2_PLACEMENT_3D ( 'NONE', #40960, #34250, #18336 ) ;
#50501=ORIENTED_EDGE ( 'NONE', *, *, #11141, .F. ) ;
#50502=CARTESIAN_POINT ( 'NONE',  ( 1.634292677759869195, 8.227189898828703107, 26.00000000000000711 ) ) ;
#50507=DIRECTION ( 'NONE',  ( 1.034072152899300274E-14, 1.000000000000000000, 0.000000000000000000 ) ) ;
#50513=AXIS2_PLACEMENT_3D ( 'NONE', #41375, #3910, #68614 ) ;
#50527=VERTEX_POINT ( 'NONE', #6912 ) ;
#50533=ORIENTED_EDGE ( 'NONE', *, *, #4809, .T. ) ;
#50535=LINE ( 'NONE', #33576, #54937 ) ;
#50541=CIRCLE ( 'NONE', #6548, 0.1749999999999998224 ) ;
#50547=EDGE_CURVE ( 'NONE', #45122, #66645, #32423, .T. ) ;
#50549=CARTESIAN_POINT ( 'NONE',  ( -3.842976262117221875, 10.30047626211716860, 54.00000000000000711 ) ) ;
#50559=CARTESIAN_POINT ( 'NONE',  ( 3.157023737882800773, 5.242976262117208464, 54.00000000000000711 ) ) ;
#50567=VECTOR ( 'NONE', #4049, 1000.000000000000000 ) ;
#50568=CIRCLE ( 'NONE', #17810, 0.5249999999999994671 ) ;
#50570=CARTESIAN_POINT ( 'NONE',  ( -8.079219948824961861, -8.711985858128649340, 54.00000000000000711 ) ) ;
#50571=DIRECTION ( 'NONE',  ( 0.000000000000000000, 1.000000000000000000, 0.000000000000000000 ) ) ;
#50575=CARTESIAN_POINT ( 'NONE',  ( -6.350872789121327244, 6.822336235477381550, 26.00000000000000711 ) ) ;
#50589=ORIENTED_EDGE ( 'NONE', *, *, #8803, .F. ) ;
#50604=ORIENTED_EDGE ( 'NONE', *, *, #17161, .F. ) ;
#50609=VERTEX_POINT ( 'NONE', #60309 ) ;
#50610=ORIENTED_EDGE ( 'NONE', *, *, #35378, .F. ) ;
#50616=ORIENTED_EDGE ( 'NONE', *, *, #11169, .F. ) ;
#50623=VECTOR ( 'NONE', #68398, 1000.000000000000000 ) ;
#50628=DIRECTION ( 'NONE',  ( -2.135044278125301343E-15, 1.000000000000000000, 0.000000000000000000 ) ) ;
#50629=DIRECTION ( 'NONE',  ( 0.5000000000000004441, -0.8660254037844383745, 0.000000000000000000 ) ) ;
#50640=FACE_OUTER_BOUND ( 'NONE', #15764, .T. ) ;
#50646=CARTESIAN_POINT ( 'NONE',  ( -5.242976262117280406, -5.257023737882805747, 54.00000000000000711 ) ) ;
#50648=EDGE_CURVE ( 'NONE', #20701, #16704, #39775, .T. ) ;
#50663=ORIENTED_EDGE ( 'NONE', *, *, #9778, .T. ) ;
#50668=LINE ( 'NONE', #3283, #7737 ) ;
#50671=CYLINDRICAL_SURFACE ( 'NONE', #5957, 1.929199999999998916 ) ;
#50674=ORIENTED_EDGE ( 'NONE', *, *, #37103, .F. ) ;
#50676=EDGE_LOOP ( 'NONE', ( #56838, #860, #3319, #55989 ) ) ;
#50678=DIRECTION ( 'NONE',  ( -0.000000000000000000, 3.673940397442059868E-16, -1.000000000000000000 ) ) ;
#50680=( NAMED_UNIT ( * ) SI_UNIT ( $, .STERADIAN. ) SOLID_ANGLE_UNIT ( ) );
#50681=EDGE_CURVE ( 'NONE', #42591, #55218, #45433, .T. ) ;
#50684=ORIENTED_EDGE ( 'NONE', *, *, #61458, .T. ) ;
#50685=DIRECTION ( 'NONE',  ( 0.000000000000000000, 0.000000000000000000, 1.000000000000000000 ) ) ;
#50687=ORIENTED_EDGE ( 'NONE', *, *, #28703, .F. ) ;
#50696=DIRECTION ( 'NONE',  ( -1.000000000000000000, 0.000000000000000000, 0.000000000000000000 ) ) ;
#50697=ORIENTED_EDGE ( 'NONE', *, *, #69269, .T. ) ;
#50705=VERTEX_POINT ( 'NONE', #18929 ) ;
#50708=PLANE ( 'NONE',  #62782 ) ;
#50714=AXIS2_PLACEMENT_3D ( 'NONE', #48216, #26292, #59857 ) ;
#50726=PLANE ( 'NONE',  #60553 ) ;
#50730=DIRECTION ( 'NONE',  ( -0.7071067811865530128, -0.7071067811865421326, 0.000000000000000000 ) ) ;
#50737=LINE ( 'NONE', #40833, #48599 ) ;
#50747=DIRECTION ( 'NONE',  ( 1.079558018506126625E-14, 1.000000000000000000, 1.836970198721016622E-16 ) ) ;
#50763=ORIENTED_EDGE ( 'NONE', *, *, #61282, .F. ) ;
#50773=VERTEX_POINT ( 'NONE', #3361 ) ;
#50775=DIRECTION ( 'NONE',  ( -0.5000000000000038858, -0.8660254037844363761, 0.000000000000000000 ) ) ;
#50784=CARTESIAN_POINT ( 'NONE',  ( -4.947141984184481700, 7.342976262117180575, 54.00000000000000711 ) ) ;
#50787=EDGE_CURVE ( 'NONE', #46451, #17943, #3715, .T. ) ;
#50793=ORIENTED_EDGE ( 'NONE', *, *, #66993, .F. ) ;
#50794=VERTEX_POINT ( 'NONE', #37294 ) ;
#50795=DIRECTION ( 'NONE',  ( -0.000000000000000000, 3.673940397442059868E-16, -1.000000000000000000 ) ) ;
#50811=CARTESIAN_POINT ( 'NONE',  ( 8.580623737882843827, 9.689726262117162037, 26.00000000000000711 ) ) ;
#50813=DIRECTION ( 'NONE',  ( 0.6414496315691494699, 0.7671651518153064231, 2.818519042764025305E-16 ) ) ;
#50817=DIRECTION ( 'NONE',  ( 0.000000000000000000, -1.000000000000000000, -3.673940397442059868E-16 ) ) ;
#50818=EDGE_CURVE ( 'NONE', #47021, #7568, #31309, .T. ) ;
#50826=CARTESIAN_POINT ( 'NONE',  ( -1.991476262117315432, -8.612468434717262866, 54.00000000000000711 ) ) ;
#50827=EDGE_LOOP ( 'NONE', ( #30645, #45463, #43921, #25106 ) ) ;
#50835=CARTESIAN_POINT ( 'NONE',  ( 5.257023737882819070, -5.257023737882815517, 26.00000000000000711 ) ) ;
#50839=CARTESIAN_POINT ( 'NONE',  ( -5.242976262117275077, -5.257023737882800418, 26.00000000000000711 ) ) ;
#50842=LINE ( 'NONE', #66423, #16317 ) ;
#50849=CARTESIAN_POINT ( 'NONE',  ( 5.793274621760843957, -6.358413763958980169, 54.00000000000000711 ) ) ;
#50852=EDGE_CURVE ( 'NONE', #22770, #57348, #15024, .T. ) ;
#50857=ORIENTED_EDGE ( 'NONE', *, *, #65320, .T. ) ;
#50872=DIRECTION ( 'NONE',  ( -0.000000000000000000, 3.673940397442059868E-16, -1.000000000000000000 ) ) ;
#50877=DIRECTION ( 'NONE',  ( -1.000000000000000000, 0.000000000000000000, 0.000000000000000000 ) ) ;
#50880=DIRECTION ( 'NONE',  ( 0.000000000000000000, 3.673940397442059868E-16, -1.000000000000000000 ) ) ;
#50888=ORIENTED_EDGE ( 'NONE', *, *, #35780, .F. ) ;
#50892=LINE ( 'NONE', #56893, #44634 ) ;
#50896=EDGE_CURVE ( 'NONE', #18842, #59664, #25644, .T. ) ;
#50900=CARTESIAN_POINT ( 'NONE',  ( -8.566576262117260754, 9.689726262117185129, 54.00000000000000711 ) ) ;
#50909=LINE ( 'NONE', #24036, #12382 ) ;
#50913=ORIENTED_EDGE ( 'NONE', *, *, #12949, .F. ) ;
#50915=ORIENTED_EDGE ( 'NONE', *, *, #790, .F. ) ;
#50918=FACE_OUTER_BOUND ( 'NONE', #18966, .T. ) ;
#50937=CARTESIAN_POINT ( 'NONE',  ( 2.369523737882786918, -9.562023737882787700, 26.00000000000000000 ) ) ;
#50942=EDGE_CURVE ( 'NONE', #6930, #43292, #5814, .T. ) ;
#50944=ORIENTED_EDGE ( 'NONE', *, *, #31581, .T. ) ;
#50945=EDGE_CURVE ( 'NONE', #47387, #36248, #49301, .T. ) ;
#50957=CARTESIAN_POINT ( 'NONE',  ( 6.364920264886885448, -3.677663764522628664, 54.00000000000000711 ) ) ;
#50966=VECTOR ( 'NONE', #36147, 1000.000000000000000 ) ;
#50978=LINE ( 'NONE', #67599, #25617 ) ;
#50993=EDGE_LOOP ( 'NONE', ( #63467, #57337, #43382, #66757 ) ) ;
#50995=VECTOR ( 'NONE', #30810, 1000.000000000000000 ) ;
#51035=CARTESIAN_POINT ( 'NONE',  ( -4.706725378239246638, -4.155633711806646424, 26.00000000000000711 ) ) ;
#51036=FACE_OUTER_BOUND ( 'NONE', #37737, .T. ) ;
#51040=CARTESIAN_POINT ( 'NONE',  ( -8.916576262117258622, 10.03972626211718477, 54.00000000000000711 ) ) ;
#51047=AXIS2_PLACEMENT_3D ( 'NONE', #41679, #68206, #3510 ) ;
#51067=PLANE ( 'NONE',  #13974 ) ;
#51071=CARTESIAN_POINT ( 'NONE',  ( 3.677663764522614454, -6.364920264886879231, 54.00000000000000711 ) ) ;
#51075=VERTEX_POINT ( 'NONE', #24499 ) ;
#51081=FACE_OUTER_BOUND ( 'NONE', #12387, .T. ) ;
#51085=CARTESIAN_POINT ( 'NONE',  ( -6.486996718459913325, -3.157023737882783454, 54.00000000000000711 ) ) ;
#51087=ORIENTED_EDGE ( 'NONE', *, *, #18820, .F. ) ;
#51101=VERTEX_POINT ( 'NONE', #2224 ) ;
#51103=DIRECTION ( 'NONE',  ( 1.836970198721029934E-16, 1.836970198721010706E-16, -1.000000000000000000 ) ) ;
#51104=CARTESIAN_POINT ( 'NONE',  ( -10.30047626211725742, 3.842976262117182351, 26.00000000000000711 ) ) ;
#51113=LINE ( 'NONE', #13632, #65900 ) ;
#51114=CARTESIAN_POINT ( 'NONE',  ( 3.857023737882813386, 10.30047626211720768, 26.00000000000000711 ) ) ;
#51117=ORIENTED_EDGE ( 'NONE', *, *, #18070, .T. ) ;
#51120=CIRCLE ( 'NONE', #57891, 0.3499999999999996447 ) ;
#51123=AXIS2_PLACEMENT_3D ( 'NONE', #36090, #52735, #47062 ) ;
#51124=ORIENTED_EDGE ( 'NONE', *, *, #53856, .T. ) ;
#51135=ORIENTED_EDGE ( 'NONE', *, *, #66656, .T. ) ;
#51138=EDGE_CURVE ( 'NONE', #61285, #17051, #24972, .T. ) ;
#51140=CARTESIAN_POINT ( 'NONE',  ( 9.404523737882817258, -1.480523737882826207, 54.00000000000000711 ) ) ;
#51141=AXIS2_PLACEMENT_3D ( 'NONE', #42010, #3827, #37071 ) ;
#51143=DIRECTION ( 'NONE',  ( 0.000000000000000000, 0.000000000000000000, 1.000000000000000000 ) ) ;
#51147=ORIENTED_EDGE ( 'NONE', *, *, #4209, .T. ) ;
#51152=CARTESIAN_POINT ( 'NONE',  ( -3.667976262117228714, 9.722976262117169810, 54.00000000000000711 ) ) ;
#51153=CARTESIAN_POINT ( 'NONE',  ( 4.149127210878726935, -6.836383711242993044, 26.00000000000000000 ) ) ;
#51158=PLANE ( 'NONE',  #69551 ) ;
#51161=LINE ( 'NONE', #39839, #59764 ) ;
#51163=AXIS2_PLACEMENT_3D ( 'NONE', #58851, #69452, #20314 ) ;
#51170=ORIENTED_EDGE ( 'NONE', *, *, #37747, .T. ) ;
#51180=VERTEX_POINT ( 'NONE', #51357 ) ;
#51184=FACE_OUTER_BOUND ( 'NONE', #34350, .T. ) ;
#51189=ORIENTED_EDGE ( 'NONE', *, *, #45684, .T. ) ;
#51195=EDGE_CURVE ( 'NONE', #34744, #16520, #9183, .T. ) ;
#51197=LINE ( 'NONE', #29979, #40371 ) ;
#51198=DIRECTION ( 'NONE',  ( 0.000000000000000000, -0.000000000000000000, 1.000000000000000000 ) ) ;
#51215=EDGE_CURVE ( 'NONE', #49797, #54695, #8570, .T. ) ;
#51221=VERTEX_POINT ( 'NONE', #35795 ) ;
#51231=CARTESIAN_POINT ( 'NONE',  ( -10.30047626211725742, 6.642976262117184838, 54.00000000000000711 ) ) ;
#51233=DIRECTION ( 'NONE',  ( 1.836970198721029934E-16, 1.836970198721010706E-16, -1.000000000000000000 ) ) ;
#51238=CARTESIAN_POINT ( 'NONE',  ( -8.697938382363135545, 2.406732575409538111, 54.00000000000000711 ) ) ;
#51240=DIRECTION ( 'NONE',  ( -1.053224967557348291E-14, -1.000000000000000000, 0.000000000000000000 ) ) ;
#51243=DIRECTION ( 'NONE',  ( 3.540251991789403884E-15, 1.000000000000000000, 0.000000000000000000 ) ) ;
#51247=CYLINDRICAL_SURFACE ( 'NONE', #810, 1.929199999999998028 ) ;
#51251=ORIENTED_EDGE ( 'NONE', *, *, #63568, .F. ) ;
#51254=ORIENTED_EDGE ( 'NONE', *, *, #36927, .F. ) ;
#51271=EDGE_CURVE ( 'NONE', #50794, #97, #20235, .T. ) ;
#51275=VECTOR ( 'NONE', #26882, 1000.000000000000000 ) ;
#51280=CARTESIAN_POINT ( 'NONE',  ( 9.737023737882816832, -3.682023737882826886, 54.00000000000000711 ) ) ;
#51293=VERTEX_POINT ( 'NONE', #57714 ) ;
#51296=ORIENTED_EDGE ( 'NONE', *, *, #43617, .F. ) ;
#51302=VERTEX_POINT ( 'NONE', #15293 ) ;
#51303=VECTOR ( 'NONE', #46320, 1000.000000000000000 ) ;
#51313=CIRCLE ( 'NONE', #1591, 0.1749999999999989342 ) ;
#51321=VECTOR ( 'NONE', #62367, 1000.000000000000000 ) ;
#51334=DIRECTION ( 'NONE',  ( -0.000000000000000000, -0.000000000000000000, -1.000000000000000000 ) ) ;
#51335=EDGE_CURVE ( 'NONE', #40788, #56650, #66797, .T. ) ;
#51345=DIRECTION ( 'NONE',  ( 0.000000000000000000, 1.000000000000000000, 0.000000000000000000 ) ) ;
#51346=EDGE_LOOP ( 'NONE', ( #17476, #26945, #14860, #26694 ) ) ;
#51357=CARTESIAN_POINT ( 'NONE',  ( -8.598420958951633608, -1.480523737882746271, 54.00000000000000711 ) ) ;
#51361=CARTESIAN_POINT ( 'NONE',  ( -8.697938382363103571, -2.420780051175099423, 54.00000000000000711 ) ) ;
#51372=VECTOR ( 'NONE', #32162, 1000.000000000000000 ) ;
#51378=VECTOR ( 'NONE', #35817, 1000.000000000000000 ) ;
#51389=LINE ( 'NONE', #40437, #57648 ) ;
#51392=DIRECTION ( 'NONE',  ( -7.304098846218132892E-15, -1.000000000000000000, 0.000000000000000000 ) ) ;
#51395=VERTEX_POINT ( 'NONE', #1116 ) ;
#51400=EDGE_CURVE ( 'NONE', #40232, #2123, #54175, .T. ) ;
#51404=EDGE_CURVE ( 'NONE', #30081, #58674, #10335, .T. ) ;
#51408=EDGE_CURVE ( 'NONE', #28592, #49752, #43196, .T. ) ;
#51418=VECTOR ( 'NONE', #28513, 1000.000000000000000 ) ;
#51422=EDGE_CURVE ( 'NONE', #66946, #31134, #1304, .T. ) ;
#51423=CARTESIAN_POINT ( 'NONE',  ( 3.677663764522608680, 6.350872789121272177, 54.00000000000000711 ) ) ;
#51425=DIRECTION ( 'NONE',  ( -0.000000000000000000, -0.000000000000000000, -1.000000000000000000 ) ) ;
#51435=CARTESIAN_POINT ( 'NONE',  ( 5.257023737882819070, -4.032023737882816761, 26.00000000000000711 ) ) ;
#51439=DIRECTION ( 'NONE',  ( 0.8660254037844562491, 0.4999999999999695244, 2.509347957447841320E-16 ) ) ;
#51440=FACE_OUTER_BOUND ( 'NONE', #31929, .T. ) ;
#51442=VECTOR ( 'NONE', #31187, 1000.000000000000000 ) ;
#51452=ORIENTED_EDGE ( 'NONE', *, *, #47815, .F. ) ;
#51457=PLANE ( 'NONE',  #17580 ) ;
#51458=DIRECTION ( 'NONE',  ( -9.912705577010336396E-15, -1.000000000000000000, 0.000000000000000000 ) ) ;
#51462=VERTEX_POINT ( 'NONE', #50234 ) ;
#51464=ORIENTED_EDGE ( 'NONE', *, *, #34942, .F. ) ;
#51465=ORIENTED_EDGE ( 'NONE', *, *, #55080, .F. ) ;
#51473=VERTEX_POINT ( 'NONE', #2140 ) ;
#51480=ORIENTED_EDGE ( 'NONE', *, *, #12782, .T. ) ;
#51481=EDGE_CURVE ( 'NONE', #37047, #24795, #9233, .T. ) ;
#51483=ORIENTED_EDGE ( 'NONE', *, *, #23473, .T. ) ;
#51488=ADVANCED_FACE ( 'NONE', ( #12731 ), #9108, .T. ) ;
#51492=ORIENTED_EDGE ( 'NONE', *, *, #41521, .T. ) ;
#51494=EDGE_CURVE ( 'NONE', #61865, #60944, #18386, .T. ) ;
#51498=CARTESIAN_POINT ( 'NONE',  ( -7.342976262117288933, -6.665817930929258672, 26.00000000000000000 ) ) ;
#51505=VECTOR ( 'NONE', #65859, 1000.000000000000000 ) ;
#51525=AXIS2_PLACEMENT_3D ( 'NONE', #54223, #10726, #16381 ) ;
#51526=VECTOR ( 'NONE', #58082, 1000.000000000000000 ) ;
#51532=ORIENTED_EDGE ( 'NONE', *, *, #53520, .T. ) ;
#51540=DIRECTION ( 'NONE',  ( 1.836970198721029934E-16, -1.836970198721036344E-16, 1.000000000000000000 ) ) ;
#51548=CARTESIAN_POINT ( 'NONE',  ( 3.664523737882781518, -10.31452373788281029, 54.00000000000000711 ) ) ;
#51557=DIRECTION ( 'NONE',  ( -0.7071067811865550112, -0.7071067811865401342, -2.597868168706466299E-16 ) ) ;
#51584=FACE_OUTER_BOUND ( 'NONE', #57638, .T. ) ;
#51585=ORIENTED_EDGE ( 'NONE', *, *, #48827, .T. ) ;
#51598=DIRECTION ( 'NONE',  ( 1.000000000000000000, 0.000000000000000000, 0.000000000000000000 ) ) ;
#51614=EDGE_LOOP ( 'NONE', ( #5841, #53173, #69407, #21851 ) ) ;
#51625=CIRCLE ( 'NONE', #45967, 0.5249999999999994671 ) ;
#51653=CARTESIAN_POINT ( 'NONE',  ( -8.821682069070746479, -2.369523737882742953, 54.00000000000000711 ) ) ;
#51657=EDGE_LOOP ( 'NONE', ( #12613, #45822, #998, #21619 ) ) ;
#51667=EDGE_LOOP ( 'NONE', ( #43047, #17135, #54634, #2605 ) ) ;
#51668=ORIENTED_EDGE ( 'NONE', *, *, #38625, .T. ) ;
#51679=CARTESIAN_POINT ( 'NONE',  ( 5.257023737882819070, -5.257023737882825287, 54.00000000000000711 ) ) ;
#51690=CARTESIAN_POINT ( 'NONE',  ( -7.342976262117252517, -3.848229544836288429, 54.00000000000000711 ) ) ;
#51696=ORIENTED_EDGE ( 'NONE', *, *, #50062, .F. ) ;
#51707=ORIENTED_EDGE ( 'NONE', *, *, #28619, .F. ) ;
#51708=LINE ( 'NONE', #19511, #36998 ) ;
#51721=CARTESIAN_POINT ( 'NONE',  ( -9.722976262117258628, 7.290476262117236317, 54.00000000000000711 ) ) ;
#51723=ORIENTED_EDGE ( 'NONE', *, *, #16070, .T. ) ;
#51724=VERTEX_POINT ( 'NONE', #52607 ) ;
#51725=CARTESIAN_POINT ( 'NONE',  ( 5.257023737882801306, 5.242976262117200470, 54.00000000000000711 ) ) ;
#51734=VECTOR ( 'NONE', #68789, 1000.000000000000000 ) ;
#51741=VERTEX_POINT ( 'NONE', #57892 ) ;
#51746=CARTESIAN_POINT ( 'NONE',  ( 8.835729544836331328, 8.130476262117188213, 54.00000000000000711 ) ) ;
#51760=ORIENTED_EDGE ( 'NONE', *, *, #22071, .T. ) ;
#51762=CARTESIAN_POINT ( 'NONE',  ( 8.144523737882817471, -9.562023737882817898, 54.00000000000000711 ) ) ;
#51768=VERTEX_POINT ( 'NONE', #9823 ) ;
#51777=CIRCLE ( 'NONE', #56306, 0.5249999999999990230 ) ;
#51778=DIRECTION ( 'NONE',  ( 0.6414496315691469164, -0.7671651518153087546, -2.587583378555128790E-16 ) ) ;
#51781=CARTESIAN_POINT ( 'NONE',  ( -2.355476262117325525, -9.562023737882830332, 54.00000000000000711 ) ) ;
#51793=LINE ( 'NONE', #47195, #45536 ) ;
#51794=DIRECTION ( 'NONE',  ( -1.000000000000000000, 3.491481338843133355E-15, 0.000000000000000000 ) ) ;
#51806=EDGE_CURVE ( 'NONE', #28114, #20102, #20068, .T. ) ;
#51813=EDGE_CURVE ( 'NONE', #67274, #59501, #39447, .T. ) ;
#51814=ORIENTED_EDGE ( 'NONE', *, *, #9942, .F. ) ;
#51816=ORIENTED_EDGE ( 'NONE', *, *, #30738, .T. ) ;
#51824=EDGE_LOOP ( 'NONE', ( #18576, #42266, #39163, #412 ) ) ;
#51845=LINE ( 'NONE', #24626, #24324 ) ;
#51847=EDGE_CURVE ( 'NONE', #23882, #15959, #66333, .T. ) ;
#51856=CARTESIAN_POINT ( 'NONE',  ( 8.580623737882849156, 9.689726262117156708, 54.00000000000000711 ) ) ;
#51859=VERTEX_POINT ( 'NONE', #43370 ) ;
#51873=CARTESIAN_POINT ( 'NONE',  ( -7.955476262117259445, 8.821682069070703847, 54.00000000000000711 ) ) ;
#51881=VERTEX_POINT ( 'NONE', #23187 ) ;
#51886=CARTESIAN_POINT ( 'NONE',  ( -7.955476262117259445, 8.821682069070703847, 26.00000000000000711 ) ) ;
#51894=CARTESIAN_POINT ( 'NONE',  ( 6.364920264886889001, 6.822336235477383326, 54.00000000000000711 ) ) ;
#51896=ADVANCED_FACE ( 'NONE', ( #1283 ), #16513, .T. ) ;
#51908=CARTESIAN_POINT ( 'NONE',  ( -10.30047626211725742, 3.650476262117184234, 54.00000000000000711 ) ) ;
#51910=DIRECTION ( 'NONE',  ( 0.000000000000000000, 1.000000000000000000, 0.000000000000000000 ) ) ;
#51928=CIRCLE ( 'NONE', #59848, 0.1749999999999998224 ) ;
#51932=FACE_OUTER_BOUND ( 'NONE', #58967, .T. ) ;
#51934=CARTESIAN_POINT ( 'NONE',  ( -10.49297626211729018, -6.849523737882743823, 26.00000000000000000 ) ) ;
#51946=CARTESIAN_POINT ( 'NONE',  ( -9.547976262117254365, 2.355476262117183417, 54.00000000000000711 ) ) ;
#51950=VECTOR ( 'NONE', #13990, 1000.000000000000000 ) ;
#51951=PLANE ( 'NONE',  #51047 ) ;
#51953=PLANE ( 'NONE',  #77 ) ;
#51955=ORIENTED_EDGE ( 'NONE', *, *, #52722, .T. ) ;
#51968=CARTESIAN_POINT ( 'NONE',  ( -3.650476262117221093, 10.49297626211717116, 54.00000000000000711 ) ) ;
#51978=CARTESIAN_POINT ( 'NONE',  ( -7.517976262117260333, 6.651770455163663165, 26.00000000000000711 ) ) ;
#51981=EDGE_CURVE ( 'NONE', #39378, #42765, #19284, .T. ) ;
#52004=AXIS2_PLACEMENT_3D ( 'NONE', #7893, #50685, #61993 ) ;
#52012=CARTESIAN_POINT ( 'NONE',  ( 8.711985858128693749, -8.093267424590459669, 26.00000000000000000 ) ) ;
#52023=VECTOR ( 'NONE', #26466, 1000.000000000000000 ) ;
#52026=DIRECTION ( 'NONE',  ( -1.203165845134433242E-14, -1.000000000000000000, -1.836970198721014403E-16 ) ) ;
#52052=DIRECTION ( 'NONE',  ( 0.000000000000000000, 0.000000000000000000, 1.000000000000000000 ) ) ;
#52054=VERTEX_POINT ( 'NONE', #36244 ) ;
#52055=DIRECTION ( 'NONE',  ( -0.7071067811865475727, 0.7071067811865475727, 0.000000000000000000 ) ) ;
#52066=ORIENTED_EDGE ( 'NONE', *, *, #43846, .F. ) ;
#52072=VECTOR ( 'NONE', #48732, 1000.000000000000000 ) ;
#52081=PLANE ( 'NONE',  #3856 ) ;
#52087=ORIENTED_EDGE ( 'NONE', *, *, #25832, .F. ) ;
#52088=LINE ( 'NONE', #14603, #23155 ) ;
#52098=FACE_OUTER_BOUND ( 'NONE', #66431, .T. ) ;
#52100=EDGE_LOOP ( 'NONE', ( #17988, #46975, #50793, #28686 ) ) ;
#52102=ORIENTED_EDGE ( 'NONE', *, *, #20212, .T. ) ;
#52115=CYLINDRICAL_SURFACE ( 'NONE', #20831, 0.7112000000000124889 ) ;
#52121=EDGE_LOOP ( 'NONE', ( #1317, #24736, #29915, #46322 ) ) ;
#52126=ORIENTED_EDGE ( 'NONE', *, *, #14971, .F. ) ;
#52127=DIRECTION ( 'NONE',  ( -0.000000000000000000, 3.673940397442059868E-16, -1.000000000000000000 ) ) ;
#52129=EDGE_CURVE ( 'NONE', #902, #68930, #47639, .T. ) ;
#52142=VECTOR ( 'NONE', #15966, 1000.000000000000000 ) ;
#52149=CARTESIAN_POINT ( 'NONE',  ( -8.566576262117260754, 8.916576262117214213, 54.00000000000000711 ) ) ;
#52154=EDGE_CURVE ( 'NONE', #32932, #31078, #21385, .T. ) ;
#52155=CARTESIAN_POINT ( 'NONE',  ( -3.663616288757085560, -4.149127210878725158, 26.00000000000000711 ) ) ;
#52160=ORIENTED_EDGE ( 'NONE', *, *, #4505, .T. ) ;
#52170=EDGE_CURVE ( 'NONE', #2772, #37989, #4086, .T. ) ;
#52171=LINE ( 'NONE', #19997, #29761 ) ;
#52175=ORIENTED_EDGE ( 'NONE', *, *, #37663, .T. ) ;
#52186=CIRCLE ( 'NONE', #31760, 0.1749999999999993783 ) ;
#52187=LINE ( 'NONE', #9052, #66170 ) ;
#52196=ORIENTED_EDGE ( 'NONE', *, *, #18524, .T. ) ;
#52213=DIRECTION ( 'NONE',  ( -1.000000000000000000, 0.000000000000000000, 0.000000000000000000 ) ) ;
#52216=CARTESIAN_POINT ( 'NONE',  ( 8.612468434717182930, 1.466476262117163865, 54.00000000000000711 ) ) ;
#52217=EDGE_CURVE ( 'NONE', #11146, #56487, #42247, .T. ) ;
#52221=DIRECTION ( 'NONE',  ( -0.000000000000000000, -0.000000000000000000, -1.000000000000000000 ) ) ;
#52225=LINE ( 'NONE', #35596, #66225 ) ;
#52226=VECTOR ( 'NONE', #30161, 1000.000000000000114 ) ;
#52227=EDGE_CURVE ( 'NONE', #12509, #63544, #7036, .T. ) ;
#52229=CARTESIAN_POINT ( 'NONE',  ( -10.30047626211725742, 3.842976262117182351, 54.00000000000000711 ) ) ;
#52234=ADVANCED_FACE ( 'NONE', ( #11458 ), #11119, .F. ) ;
#52235=DIRECTION ( 'NONE',  ( 0.4999999999999695799, -0.8660254037844563602, -6.723777587269172655E-17 ) ) ;
#52253=EDGE_CURVE ( 'NONE', #58636, #54732, #5827, .T. ) ;
#52257=DIRECTION ( 'NONE',  ( -0.000000000000000000, -0.000000000000000000, -1.000000000000000000 ) ) ;
#52282=CARTESIAN_POINT ( 'NONE',  ( 8.711985858128681315, 8.079219948824839292, 26.00000000000000711 ) ) ;
#52284=ORIENTED_EDGE ( 'NONE', *, *, #59186, .F. ) ;
#52298=EDGE_CURVE ( 'NONE', #7002, #29126, #21732, .T. ) ;
#52302=EDGE_CURVE ( 'NONE', #57627, #65232, #64874, .T. ) ;
#52307=CARTESIAN_POINT ( 'NONE',  ( -6.642976262117260333, 10.30047626211718104, 26.00000000000000711 ) ) ;
#52313=EDGE_CURVE ( 'NONE', #22714, #31391, #16433, .T. ) ;
#52316=DIRECTION ( 'NONE',  ( -0.000000000000000000, 3.673940397442059868E-16, -1.000000000000000000 ) ) ;
#52321=ADVANCED_FACE ( 'NONE', ( #49312 ), #6163, .T. ) ;
#52322=DIRECTION ( 'NONE',  ( -1.000000000000000000, 0.000000000000000000, 0.000000000000000000 ) ) ;
#52332=ORIENTED_EDGE ( 'NONE', *, *, #32966, .F. ) ;
#52334=CARTESIAN_POINT ( 'NONE',  ( 3.724485858128677940, -7.408280051175165859, 54.00000000000000711 ) ) ;
#52358=LINE ( 'NONE', #20520, #28533 ) ;
#52366=ORIENTED_EDGE ( 'NONE', *, *, #28567, .F. ) ;
#52367=DIRECTION ( 'NONE',  ( 1.000000000000000000, 0.000000000000000000, 0.000000000000000000 ) ) ;
#52373=ORIENTED_EDGE ( 'NONE', *, *, #52298, .F. ) ;
#52376=DIRECTION ( 'NONE',  ( 1.000000000000000000, -2.309061475090597584E-14, 1.836970198720987533E-16 ) ) ;
#52378=ORIENTED_EDGE ( 'NONE', *, *, #9558, .F. ) ;
#52380=EDGE_CURVE ( 'NONE', #45362, #35367, #56333, .T. ) ;
#52383=EDGE_CURVE ( 'NONE', #61211, #69660, #45361, .T. ) ;
#52385=EDGE_CURVE ( 'NONE', #18784, #37577, #35448, .T. ) ;
#52392=PLANE ( 'NONE',  #41678 ) ;
#52394=ORIENTED_EDGE ( 'NONE', *, *, #28057, .T. ) ;
#52406=EDGE_LOOP ( 'NONE', ( #53039, #13260, #21239, #7190, #3822, #40080, #1711, #16626, #14458, #2214, #14127, #17730, #29658, #15920, #60852, #68372, #36515 ) ) ;
#52410=DIRECTION ( 'NONE',  ( -0.7071067811865474617, -0.7071067811865474617, 0.000000000000000000 ) ) ;
#52411=AXIS2_PLACEMENT_3D ( 'NONE', #40021, #23780, #45333 ) ;
#52420=CARTESIAN_POINT ( 'NONE',  ( -6.350872789121319251, -3.677663764522589140, 54.00000000000000711 ) ) ;
#52422=LINE ( 'NONE', #3981, #69357 ) ;
#52423=DIRECTION ( 'NONE',  ( -0.000000000000000000, 3.673940397442059868E-16, -1.000000000000000000 ) ) ;
#52424=ORIENTED_EDGE ( 'NONE', *, *, #57271, .F. ) ;
#52436=DIRECTION ( 'NONE',  ( 3.596772705736696467E-15, 1.000000000000000000, 0.000000000000000000 ) ) ;
#52446=DIRECTION ( 'NONE',  ( 0.000000000000000000, -1.000000000000000000, 0.000000000000000000 ) ) ;
#52447=AXIS2_PLACEMENT_3D ( 'NONE', #28683, #61192, #54890 ) ;
#52449=EDGE_LOOP ( 'NONE', ( #68553, #29837, #21243, #8606 ) ) ;
#52450=ORIENTED_EDGE ( 'NONE', *, *, #827, .T. ) ;
#52452=DIRECTION ( 'NONE',  ( -0.000000000000000000, -0.000000000000000000, -1.000000000000000000 ) ) ;
#52475=FACE_OUTER_BOUND ( 'NONE', #521, .T. ) ;
#52493=CARTESIAN_POINT ( 'NONE',  ( 9.703773737882785966, -9.703773737882814387, 26.00000000000000000 ) ) ;
#52495=CARTESIAN_POINT ( 'NONE',  ( -10.03972626211722918, 8.916576262117214213, 54.00000000000000711 ) ) ;
#52509=CARTESIAN_POINT ( 'NONE',  ( -4.706725378239257296, -6.358413763958960629, 54.00000000000000711 ) ) ;
#52516=ORIENTED_EDGE ( 'NONE', *, *, #58742, .T. ) ;
#52526=CARTESIAN_POINT ( 'NONE',  ( -8.916576262117343887, -8.930623737882761759, 26.00000000000000000 ) ) ;
#52527=CARTESIAN_POINT ( 'NONE',  ( 3.857023737882779635, -10.31452373788280141, 26.00000000000000000 ) ) ;
#52530=CYLINDRICAL_SURFACE ( 'NONE', #46071, 1.224999999999998757 ) ;
#52533=CARTESIAN_POINT ( 'NONE',  ( -10.49297626211729551, -6.849523737882748264, 54.00000000000000711 ) ) ;
#52535=ORIENTED_EDGE ( 'NONE', *, *, #61879, .F. ) ;
#52536=VECTOR ( 'NONE', #50315, 1000.000000000000000 ) ;
#52537=ORIENTED_EDGE ( 'NONE', *, *, #51422, .T. ) ;
#52544=LINE ( 'NONE', #25319, #25555 ) ;
#52549=AXIS2_PLACEMENT_3D ( 'NONE', #62963, #14516, #13460 ) ;
#52552=VERTEX_POINT ( 'NONE', #3645 ) ;
#52553=VECTOR ( 'NONE', #46949, 1000.000000000000000 ) ;
#52555=FACE_OUTER_BOUND ( 'NONE', #48882, .T. ) ;
#52557=DIRECTION ( 'NONE',  ( 0.7671651518153006499, -0.6414496315691565753, -2.356647714346250026E-16 ) ) ;
#52568=LINE ( 'NONE', #59611, #61822 ) ;
#52573=FACE_OUTER_BOUND ( 'NONE', #41628, .T. ) ;
#52577=CARTESIAN_POINT ( 'NONE',  ( -4.031976262117261456, 3.142976262117183506, 54.00000000000000711 ) ) ;
#52587=CARTESIAN_POINT ( 'NONE',  ( -6.350872789121327244, 6.822336235477381550, 54.00000000000000711 ) ) ;
#52607=CARTESIAN_POINT ( 'NONE',  ( -9.915476262117195461, -0.9555237378827157180, 26.00000000000000711 ) ) ;
#52614=ORIENTED_EDGE ( 'NONE', *, *, #25832, .T. ) ;
#52628=ORIENTED_EDGE ( 'NONE', *, *, #2090, .T. ) ;
#52630=ADVANCED_FACE ( 'NONE', ( #58450 ), #52081, .T. ) ;
#52632=DIRECTION ( 'NONE',  ( 9.799566706031580591E-15, 1.000000000000000000, 1.836970198721018348E-16 ) ) ;
#52636=CARTESIAN_POINT ( 'NONE',  ( 10.50702373788281818, -9.795823737882802362, 26.00000000000000000 ) ) ;
#52649=VERTEX_POINT ( 'NONE', #41109 ) ;
#52650=VECTOR ( 'NONE', #41507, 999.9999999999998863 ) ;
#52655=LINE ( 'NONE', #64563, #64215 ) ;
#52664=CARTESIAN_POINT ( 'NONE',  ( -10.49297626211725110, -3.664523737882711352, 54.00000000000000711 ) ) ;
#52665=LINE ( 'NONE', #3511, #58429 ) ;
#52675=LINE ( 'NONE', #64320, #7387 ) ;
#52680=CARTESIAN_POINT ( 'NONE',  ( -9.547976262117254365, 8.130476262117182884, 54.00000000000000711 ) ) ;
#52681=ORIENTED_EDGE ( 'NONE', *, *, #64380, .F. ) ;
#52682=CARTESIAN_POINT ( 'NONE',  ( -4.141586236041129077, -4.720772854004773755, 54.00000000000000711 ) ) ;
#52693=ORIENTED_EDGE ( 'NONE', *, *, #63477, .T. ) ;
#52695=LINE ( 'NONE', #57631, #54014 ) ;
#52696=VECTOR ( 'NONE', #22762, 1000.000000000000000 ) ;
#52698=CARTESIAN_POINT ( 'NONE',  ( -3.834182069070823040, -7.357023737882818715, 54.00000000000000711 ) ) ;
#52703=ORIENTED_EDGE ( 'NONE', *, *, #27187, .T. ) ;
#52713=CYLINDRICAL_SURFACE ( 'NONE', #15160, 0.1749999999999998224 ) ;
#52715=ADVANCED_FACE ( 'NONE', ( #37574 ), #69751, .F. ) ;
#52720=LINE ( 'NONE', #48442, #61446 ) ;
#52721=ORIENTED_EDGE ( 'NONE', *, *, #11108, .F. ) ;
#52722=EDGE_CURVE ( 'NONE', #3304, #69903, #16702, .T. ) ;
#52730=DIRECTION ( 'NONE',  ( -0.000000000000000000, -0.000000000000000000, -1.000000000000000000 ) ) ;
#52735=DIRECTION ( 'NONE',  ( 1.836970198721029934E-16, 1.836970198721010706E-16, -1.000000000000000000 ) ) ;
#52738=ADVANCED_FACE ( 'NONE', ( #43210 ), #59482, .T. ) ;
#52748=ORIENTED_EDGE ( 'NONE', *, *, #24145, .F. ) ;
#52759=CARTESIAN_POINT ( 'NONE',  ( 3.157023737882800329, 6.486996718459884903, 26.00000000000000711 ) ) ;
#52764=EDGE_CURVE ( 'NONE', #37068, #69196, #54878, .T. ) ;
#52768=CARTESIAN_POINT ( 'NONE',  ( 5.257023737882801306, 5.242976262117200470, 54.00000000000000711 ) ) ;
#52784=VERTEX_POINT ( 'NONE', #60846 ) ;
#52792=CARTESIAN_POINT ( 'NONE',  ( -9.547976262117254365, 2.355476262117183417, 26.00000000000000711 ) ) ;
#52799=CARTESIAN_POINT ( 'NONE',  ( 8.612468434717188259, 1.991476262117162888, 54.00000000000000711 ) ) ;
#52801=CARTESIAN_POINT ( 'NONE',  ( 10.50702373788278265, 3.650476262117142934, 54.00000000000000711 ) ) ;
#52806=EDGE_CURVE ( 'NONE', #37820, #51075, #2154, .T. ) ;
#52815=DIRECTION ( 'NONE',  ( 0.5000000000000004441, -0.8660254037844383745, 0.000000000000000000 ) ) ;
#52833=ORIENTED_EDGE ( 'NONE', *, *, #47671, .F. ) ;
#52839=ORIENTED_EDGE ( 'NONE', *, *, #21341, .F. ) ;
#52841=CARTESIAN_POINT ( 'NONE',  ( -6.822336235477446387, 6.350872789121265072, 54.00000000000000711 ) ) ;
#52844=PLANE ( 'NONE',  #37277 ) ;
#52848=EDGE_CURVE ( 'NONE', #15217, #50527, #8370, .T. ) ;
#52850=LINE ( 'NONE', #47519, #24401 ) ;
#52860=CARTESIAN_POINT ( 'NONE',  ( -4.706725378239217328, 4.141586236041038482, 26.00000000000000711 ) ) ;
#52863=LINE ( 'NONE', #25981, #18539 ) ;
#52865=FACE_OUTER_BOUND ( 'NONE', #8589, .T. ) ;
#52875=DIRECTION ( 'NONE',  ( 2.135044278125299371E-15, 1.000000000000000000, 0.000000000000000000 ) ) ;
#52879=ADVANCED_BREP_SHAPE_REPRESENTATION ( '', ( #21410, #45918 ), #44782 ) ;
#52880=VECTOR ( 'NONE', #41161, 1000.000000000000000 ) ;
#52892=EDGE_CURVE ( 'NONE', #28725, #34946, #29366, .T. ) ;
#52894=EDGE_CURVE ( 'NONE', #22289, #45362, #2499, .T. ) ;
#52895=ADVANCED_FACE ( 'NONE', ( #24429 ), #56937, .T. ) ;
#52904=VERTEX_POINT ( 'NONE', #47045 ) ;
#52910=LINE ( 'NONE', #4114, #59352 ) ;
#52914=CARTESIAN_POINT ( 'NONE',  ( -4.135079735113167843, 6.822336235477362010, 54.00000000000000711 ) ) ;
#52915=DIRECTION ( 'NONE',  ( -0.000000000000000000, -0.000000000000000000, -1.000000000000000000 ) ) ;
#52916=VERTEX_POINT ( 'NONE', #41384 ) ;
#52921=VERTEX_POINT ( 'NONE', #4621 ) ;
#52922=VECTOR ( 'NONE', #658, 1000.000000000000114 ) ;
#52923=EDGE_CURVE ( 'NONE', #22860, #10855, #12909, .T. ) ;
#52924=DIRECTION ( 'NONE',  ( 1.000000000000000000, -8.339399738404101090E-15, 0.000000000000000000 ) ) ;
#52929=DIRECTION ( 'NONE',  ( -0.8660254037844400399, -0.4999999999999973910, 6.723777587268495961E-17 ) ) ;
#52930=DIRECTION ( 'NONE',  ( -1.000000000000000000, 1.047444401652940007E-14, -1.836970198721010952E-16 ) ) ;
#52940=LINE ( 'NONE', #31000, #46978 ) ;
#52943=CARTESIAN_POINT ( 'NONE',  ( -3.663616288757055806, 4.135079735113128763, 54.00000000000000711 ) ) ;
#52953=ORIENTED_EDGE ( 'NONE', *, *, #20583, .T. ) ;
#52963=VERTEX_POINT ( 'NONE', #57997 ) ;
#52970=AXIS2_PLACEMENT_3D ( 'NONE', #65180, #3407, #10036 ) ;
#52971=DIRECTION ( 'NONE',  ( -1.836970198721029934E-16, -1.836970198721010706E-16, 1.000000000000000000 ) ) ;
#52978=CIRCLE ( 'NONE', #1035, 0.5249999999999994671 ) ;
#52981=ORIENTED_EDGE ( 'NONE', *, *, #13480, .T. ) ;
#52982=VERTEX_POINT ( 'NONE', #51653 ) ;
#52983=ORIENTED_EDGE ( 'NONE', *, *, #67652, .F. ) ;
#52986=EDGE_CURVE ( 'NONE', #63705, #38341, #31494, .T. ) ;
#52994=ORIENTED_EDGE ( 'NONE', *, *, #45749, .T. ) ;
#53007=DIRECTION ( 'NONE',  ( -2.135044278125299371E-15, -1.000000000000000000, -3.673940397442060361E-16 ) ) ;
#53011=CYLINDRICAL_SURFACE ( 'NONE', #8131, 0.1749999999999998224 ) ;
#53012=DIRECTION ( 'NONE',  ( 0.7071067811865474617, 0.7071067811865474617, 2.597868168706479611E-16 ) ) ;
#53014=EDGE_CURVE ( 'NONE', #69896, #58380, #19733, .T. ) ;
#53023=ORIENTED_EDGE ( 'NONE', *, *, #44047, .T. ) ;
#53025=CARTESIAN_POINT ( 'NONE',  ( 4.149127210878741145, 3.663616288756999406, 54.00000000000000711 ) ) ;
#53029=VERTEX_POINT ( 'NONE', #14872 ) ;
#53039=ORIENTED_EDGE ( 'NONE', *, *, #25074, .F. ) ;
#53041=CARTESIAN_POINT ( 'NONE',  ( 6.501044194225490180, -3.157023737882824754, 54.00000000000000711 ) ) ;
#53050=VERTEX_POINT ( 'NONE', #63669 ) ;
#53052=CIRCLE ( 'NONE', #29280, 0.1749999999999980738 ) ;
#53053=ORIENTED_EDGE ( 'NONE', *, *, #36276, .T. ) ;
#53074=CARTESIAN_POINT ( 'NONE',  ( 5.552858015815571591, 7.342976262117199227, 54.00000000000000711 ) ) ;
#53075=EDGE_CURVE ( 'NONE', #29966, #42141, #27916, .T. ) ;
#53084=ORIENTED_EDGE ( 'NONE', *, *, #18629, .T. ) ;
#53091=DIRECTION ( 'NONE',  ( -2.135044278125299371E-15, -1.000000000000000000, 0.000000000000000000 ) ) ;
#53107=ADVANCED_FACE ( 'NONE', ( #38192 ), #16959, .F. ) ;
#53112=DIRECTION ( 'NONE',  ( -0.000000000000000000, -0.000000000000000000, -1.000000000000000000 ) ) ;
#53113=EDGE_CURVE ( 'NONE', #3391, #6834, #49132, .T. ) ;
#53125=CARTESIAN_POINT ( 'NONE',  ( 6.836383711242975281, 4.135079735113102117, 54.00000000000000711 ) ) ;
#53129=ADVANCED_FACE ( 'NONE', ( #64359 ), #17288, .F. ) ;
#53132=DIRECTION ( 'NONE',  ( -0.7071067811865514585, -0.7071067811865435759, -2.597868168706465806E-16 ) ) ;
#53134=DIRECTION ( 'NONE',  ( 0.000000000000000000, 1.000000000000000000, 0.000000000000000000 ) ) ;
#53136=EDGE_CURVE ( 'NONE', #9829, #29192, #64697, .T. ) ;
#53153=DIRECTION ( 'NONE',  ( 0.7071067811865348052, -0.7071067811865602293, -3.278703137324831017E-30 ) ) ;
#53159=LINE ( 'NONE', #68353, #51378 ) ;
#53161=DIRECTION ( 'NONE',  ( 0.000000000000000000, -1.000000000000000000, 0.000000000000000000 ) ) ;
#53163=ADVANCED_FACE ( 'NONE', ( #18316 ), #34925, .F. ) ;
#53165=VECTOR ( 'NONE', #36576, 1000.000000000000000 ) ;
#53168=ORIENTED_EDGE ( 'NONE', *, *, #57607, .T. ) ;
#53173=ORIENTED_EDGE ( 'NONE', *, *, #32301, .F. ) ;
#53180=DIRECTION ( 'NONE',  ( 1.836970198721029934E-16, -1.836970198721036344E-16, 1.000000000000000000 ) ) ;
#53187=LINE ( 'NONE', #30200, #52650 ) ;
#53190=EDGE_CURVE ( 'NONE', #19581, #27218, #50157, .T. ) ;
#53192=ORIENTED_EDGE ( 'NONE', *, *, #39034, .F. ) ;
#53200=EDGE_CURVE ( 'NONE', #27591, #55844, #29628, .T. ) ;
#53211=DIRECTION ( 'NONE',  ( -0.7071067811865550112, -0.7071067811865401342, -2.597868168706467285E-16 ) ) ;
#53227=ORIENTED_EDGE ( 'NONE', *, *, #17230, .T. ) ;
#53230=PLANE ( 'NONE',  #48199 ) ;
#53240=LINE ( 'NONE', #57466, #61385 ) ;
#53244=VECTOR ( 'NONE', #44344, 1000.000000000000000 ) ;
#53246=ORIENTED_EDGE ( 'NONE', *, *, #4985, .T. ) ;
#53251=ORIENTED_EDGE ( 'NONE', *, *, #20212, .F. ) ;
#53273=CARTESIAN_POINT ( 'NONE',  ( -3.650476262117221093, 10.49297626211717116, 54.00000000000000711 ) ) ;
#53280=DIRECTION ( 'NONE',  ( 2.135044278125299371E-15, -1.000000000000000000, -3.673940397442060361E-16 ) ) ;
#53281=EDGE_CURVE ( 'NONE', #43741, #57348, #40938, .T. ) ;
#53292=DIRECTION ( 'NONE',  ( -1.000000000000000000, 0.000000000000000000, 0.000000000000000000 ) ) ;
#53297=DIRECTION ( 'NONE',  ( 0.8660254037844322683, -0.5000000000000111022, 6.723777587268230953E-17 ) ) ;
#53298=LINE ( 'NONE', #10491, #59059 ) ;
#53299=DIRECTION ( 'NONE',  ( -0.6414496315691645689, -0.7671651518152939886, -2.587583378555115478E-16 ) ) ;
#53304=DIRECTION ( 'NONE',  ( 0.7071067811865451302, -0.7071067811865500152, -2.597868168706484541E-16 ) ) ;
#53305=DIRECTION ( 'NONE',  ( -1.000000000000000000, -0.000000000000000000, -0.000000000000000000 ) ) ;
#53310=VECTOR ( 'NONE', #44392, 1000.000000000000000 ) ;
#53311=CIRCLE ( 'NONE', #16053, 0.5249999999999990230 ) ;
#53323=EDGE_CURVE ( 'NONE', #2395, #61211, #36342, .T. ) ;
#53324=LINE ( 'NONE', #68529, #23365 ) ;
#53330=VERTEX_POINT ( 'NONE', #46591 ) ;
#53335=LINE ( 'NONE', #9484, #27483 ) ;
#53342=VECTOR ( 'NONE', #48367, 1000.000000000000000 ) ;
#53347=VECTOR ( 'NONE', #21175, 1000.000000000000000 ) ;
#53354=ORIENTED_EDGE ( 'NONE', *, *, #37438, .F. ) ;
#53360=CARTESIAN_POINT ( 'NONE',  ( -6.817976262117321440, -9.737023737882781305, 26.00000000000000000 ) ) ;
#53369=AXIS2_PLACEMENT_3D ( 'NONE', #53922, #32343, #6158 ) ;
#53379=CARTESIAN_POINT ( 'NONE',  ( -8.916576262117349216, -8.930623737882767088, 54.00000000000000711 ) ) ;
#53382=DIRECTION ( 'NONE',  ( -0.000000000000000000, -0.000000000000000000, -1.000000000000000000 ) ) ;
#53384=EDGE_CURVE ( 'NONE', #4139, #63093, #26099, .T. ) ;
#53396=ORIENTED_EDGE ( 'NONE', *, *, #9468, .T. ) ;
#53397=AXIS2_PLACEMENT_3D ( 'NONE', #27429, #929, #11496 ) ;
#53401=DIRECTION ( 'NONE',  ( 0.000000000000000000, -3.673940397442059868E-16, 1.000000000000000000 ) ) ;
#53407=DIRECTION ( 'NONE',  ( 0.7071067811865527908, 0.7071067811865422437, 0.000000000000000000 ) ) ;
#53412=ORIENTED_EDGE ( 'NONE', *, *, #36690, .T. ) ;
#53413=EDGE_CURVE ( 'NONE', #14823, #18830, #21138, .T. ) ;
#53415=DIRECTION ( 'NONE',  ( -0.000000000000000000, 3.673940397442059868E-16, -1.000000000000000000 ) ) ;
#53417=VERTEX_POINT ( 'NONE', #43384 ) ;
#53427=AXIS2_PLACEMENT_3D ( 'NONE', #48041, #38479, #37783 ) ;
#53429=EDGE_LOOP ( 'NONE', ( #16405, #66837, #67869, #42773 ) ) ;
#53432=CARTESIAN_POINT ( 'NONE',  ( -10.03972626211732688, -9.703773737882722017, 54.00000000000000711 ) ) ;
#53435=CYLINDRICAL_SURFACE ( 'NONE', #1845, 0.5249999999999994671 ) ;
#53447=EDGE_CURVE ( 'NONE', #53029, #61001, #10520, .T. ) ;
#53453=EDGE_CURVE ( 'NONE', #23904, #10855, #58621, .T. ) ;
#53487=CARTESIAN_POINT ( 'NONE',  ( 9.562023737882759278, 2.355476262117158104, 26.00000000000000711 ) ) ;
#53491=VERTEX_POINT ( 'NONE', #33729 ) ;
#53513=EDGE_CURVE ( 'NONE', #6935, #63729, #6708, .T. ) ;
#53518=AXIS2_PLACEMENT_3D ( 'NONE', #45987, #3560, #3208 ) ;
#53520=EDGE_CURVE ( 'NONE', #61120, #36648, #44671, .T. ) ;
#53526=VECTOR ( 'NONE', #65597, 1000.000000000000000 ) ;
#53527=DIRECTION ( 'NONE',  ( -1.062075597536821205E-14, -1.000000000000000000, 0.000000000000000000 ) ) ;
#53533=CARTESIAN_POINT ( 'NONE',  ( 9.703773737882817940, 10.03972626211715280, 54.00000000000000711 ) ) ;
#53539=DIRECTION ( 'NONE',  ( -5.163402228214836012E-15, -1.000000000000000000, -1.836970198721026976E-16 ) ) ;
#53545=EDGE_CURVE ( 'NONE', #10010, #8859, #60273, .T. ) ;
#53546=ORIENTED_EDGE ( 'NONE', *, *, #38883, .T. ) ;
#53548=CARTESIAN_POINT ( 'NONE',  ( 6.832023737882815695, 9.722976262117192903, 54.00000000000000711 ) ) ;
#53558=CARTESIAN_POINT ( 'NONE',  ( 9.562023737882814345, -2.544523737882825820, 54.00000000000000711 ) ) ;
#53559=CARTESIAN_POINT ( 'NONE',  ( -10.49297626211726175, 6.835476262117182955, 54.00000000000000711 ) ) ;
#53568=ORIENTED_EDGE ( 'NONE', *, *, #21028, .T. ) ;
#53576=VECTOR ( 'NONE', #22938, 1000.000000000000000 ) ;
#53589=ORIENTED_EDGE ( 'NONE', *, *, #25569, .F. ) ;
#53605=ADVANCED_FACE ( 'NONE', ( #34793 ), #66970, .F. ) ;
#53608=EDGE_LOOP ( 'NONE', ( #42749, #10534, #37983, #33188 ) ) ;
#53624=ADVANCED_FACE ( 'NONE', ( #63077 ), #25250, .T. ) ;
#53635=EDGE_LOOP ( 'NONE', ( #29823, #59256, #5919, #616 ) ) ;
#53640=LINE ( 'NONE', #31726, #36495 ) ;
#53648=CARTESIAN_POINT ( 'NONE',  ( -2.617976262117251540, 6.486996718459834277, 26.00000000000000711 ) ) ;
#53659=CARTESIAN_POINT ( 'NONE',  ( -2.530476262117233865, 8.821682069070682530, 54.00000000000000711 ) ) ;
#53663=ORIENTED_EDGE ( 'NONE', *, *, #25563, .F. ) ;
#53664=VERTEX_POINT ( 'NONE', #63432 ) ;
#53678=CARTESIAN_POINT ( 'NONE',  ( -3.667976262117228714, 9.722976262117169810, 26.00000000000000711 ) ) ;
#53683=VERTEX_POINT ( 'NONE', #14297 ) ;
#53690=FACE_OUTER_BOUND ( 'NONE', #26665, .T. ) ;
#53692=CARTESIAN_POINT ( 'NONE',  ( -4.141586236041100655, 5.779227145995200488, 54.00000000000000711 ) ) ;
#53693=DIRECTION ( 'NONE',  ( -1.836970198721029934E-16, 1.836970198721036590E-16, -1.000000000000000000 ) ) ;
#53697=DIRECTION ( 'NONE',  ( -1.062075597536822467E-14, -1.000000000000000000, 0.000000000000000000 ) ) ;
#53701=CIRCLE ( 'NONE', #2854, 0.1749999999999998224 ) ;
#53715=EDGE_CURVE ( 'NONE', #30081, #37047, #58123, .T. ) ;
#53720=EDGE_LOOP ( 'NONE', ( #2792, #43844, #62215, #65761 ) ) ;
#53727=CARTESIAN_POINT ( 'NONE',  ( 4.155633711806649089, 5.779227145995230686, 54.00000000000000711 ) ) ;
#53735=ORIENTED_EDGE ( 'NONE', *, *, #44785, .F. ) ;
#53736=VECTOR ( 'NONE', #1763, 1000.000000000000114 ) ;
#53743=ORIENTED_EDGE ( 'NONE', *, *, #40418, .T. ) ;
#53745=ADVANCED_FACE ( 'NONE', ( #52475 ), #52844, .F. ) ;
#53753=DIRECTION ( 'NONE',  ( -1.836970198721029934E-16, -1.836970198721010706E-16, 1.000000000000000000 ) ) ;
#53755=EDGE_LOOP ( 'NONE', ( #62418, #22648, #5734, #25311 ) ) ;
#53764=CARTESIAN_POINT ( 'NONE',  ( -1.991476262117315432, -8.612468434717262866, 54.00000000000000711 ) ) ;
#53768=CARTESIAN_POINT ( 'NONE',  ( -7.342976262117269393, -4.961189459949999936, 26.00000000000000711 ) ) ;
#53772=DIRECTION ( 'NONE',  ( -0.000000000000000000, 3.673940397442059868E-16, -1.000000000000000000 ) ) ;
#53774=ORIENTED_EDGE ( 'NONE', *, *, #48788, .T. ) ;
#53777=CARTESIAN_POINT ( 'NONE',  ( -0.9414762621172249046, 9.915476262117151052, 54.00000000000000711 ) ) ;
#53784=DIRECTION ( 'NONE',  ( 0.000000000000000000, 3.673940397442059868E-16, -1.000000000000000000 ) ) ;
#53786=VECTOR ( 'NONE', #65357, 1000.000000000000000 ) ;
#53802=EDGE_CURVE ( 'NONE', #34368, #62916, #5449, .T. ) ;
#53822=ORIENTED_EDGE ( 'NONE', *, *, #21781, .T. ) ;
#53826=LINE ( 'NONE', #6070, #38779 ) ;
#53827=AXIS2_PLACEMENT_3D ( 'NONE', #34223, #66763, #12310 ) ;
#53828=VECTOR ( 'NONE', #59419, 1000.000000000000000 ) ;
#53837=CARTESIAN_POINT ( 'NONE',  ( 9.912023737882815766, -6.832023737882813919, 26.00000000000000000 ) ) ;
#53838=CARTESIAN_POINT ( 'NONE',  ( 2.544523737882817382, 9.547976262117206403, 54.00000000000000711 ) ) ;
#53840=CARTESIAN_POINT ( 'NONE',  ( 5.257023737882801306, 5.242976262117200470, 54.00000000000000711 ) ) ;
#53849=CYLINDRICAL_SURFACE ( 'NONE', #10647, 0.1749999999999989342 ) ;
#53856=EDGE_CURVE ( 'NONE', #5174, #37532, #31956, .T. ) ;
#53862=AXIS2_PLACEMENT_3D ( 'NONE', #39824, #51143, #29213 ) ;
#53865=VERTEX_POINT ( 'NONE', #42904 ) ;
#53873=VECTOR ( 'NONE', #60298, 1000.000000000000000 ) ;
#53876=DIRECTION ( 'NONE',  ( -0.000000000000000000, -0.000000000000000000, -1.000000000000000000 ) ) ;
#53878=ORIENTED_EDGE ( 'NONE', *, *, #43052, .T. ) ;
#53892=CARTESIAN_POINT ( 'NONE',  ( -7.394232575409614761, 6.775514141871308738, 54.00000000000000711 ) ) ;
#53900=CARTESIAN_POINT ( 'NONE',  ( -9.897976262117259338, 6.642976262117183950, 26.00000000000000711 ) ) ;
#53901=CARTESIAN_POINT ( 'NONE',  ( -5.242976262117259978, 5.242976262117182706, 26.00000000000000711 ) ) ;
#53902=ORIENTED_EDGE ( 'NONE', *, *, #36287, .F. ) ;
#53910=AXIS2_PLACEMENT_3D ( 'NONE', #22208, #38796, #23225 ) ;
#53912=EDGE_CURVE ( 'NONE', #2504, #64281, #48564, .T. ) ;
#53914=ORIENTED_EDGE ( 'NONE', *, *, #11468, .T. ) ;
#53922=CARTESIAN_POINT ( 'NONE',  ( 8.612468434717241550, -2.005523737882815460, 26.00000000000000711 ) ) ;
#53924=CIRCLE ( 'NONE', #1957, 0.3499999999999996447 ) ;
#53934=DIRECTION ( 'NONE',  ( 0.000000000000000000, 0.000000000000000000, 1.000000000000000000 ) ) ;
#53937=ORIENTED_EDGE ( 'NONE', *, *, #48178, .T. ) ;
#53945=EDGE_CURVE ( 'NONE', #58511, #40726, #1494, .T. ) ;
#53947=ORIENTED_EDGE ( 'NONE', *, *, #36264, .F. ) ;
#53951=CARTESIAN_POINT ( 'NONE',  ( -9.547976262117222390, -2.369523737882729186, 54.00000000000000711 ) ) ;
#53956=VECTOR ( 'NONE', #25330, 1000.000000000000000 ) ;
#53961=CARTESIAN_POINT ( 'NONE',  ( -4.706725378239216440, 6.344366288193329595, 26.00000000000000711 ) ) ;
#53972=DIRECTION ( 'NONE',  ( -0.000000000000000000, 1.000000000000000000, 3.673940397442059868E-16 ) ) ;
#53974=LINE ( 'NONE', #33083, #42945 ) ;
#53979=CYLINDRICAL_SURFACE ( 'NONE', #67683, 0.1749999999999998224 ) ;
#53980=FACE_OUTER_BOUND ( 'NONE', #41925, .T. ) ;
#53983=CARTESIAN_POINT ( 'NONE',  ( -7.955476262117326947, -9.737023737882770646, 54.00000000000000711 ) ) ;
#53984=ORIENTED_EDGE ( 'NONE', *, *, #43723, .T. ) ;
#53997=AXIS2_PLACEMENT_3D ( 'NONE', #58426, #47790, #31548 ) ;
#54000=CARTESIAN_POINT ( 'NONE',  ( 3.857023737882779635, -10.31452373788281029, 54.00000000000000711 ) ) ;
#54001=EDGE_CURVE ( 'NONE', #25655, #23009, #66202, .T. ) ;
#54007=DIRECTION ( 'NONE',  ( -0.000000000000000000, 3.673940397442059868E-16, -1.000000000000000000 ) ) ;
#54009=ORIENTED_EDGE ( 'NONE', *, *, #44932, .F. ) ;
#54010=LINE ( 'NONE', #48345, #9184 ) ;
#54014=VECTOR ( 'NONE', #15570, 999.9999999999998863 ) ;
#54015=DIRECTION ( 'NONE',  ( -1.000000000000000000, 0.000000000000000000, 0.000000000000000000 ) ) ;
#54019=ORIENTED_EDGE ( 'NONE', *, *, #36272, .F. ) ;
#54028=VERTEX_POINT ( 'NONE', #66880 ) ;
#54032=EDGE_LOOP ( 'NONE', ( #6489, #37249, #51492, #54776 ) ) ;
#54034=VECTOR ( 'NONE', #48310, 1000.000000000000000 ) ;
#54035=CARTESIAN_POINT ( 'NONE',  ( -10.30047626211725742, 3.650476262117184234, 54.00000000000000711 ) ) ;
#54036=LINE ( 'NONE', #5243, #62182 ) ;
#54038=EDGE_LOOP ( 'NONE', ( #8474, #30820, #10367, #11287 ) ) ;
#54040=EDGE_LOOP ( 'NONE', ( #25867, #10692, #25245, #32756 ) ) ;
#54043=EDGE_LOOP ( 'NONE', ( #20228, #54740, #9040, #4458 ) ) ;
#54054=DIRECTION ( 'NONE',  ( 0.7071067811865411334, -0.7071067811865539010, -2.597868168706484541E-16 ) ) ;
#54056=LINE ( 'NONE', #33167, #5231 ) ;
#54063=DIRECTION ( 'NONE',  ( 1.836970198721029934E-16, 1.836970198721010706E-16, -1.000000000000000000 ) ) ;
#54065=AXIS2_PLACEMENT_3D ( 'NONE', #44354, #44018, #23845 ) ;
#54068=DIRECTION ( 'NONE',  ( -0.4999999999999755196, 0.8660254037844526964, 2.509347957447861534E-16 ) ) ;
#54075=EDGE_CURVE ( 'NONE', #51462, #28725, #22672, .T. ) ;
#54076=DIRECTION ( 'NONE',  ( -1.836970198721029934E-16, -1.836970198721010706E-16, 1.000000000000000000 ) ) ;
#54087=DIRECTION ( 'NONE',  ( 0.000000000000000000, 0.000000000000000000, 1.000000000000000000 ) ) ;
#54103=CARTESIAN_POINT ( 'NONE',  ( -5.242976262117259978, 5.242976262117182706, 26.00000000000000711 ) ) ;
#54111=PLANE ( 'NONE',  #6768 ) ;
#54112=ORIENTED_EDGE ( 'NONE', *, *, #57467, .F. ) ;
#54115=VECTOR ( 'NONE', #69794, 1000.000000000000000 ) ;
#54116=CARTESIAN_POINT ( 'NONE',  ( 4.961189459950046121, 7.342976262117201003, 54.00000000000000711 ) ) ;
#54123=CARTESIAN_POINT ( 'NONE',  ( 6.872275254348426010, -3.003254798005752235, 26.00000000000000711 ) ) ;
#54124=VERTEX_POINT ( 'NONE', #62281 ) ;
#54130=ORIENTED_EDGE ( 'NONE', *, *, #43617, .T. ) ;
#54131=DIRECTION ( 'NONE',  ( -0.000000000000000000, 3.673940397442059868E-16, -1.000000000000000000 ) ) ;
#54134=AXIS2_PLACEMENT_3D ( 'NONE', #62632, #64068, #31879 ) ;
#54136=CARTESIAN_POINT ( 'NONE',  ( 8.835729544836338434, -2.544523737882816050, 26.00000000000000711 ) ) ;
#54150=ADVANCED_FACE ( 'NONE', ( #20202 ), #41763, .T. ) ;
#54157=AXIS2_PLACEMENT_3D ( 'NONE', #39806, #23557, #2344 ) ;
#54161=EDGE_CURVE ( 'NONE', #28070, #31078, #29406, .T. ) ;
#54175=LINE ( 'NONE', #54518, #20487 ) ;
#54186=VECTOR ( 'NONE', #27135, 1000.000000000000000 ) ;
#54191=ORIENTED_EDGE ( 'NONE', *, *, #229, .T. ) ;
#54201=ORIENTED_EDGE ( 'NONE', *, *, #51404, .T. ) ;
#54202=ADVANCED_FACE ( 'NONE', ( #68995 ), #64063, .T. ) ;
#54206=CARTESIAN_POINT ( 'NONE',  ( -10.30047626211725742, 3.842976262117182351, 26.00000000000000711 ) ) ;
#54212=VECTOR ( 'NONE', #39782, 1000.000000000000000 ) ;
#54213=ORIENTED_EDGE ( 'NONE', *, *, #36705, .T. ) ;
#54223=CARTESIAN_POINT ( 'NONE',  ( 7.532023737882817649, -3.848229544836346605, 54.00000000000000711 ) ) ;
#54232=CARTESIAN_POINT ( 'NONE',  ( 10.50702373788280752, 6.835476262117182067, 54.00000000000000711 ) ) ;
#54246=DIRECTION ( 'NONE',  ( -1.836970198721029934E-16, 1.836970198721036590E-16, -1.000000000000000000 ) ) ;
#54263=LINE ( 'NONE', #27037, #68036 ) ;
#54268=ORIENTED_EDGE ( 'NONE', *, *, #45909, .F. ) ;
#54273=DIRECTION ( 'NONE',  ( -9.912705577010336396E-15, -1.000000000000000000, 0.000000000000000000 ) ) ;
#54283=ADVANCED_FACE ( 'NONE', ( #69342 ), #31183, .F. ) ;
#54284=ORIENTED_EDGE ( 'NONE', *, *, #50787, .F. ) ;
#54289=ORIENTED_EDGE ( 'NONE', *, *, #27943, .F. ) ;
#54290=DIRECTION ( 'NONE',  ( 0.7671651518153065341, -0.6414496315691495809, 0.000000000000000000 ) ) ;
#54294=ORIENTED_EDGE ( 'NONE', *, *, #36583, .T. ) ;
#54312=PLANE ( 'NONE',  #46635 ) ;
#54314=DIRECTION ( 'NONE',  ( -1.000000000000000000, 0.000000000000000000, 0.000000000000000000 ) ) ;
#54321=CARTESIAN_POINT ( 'NONE',  ( -10.49297626211729551, -6.849523737882748264, 54.00000000000000711 ) ) ;
#54323=CARTESIAN_POINT ( 'NONE',  ( -3.650476262117223314, 10.30047626211716683, 26.00000000000000711 ) ) ;
#54324=VECTOR ( 'NONE', #66019, 1000.000000000000000 ) ;
#54327=ORIENTED_EDGE ( 'NONE', *, *, #49962, .F. ) ;
#54329=CARTESIAN_POINT ( 'NONE',  ( -6.651770455163783957, -7.532023737882790115, 54.00000000000000711 ) ) ;
#54341=DIRECTION ( 'NONE',  ( -0.000000000000000000, -0.000000000000000000, -1.000000000000000000 ) ) ;
#54347=ORIENTED_EDGE ( 'NONE', *, *, #50942, .T. ) ;
#54348=CARTESIAN_POINT ( 'NONE',  ( 8.835729544836325999, 8.130476262117191766, 26.00000000000000711 ) ) ;
#54352=DIRECTION ( 'NONE',  ( 3.491481338843133355E-15, 1.000000000000000000, 0.000000000000000000 ) ) ;
#54360=LINE ( 'NONE', #12236, #32764 ) ;
#54361=VERTEX_POINT ( 'NONE', #23667 ) ;
#54362=ORIENTED_EDGE ( 'NONE', *, *, #53384, .T. ) ;
#54365=ADVANCED_FACE ( 'NONE', ( #1756 ), #28284, .T. ) ;
#54367=ORIENTED_EDGE ( 'NONE', *, *, #30128, .F. ) ;
#54375=ORIENTED_EDGE ( 'NONE', *, *, #18200, .T. ) ;
#54380=EDGE_CURVE ( 'NONE', #48238, #40825, #66460, .T. ) ;
#54382=CARTESIAN_POINT ( 'NONE',  ( -6.344366288193410419, 4.706725378239148050, 26.00000000000000711 ) ) ;
#54386=EDGE_LOOP ( 'NONE', ( #66070, #42374, #5440, #59133 ) ) ;
#54393=EDGE_CURVE ( 'NONE', #4451, #45572, #44109, .T. ) ;
#54400=VECTOR ( 'NONE', #64733, 1000.000000000000114 ) ;
#54406=ADVANCED_FACE ( 'NONE', ( #55514 ), #12010, .F. ) ;
#54412=PLANE ( 'NONE',  #64817 ) ;
#54422=ADVANCED_FACE ( 'NONE', ( #33591 ), #23331, .F. ) ;
#54424=ORIENTED_EDGE ( 'NONE', *, *, #51813, .T. ) ;
#54430=EDGE_CURVE ( 'NONE', #69312, #56335, #61137, .T. ) ;
#54435=DIRECTION ( 'NONE',  ( -1.000000000000000000, 0.000000000000000000, 0.000000000000000000 ) ) ;
#54442=VERTEX_POINT ( 'NONE', #49173 ) ;
#54446=ORIENTED_EDGE ( 'NONE', *, *, #67187, .T. ) ;
#54457=ORIENTED_EDGE ( 'NONE', *, *, #50648, .T. ) ;
#54468=EDGE_CURVE ( 'NONE', #31078, #58674, #40284, .T. ) ;
#54472=CIRCLE ( 'NONE', #47701, 1.929199999999997139 ) ;
#54476=DIRECTION ( 'NONE',  ( 1.000000000000000000, 0.000000000000000000, 0.000000000000000000 ) ) ;
#54480=EDGE_CURVE ( 'NONE', #7568, #29126, #62196, .T. ) ;
#54483=DIRECTION ( 'NONE',  ( 1.836970198721029934E-16, -1.836970198721036344E-16, 1.000000000000000000 ) ) ;
#54485=DIRECTION ( 'NONE',  ( 0.000000000000000000, 0.000000000000000000, 1.000000000000000000 ) ) ;
#54486=ADVANCED_FACE ( 'NONE', ( #68208 ), #29666, .F. ) ;
#54487=ADVANCED_FACE ( 'NONE', ( #18350 ), #51953, .F. ) ;
#54489=LINE ( 'NONE', #21947, #39412 ) ;
#54518=CARTESIAN_POINT ( 'NONE',  ( -4.031976262117261456, 3.142976262117183506, 54.00000000000000711 ) ) ;
#54519=ORIENTED_EDGE ( 'NONE', *, *, #16069, .F. ) ;
#54522=VERTEX_POINT ( 'NONE', #3165 ) ;
#54523=ORIENTED_EDGE ( 'NONE', *, *, #1313, .F. ) ;
#54526=DIRECTION ( 'NONE',  ( -0.000000000000000000, 3.673940397442059868E-16, -1.000000000000000000 ) ) ;
#54528=AXIS2_PLACEMENT_3D ( 'NONE', #52943, #69185, #5188 ) ;
#54536=ORIENTED_EDGE ( 'NONE', *, *, #15903, .T. ) ;
#54540=DIRECTION ( 'NONE',  ( 0.7671651518153006499, 0.6414496315691565753, 0.000000000000000000 ) ) ;
#54541=EDGE_CURVE ( 'NONE', #40746, #13295, #24726, .T. ) ;
#54551=VECTOR ( 'NONE', #20580, 1000.000000000000000 ) ;
#54561=DIRECTION ( 'NONE',  ( 9.912705577010319041E-15, 1.000000000000000000, 0.000000000000000000 ) ) ;
#54566=DIRECTION ( 'NONE',  ( -1.836970198721029934E-16, 1.836970198721036590E-16, -1.000000000000000000 ) ) ;
#54574=ORIENTED_EDGE ( 'NONE', *, *, #46102, .F. ) ;
#54575=DIRECTION ( 'NONE',  ( -4.956352788505168198E-15, -1.000000000000000000, 0.000000000000000000 ) ) ;
#54581=CIRCLE ( 'NONE', #63614, 0.7112000000000124889 ) ;
#54586=CARTESIAN_POINT ( 'NONE',  ( -7.517976262117260333, 3.834182069070703580, 54.00000000000000711 ) ) ;
#54588=CARTESIAN_POINT ( 'NONE',  ( 4.961189459950046121, 7.342976262117201003, 54.00000000000000711 ) ) ;
#54591=CARTESIAN_POINT ( 'NONE',  ( 8.711985858128644011, 2.406732575409517239, 54.00000000000000711 ) ) ;
#54599=AXIS2_PLACEMENT_3D ( 'NONE', #57004, #8565, #53134 ) ;
#54611=LINE ( 'NONE', #31657, #22858 ) ;
#54613=VECTOR ( 'NONE', #34113, 1000.000000000000000 ) ;
#54615=CARTESIAN_POINT ( 'NONE',  ( 6.836383711243005479, -6.364920264886905876, 54.00000000000000711 ) ) ;
#54623=VECTOR ( 'NONE', #5379, 1000.000000000000114 ) ;
#54624=AXIS2_PLACEMENT_3D ( 'NONE', #35185, #8322, #29893 ) ;
#54626=ORIENTED_EDGE ( 'NONE', *, *, #8941, .F. ) ;
#54627=VERTEX_POINT ( 'NONE', #47692 ) ;
#54634=ORIENTED_EDGE ( 'NONE', *, *, #42056, .F. ) ;
#54645=DIRECTION ( 'NONE',  ( 3.491481338843133355E-15, 1.000000000000000000, 1.836970198721029934E-16 ) ) ;
#54646=EDGE_LOOP ( 'NONE', ( #34034, #15037, #32768, #45885 ) ) ;
#54649=DIRECTION ( 'NONE',  ( -0.000000000000000000, -0.000000000000000000, -1.000000000000000000 ) ) ;
#54650=CARTESIAN_POINT ( 'NONE',  ( 9.737023737882816832, -6.832023737882823688, 54.00000000000000711 ) ) ;
#54651=CARTESIAN_POINT ( 'NONE',  ( 8.580623737882845603, 8.916576262117189344, 54.00000000000000711 ) ) ;
#54661=CARTESIAN_POINT ( 'NONE',  ( 3.682023737882786918, -9.737023737882809726, 54.00000000000000711 ) ) ;
#54665=CARTESIAN_POINT ( 'NONE',  ( 2.544523737882787184, -9.562023737882800134, 54.00000000000000711 ) ) ;
#54676=CARTESIAN_POINT ( 'NONE',  ( 6.836383711243005479, -4.149127210878744698, 54.00000000000000711 ) ) ;
#54681=DIRECTION ( 'NONE',  ( 0.000000000000000000, 0.000000000000000000, 1.000000000000000000 ) ) ;
#54683=VECTOR ( 'NONE', #46189, 1000.000000000000000 ) ;
#54687=VERTEX_POINT ( 'NONE', #25789 ) ;
#54695=VERTEX_POINT ( 'NONE', #58998 ) ;
#54696=DIRECTION ( 'NONE',  ( 0.000000000000000000, 1.000000000000000000, 0.000000000000000000 ) ) ;
#54697=DIRECTION ( 'NONE',  ( -0.000000000000000000, -0.000000000000000000, -1.000000000000000000 ) ) ;
#54707=ORIENTED_EDGE ( 'NONE', *, *, #26871, .F. ) ;
#54716=EDGE_CURVE ( 'NONE', #29241, #5502, #44795, .T. ) ;
#54717=ORIENTED_EDGE ( 'NONE', *, *, #9385, .F. ) ;
#54720=VECTOR ( 'NONE', #31561, 1000.000000000000000 ) ;
#54732=VERTEX_POINT ( 'NONE', #27864 ) ;
#54733=ORIENTED_EDGE ( 'NONE', *, *, #24536, .F. ) ;
#54740=ORIENTED_EDGE ( 'NONE', *, *, #39139, .F. ) ;
#54741=CARTESIAN_POINT ( 'NONE',  ( 10.50702373788277910, 3.650476262117147375, 26.00000000000000711 ) ) ;
#54743=DIRECTION ( 'NONE',  ( 1.000000000000000000, -8.540177112501197482E-15, 0.000000000000000000 ) ) ;
#54753=ORIENTED_EDGE ( 'NONE', *, *, #35159, .F. ) ;
#54758=DIRECTION ( 'NONE',  ( 0.000000000000000000, -1.000000000000000000, -3.673940397442059868E-16 ) ) ;
#54761=AXIS2_PLACEMENT_3D ( 'NONE', #53764, #26892, #26535 ) ;
#54767=AXIS2_PLACEMENT_3D ( 'NONE', #48427, #42768, #43109 ) ;
#54771=EDGE_CURVE ( 'NONE', #45033, #17091, #22894, .T. ) ;
#54773=ORIENTED_EDGE ( 'NONE', *, *, #51481, .F. ) ;
#54776=ORIENTED_EDGE ( 'NONE', *, *, #5978, .T. ) ;
#54780=AXIS2_PLACEMENT_3D ( 'NONE', #63879, #12881, #6574 ) ;
#54791=ORIENTED_EDGE ( 'NONE', *, *, #34231, .T. ) ;
#54798=ORIENTED_EDGE ( 'NONE', *, *, #24896, .F. ) ;
#54811=VECTOR ( 'NONE', #43785, 1000.000000000000114 ) ;
#54818=ORIENTED_EDGE ( 'NONE', *, *, #63091, .F. ) ;
#54822=LINE ( 'NONE', #50549, #36315 ) ;
#54835=CIRCLE ( 'NONE', #49181, 0.1749999999999998224 ) ;
#54846=EDGE_CURVE ( 'NONE', #27049, #22852, #59692, .T. ) ;
#54856=EDGE_CURVE ( 'NONE', #27495, #67923, #3340, .T. ) ;
#54860=ADVANCED_FACE ( 'NONE', ( #8641 ), #35495, .F. ) ;
#54874=EDGE_CURVE ( 'NONE', #30798, #7476, #35863, .T. ) ;
#54875=CARTESIAN_POINT ( 'NONE',  ( -2.530476262117233865, 8.821682069070682530, 26.00000000000000711 ) ) ;
#54878=LINE ( 'NONE', #49559, #25308 ) ;
#54880=EDGE_LOOP ( 'NONE', ( #34380, #2053, #648, #5726 ) ) ;
#54890=DIRECTION ( 'NONE',  ( 1.000000000000000000, 0.000000000000000000, 0.000000000000000000 ) ) ;
#54897=VECTOR ( 'NONE', #66386, 1000.000000000000000 ) ;
#54900=EDGE_LOOP ( 'NONE', ( #34383, #6454, #48400, #36536 ) ) ;
#54902=LINE ( 'NONE', #22022, #42952 ) ;
#54912=ORIENTED_EDGE ( 'NONE', *, *, #61110, .T. ) ;
#54913=DIRECTION ( 'NONE',  ( -1.678252938371784572E-14, -1.000000000000000000, -1.836970198721041520E-16 ) ) ;
#54917=DIRECTION ( 'NONE',  ( 0.000000000000000000, 0.000000000000000000, 1.000000000000000000 ) ) ;
#54935=ORIENTED_EDGE ( 'NONE', *, *, #35931, .T. ) ;
#54937=VECTOR ( 'NONE', #22963, 1000.000000000000000 ) ;
#54940=EDGE_CURVE ( 'NONE', #16599, #48981, #67688, .T. ) ;
#54943=CARTESIAN_POINT ( 'NONE',  ( -4.135079735113208699, -3.677663764522613121, 54.00000000000000711 ) ) ;
#54954=EDGE_CURVE ( 'NONE', #12339, #27421, #68394, .T. ) ;
#54959=CYLINDRICAL_SURFACE ( 'NONE', #34990, 0.3499999999999996447 ) ;
#54971=VECTOR ( 'NONE', #52026, 1000.000000000000000 ) ;
#54979=EDGE_LOOP ( 'NONE', ( #31901, #5001, #11821, #68721 ) ) ;
#54989=CIRCLE ( 'NONE', #11994, 0.3499999999999996447 ) ;
#55005=FACE_OUTER_BOUND ( 'NONE', #4151, .T. ) ;
#55014=VECTOR ( 'NONE', #54054, 1000.000000000000000 ) ;
#55017=DIRECTION ( 'NONE',  ( -1.000000000000000000, 3.016910393003147986E-15, 1.108394896831706469E-30 ) ) ;
#55022=AXIS2_PLACEMENT_3D ( 'NONE', #29647, #9769, #58196 ) ;
#55035=EDGE_CURVE ( 'NONE', #15894, #10947, #1319, .T. ) ;
#55047=CARTESIAN_POINT ( 'NONE',  ( -8.566576262117353124, -9.703773737882732675, 26.00000000000000000 ) ) ;
#55049=CARTESIAN_POINT ( 'NONE',  ( -6.651770455163781293, -7.357023737882790293, 54.00000000000000711 ) ) ;
#55063=VERTEX_POINT ( 'NONE', #37624 ) ;
#55065=VECTOR ( 'NONE', #55017, 1000.000000000000000 ) ;
#55070=VECTOR ( 'NONE', #15287, 1000.000000000000000 ) ;
#55072=LINE ( 'NONE', #49058, #17556 ) ;
#55078=EDGE_CURVE ( 'NONE', #63544, #167, #58840, .T. ) ;
#55080=EDGE_CURVE ( 'NONE', #24515, #18477, #64842, .T. ) ;
#55087=VERTEX_POINT ( 'NONE', #47868 ) ;
#55089=DIRECTION ( 'NONE',  ( -1.836970198721029934E-16, 1.836970198721036590E-16, -1.000000000000000000 ) ) ;
#55106=CARTESIAN_POINT ( 'NONE',  ( -6.642976262117260333, 9.897976262117179402, 54.00000000000000711 ) ) ;
#55110=DIRECTION ( 'NONE',  ( 0.000000000000000000, 0.000000000000000000, 1.000000000000000000 ) ) ;
#55112=DIRECTION ( 'NONE',  ( -0.000000000000000000, 3.673940397442059868E-16, -1.000000000000000000 ) ) ;
#55115=LINE ( 'NONE', #5640, #18693 ) ;
#55117=ORIENTED_EDGE ( 'NONE', *, *, #14219, .T. ) ;
#55119=AXIS2_PLACEMENT_3D ( 'NONE', #56536, #8086, #19745 ) ;
#55122=CARTESIAN_POINT ( 'NONE',  ( -9.547976262117227719, -2.544523737882729453, 54.00000000000000711 ) ) ;
#55123=EDGE_LOOP ( 'NONE', ( #48160, #36532, #57749, #853 ) ) ;
#55128=EDGE_LOOP ( 'NONE', ( #30340, #66811, #8047, #61 ) ) ;
#55129=CIRCLE ( 'NONE', #28024, 0.5249999999999990230 ) ;
#55131=FACE_OUTER_BOUND ( 'NONE', #6752, .T. ) ;
#55134=ORIENTED_EDGE ( 'NONE', *, *, #20105, .F. ) ;
#55136=CARTESIAN_POINT ( 'NONE',  ( -3.842976262117221875, 10.30047626211716860, 54.00000000000000711 ) ) ;
#55145=ORIENTED_EDGE ( 'NONE', *, *, #59149, .T. ) ;
#55146=ORIENTED_EDGE ( 'NONE', *, *, #65570, .T. ) ;
#55161=DIRECTION ( 'NONE',  ( 1.000000000000000000, 0.000000000000000000, 0.000000000000000000 ) ) ;
#55169=DIRECTION ( 'NONE',  ( 1.000000000000000000, 0.000000000000000000, 0.000000000000000000 ) ) ;
#55172=VERTEX_POINT ( 'NONE', #18108 ) ;
#55173=DIRECTION ( 'NONE',  ( -1.000000000000000000, 0.000000000000000000, 0.000000000000000000 ) ) ;
#55177=ORIENTED_EDGE ( 'NONE', *, *, #20290, .F. ) ;
#55178=CARTESIAN_POINT ( 'NONE',  ( 9.912023737882782015, 3.667976262117150998, 54.00000000000000711 ) ) ;
#55211=LINE ( 'NONE', #23023, #15044 ) ;
#55212=VECTOR ( 'NONE', #44280, 1000.000000000000000 ) ;
#55213=DIRECTION ( 'NONE',  ( -0.000000000000000000, -0.000000000000000000, -1.000000000000000000 ) ) ;
#55215=CARTESIAN_POINT ( 'NONE',  ( 9.737023737882815055, -7.969523737882825642, 54.00000000000000711 ) ) ;
#55218=VERTEX_POINT ( 'NONE', #34358 ) ;
#55221=VECTOR ( 'NONE', #43185, 999.9999999999998863 ) ;
#55223=VECTOR ( 'NONE', #33519, 1000.000000000000000 ) ;
#55224=CIRCLE ( 'NONE', #50714, 0.1749999999999989342 ) ;
#55229=VERTEX_POINT ( 'NONE', #7503 ) ;
#55230=VECTOR ( 'NONE', #48137, 1000.000000000000000 ) ;
#55235=ORIENTED_EDGE ( 'NONE', *, *, #41014, .F. ) ;
#55240=CARTESIAN_POINT ( 'NONE',  ( -9.390476262117200434, -0.9555237378827314831, 54.00000000000000711 ) ) ;
#55249=AXIS2_PLACEMENT_3D ( 'NONE', #60133, #26939, #67 ) ;
#55258=CARTESIAN_POINT ( 'NONE',  ( -5.242976262117259978, 5.242976262117182706, 54.00000000000000711 ) ) ;
#55261=ADVANCED_FACE ( 'NONE', ( #28045 ), #49605, .F. ) ;
#55266=ORIENTED_EDGE ( 'NONE', *, *, #53200, .T. ) ;
#55272=DIRECTION ( 'NONE',  ( 0.000000000000000000, 1.000000000000000000, 0.000000000000000000 ) ) ;
#55278=VERTEX_POINT ( 'NONE', #61943 ) ;
#55285=CARTESIAN_POINT ( 'NONE',  ( -6.835476262117333057, -10.31452373788278543, 54.00000000000000711 ) ) ;
#55286=LINE ( 'NONE', #38335, #60546 ) ;
#55294=CARTESIAN_POINT ( 'NONE',  ( 10.31452373788281562, -6.849523737882823760, 54.00000000000000711 ) ) ;
#55295=CARTESIAN_POINT ( 'NONE',  ( -8.916576262117258622, 9.689726262117185129, 54.00000000000000711 ) ) ;
#55300=PLANE ( 'NONE',  #45767 ) ;
#55301=DIRECTION ( 'NONE',  ( -1.000000000000000000, 1.185108578570163402E-14, 1.836970198721051628E-16 ) ) ;
#55309=CIRCLE ( 'NONE', #46256, 0.3499999999999996447 ) ;
#55311=CARTESIAN_POINT ( 'NONE',  ( 9.562023737882814345, -7.969523737882814984, 26.00000000000000000 ) ) ;
#55312=ORIENTED_EDGE ( 'NONE', *, *, #30738, .F. ) ;
#55313=ORIENTED_EDGE ( 'NONE', *, *, #35159, .T. ) ;
#55318=VERTEX_POINT ( 'NONE', #68669 ) ;
#55320=VECTOR ( 'NONE', #27970, 1000.000000000000227 ) ;
#55330=CARTESIAN_POINT ( 'NONE',  ( -10.30047626211725742, 6.835476262117182955, 54.00000000000000711 ) ) ;
#55331=CARTESIAN_POINT ( 'NONE',  ( 10.31452373788280674, 6.835476262117182067, 54.00000000000000711 ) ) ;
#55341=FACE_BOUND ( 'NONE', #57405, .T. ) ;
#55353=VECTOR ( 'NONE', #20331, 999.9999999999998863 ) ;
#55364=VERTEX_POINT ( 'NONE', #31193 ) ;
#55367=LINE ( 'NONE', #11176, #57113 ) ;
#55376=CARTESIAN_POINT ( 'NONE',  ( -7.172176262117278434, -5.257023737882785319, 54.00000000000000711 ) ) ;
#55377=CARTESIAN_POINT ( 'NONE',  ( -6.350872789121327244, 3.663616288756986084, 54.00000000000000711 ) ) ;
#55379=VECTOR ( 'NONE', #66799, 1000.000000000000000 ) ;
#55381=DIRECTION ( 'NONE',  ( -1.836970198721029934E-16, 1.836970198721036590E-16, -1.000000000000000000 ) ) ;
#55387=CARTESIAN_POINT ( 'NONE',  ( 9.562023737882812569, -8.144523737882824577, 54.00000000000000711 ) ) ;
#55391=ORIENTED_EDGE ( 'NONE', *, *, #26573, .F. ) ;
#55395=ORIENTED_EDGE ( 'NONE', *, *, #9797, .F. ) ;
#55397=ORIENTED_EDGE ( 'NONE', *, *, #12375, .F. ) ;
#55406=AXIS2_PLACEMENT_3D ( 'NONE', #31302, #31642, #63812 ) ;
#55412=ADVANCED_FACE ( 'NONE', ( #398 ), #31886, .T. ) ;
#55426=CARTESIAN_POINT ( 'NONE',  ( -6.350872789121377870, -6.836383711242978833, 54.00000000000000711 ) ) ;
#55428=LINE ( 'NONE', #61049, #30771 ) ;
#55429=DIRECTION ( 'NONE',  ( 0.000000000000000000, -3.673940397442059868E-16, 1.000000000000000000 ) ) ;
#55432=ORIENTED_EDGE ( 'NONE', *, *, #36210, .T. ) ;
#55437=AXIS2_PLACEMENT_3D ( 'NONE', #21837, #6949, #38459 ) ;
#55453=EDGE_CURVE ( 'NONE', #49797, #36712, #26225, .T. ) ;
#55454=AXIS2_PLACEMENT_3D ( 'NONE', #62620, #62986, #41056 ) ;
#55458=EDGE_CURVE ( 'NONE', #56196, #11718, #21957, .T. ) ;
#55459=AXIS2_PLACEMENT_3D ( 'NONE', #22993, #28298, #39930 ) ;
#55460=PLANE ( 'NONE',  #34796 ) ;
#55462=EDGE_CURVE ( 'NONE', #19358, #57153, #32226, .T. ) ;
#55470=CIRCLE ( 'NONE', #19315, 1.224999999999998757 ) ;
#55472=CARTESIAN_POINT ( 'NONE',  ( 7.357023737882797398, 5.538810540049960984, 26.00000000000000711 ) ) ;
#55478=VECTOR ( 'NONE', #40817, 1000.000000000000000 ) ;
#55479=DIRECTION ( 'NONE',  ( -1.836970198721029934E-16, 1.836970198721036590E-16, -1.000000000000000000 ) ) ;
#55480=CARTESIAN_POINT ( 'NONE',  ( -8.697938382363135545, 8.079219948824830411, 54.00000000000000711 ) ) ;
#55485=CARTESIAN_POINT ( 'NONE',  ( -3.142976262117251451, 6.486996718459839606, 54.00000000000000711 ) ) ;
#55492=DIRECTION ( 'NONE',  ( -0.000000000000000000, 3.673940397442059868E-16, -1.000000000000000000 ) ) ;
#55493=CARTESIAN_POINT ( 'NONE',  ( 7.357023737882792069, 4.947141984184419528, 26.00000000000000711 ) ) ;
#55499=EDGE_CURVE ( 'NONE', #20779, #15964, #43519, .T. ) ;
#55505=LINE ( 'NONE', #17314, #69086 ) ;
#55506=ORIENTED_EDGE ( 'NONE', *, *, #37945, .T. ) ;
#55507=DIRECTION ( 'NONE',  ( 0.7671651518153006499, 0.6414496315691565753, 0.000000000000000000 ) ) ;
#55514=FACE_OUTER_BOUND ( 'NONE', #30689, .T. ) ;
#55519=DIRECTION ( 'NONE',  ( 1.836970198721029934E-16, 1.836970198721010706E-16, -1.000000000000000000 ) ) ;
#55521=ORIENTED_EDGE ( 'NONE', *, *, #66172, .T. ) ;
#55522=LINE ( 'NONE', #67164, #58393 ) ;
#55525=ORIENTED_EDGE ( 'NONE', *, *, #44329, .T. ) ;
#55530=CARTESIAN_POINT ( 'NONE',  ( -9.689726262117227762, 8.916576262117214213, 54.00000000000000711 ) ) ;
#55544=DIRECTION ( 'NONE',  ( -1.000000000000000000, 3.491481338843133355E-15, 0.000000000000000000 ) ) ;
#55569=CARTESIAN_POINT ( 'NONE',  ( -1.466476262117230034, 9.390476262117152473, 54.00000000000000711 ) ) ;
#55570=EDGE_LOOP ( 'NONE', ( #3394, #28309, #30214, #63056 ) ) ;
#55572=AXIS2_PLACEMENT_3D ( 'NONE', #21871, #59009, #69968 ) ;
#55584=ORIENTED_EDGE ( 'NONE', *, *, #19483, .F. ) ;
#55592=CARTESIAN_POINT ( 'NONE',  ( 1.480523737882816881, 9.390476262117212869, 54.00000000000000711 ) ) ;
#55593=EDGE_CURVE ( 'NONE', #22970, #63961, #60063, .T. ) ;
#55599=EDGE_CURVE ( 'NONE', #53330, #28620, #6952, .T. ) ;
#55603=CARTESIAN_POINT ( 'NONE',  ( 7.357023737882792069, 4.947141984184419528, 26.00000000000000711 ) ) ;
#55613=VERTEX_POINT ( 'NONE', #1769 ) ;
#55633=DIRECTION ( 'NONE',  ( -0.000000000000000000, -0.000000000000000000, -1.000000000000000000 ) ) ;
#55634=ORIENTED_EDGE ( 'NONE', *, *, #57260, .T. ) ;
#55639=ORIENTED_EDGE ( 'NONE', *, *, #25097, .T. ) ;
#55649=EDGE_CURVE ( 'NONE', #62514, #54442, #39587, .T. ) ;
#55650=ORIENTED_EDGE ( 'NONE', *, *, #65325, .T. ) ;
#55655=ORIENTED_EDGE ( 'NONE', *, *, #43547, .T. ) ;
#55656=ORIENTED_EDGE ( 'NONE', *, *, #54001, .F. ) ;
#55660=ORIENTED_EDGE ( 'NONE', *, *, #28102, .F. ) ;
#55666=DIRECTION ( 'NONE',  ( 1.000000000000000000, -3.016910393003147986E-15, 0.000000000000000000 ) ) ;
#55671=DIRECTION ( 'NONE',  ( 1.836970198721029934E-16, 1.836970198721010706E-16, -1.000000000000000000 ) ) ;
#55675=ORIENTED_EDGE ( 'NONE', *, *, #66489, .F. ) ;
#55676=FACE_OUTER_BOUND ( 'NONE', #44607, .T. ) ;
#55678=CARTESIAN_POINT ( 'NONE',  ( -8.916576262117258622, 10.03972626211718477, 54.00000000000000711 ) ) ;
#55682=CARTESIAN_POINT ( 'NONE',  ( -8.821682069070780230, 7.955476262117183062, 54.00000000000000711 ) ) ;
#55686=VERTEX_POINT ( 'NONE', #40294 ) ;
#55692=VERTEX_POINT ( 'NONE', #7764 ) ;
#55706=ORIENTED_EDGE ( 'NONE', *, *, #47160, .F. ) ;
#55711=CARTESIAN_POINT ( 'NONE',  ( -3.142976262117267883, -4.046023737882828542, 54.00000000000000711 ) ) ;
#55721=CARTESIAN_POINT ( 'NONE',  ( 7.357023737882806280, 6.651770455163672935, 54.00000000000000711 ) ) ;
#55723=ORIENTED_EDGE ( 'NONE', *, *, #11685, .F. ) ;
#55737=VERTEX_POINT ( 'NONE', #3523 ) ;
#55746=CARTESIAN_POINT ( 'NONE',  ( -5.538810540050023157, 7.342976262117183239, 54.00000000000000711 ) ) ;
#55765=FACE_OUTER_BOUND ( 'NONE', #68000, .T. ) ;
#55782=ORIENTED_EDGE ( 'NONE', *, *, #33375, .T. ) ;
#55791=EDGE_LOOP ( 'NONE', ( #62068, #13220, #9453, #23369 ) ) ;
#55796=DIRECTION ( 'NONE',  ( -1.000000000000000000, 6.308085367188448025E-15, 0.000000000000000000 ) ) ;
#55799=EDGE_CURVE ( 'NONE', #20779, #24327, #47703, .T. ) ;
#55800=CARTESIAN_POINT ( 'NONE',  ( -8.566576262117353124, -9.703773737882732675, 26.00000000000000000 ) ) ;
#55801=PLANE ( 'NONE',  #68396 ) ;
#55803=EDGE_CURVE ( 'NONE', #65821, #15450, #9527, .T. ) ;
#55809=DIRECTION ( 'NONE',  ( -1.836970198721029934E-16, -1.836970198721010706E-16, 1.000000000000000000 ) ) ;
#55817=CYLINDRICAL_SURFACE ( 'NONE', #62624, 0.1750000000000002387 ) ;
#55827=FACE_OUTER_BOUND ( 'NONE', #50163, .T. ) ;
#55830=ORIENTED_EDGE ( 'NONE', *, *, #21979, .T. ) ;
#55837=ORIENTED_EDGE ( 'NONE', *, *, #65570, .F. ) ;
#55842=CARTESIAN_POINT ( 'NONE',  ( 7.408280051175138325, 3.710438382363051790, 54.00000000000000711 ) ) ;
#55844=VERTEX_POINT ( 'NONE', #15186 ) ;
#55849=VECTOR ( 'NONE', #14409, 999.9999999999998863 ) ;
#55850=LINE ( 'NONE', #36028, #44859 ) ;
#55851=CARTESIAN_POINT ( 'NONE',  ( -7.605476262117258024, 9.722976262117178692, 25.99999580000000421 ) ) ;
#55852=CARTESIAN_POINT ( 'NONE',  ( -6.651770455163739548, 7.517976262117183062, 26.00000000000000711 ) ) ;
#55853=ORIENTED_EDGE ( 'NONE', *, *, #59283, .F. ) ;
#55856=CARTESIAN_POINT ( 'NONE',  ( -9.897976262117293089, -6.832023737882757075, 54.00000000000000711 ) ) ;
#55868=ORIENTED_EDGE ( 'NONE', *, *, #54874, .F. ) ;
#55876=EDGE_LOOP ( 'NONE', ( #60091, #17964, #66086, #33746 ) ) ;
#55882=EDGE_CURVE ( 'NONE', #43142, #20701, #16064, .T. ) ;
#55890=FACE_OUTER_BOUND ( 'NONE', #55123, .T. ) ;
#55895=EDGE_CURVE ( 'NONE', #8859, #68245, #43088, .T. ) ;
#55905=EDGE_LOOP ( 'NONE', ( #54446, #50306, #10759, #50273 ) ) ;
#55908=VECTOR ( 'NONE', #41338, 1000.000000000000000 ) ;
#55910=PLANE ( 'NONE',  #34922 ) ;
#55919=VERTEX_POINT ( 'NONE', #5619 ) ;
#55920=ORIENTED_EDGE ( 'NONE', *, *, #3298, .T. ) ;
#55930=VECTOR ( 'NONE', #13853, 1000.000000000000000 ) ;
#55945=CARTESIAN_POINT ( 'NONE',  ( 7.969523737882818537, -8.835729544836345539, 54.00000000000000711 ) ) ;
#55952=EDGE_LOOP ( 'NONE', ( #42855, #8403, #64964, #16374, #32192, #62144, #34494, #45241, #11617, #54191, #55920, #43835, #57199, #53984, #53937, #60473, #46262 ) ) ;
#55954=PLANE ( 'NONE',  #58501 ) ;
#55957=CIRCLE ( 'NONE', #25491, 0.1749999999999998224 ) ;
#55958=DIRECTION ( 'NONE',  ( -0.000000000000000000, 3.673940397442059868E-16, -1.000000000000000000 ) ) ;
#55973=VERTEX_POINT ( 'NONE', #11251 ) ;
#55980=LINE ( 'NONE', #66928, #63677 ) ;
#55989=ORIENTED_EDGE ( 'NONE', *, *, #13035, .T. ) ;
#55997=( LENGTH_UNIT ( ) NAMED_UNIT ( * ) SI_UNIT ( .MILLI., .METRE. ) );
#55998=ORIENTED_EDGE ( 'NONE', *, *, #18434, .T. ) ;
#56004=ORIENTED_EDGE ( 'NONE', *, *, #43284, .F. ) ;
#56014=AXIS2_PLACEMENT_3D ( 'NONE', #13738, #63235, #14805 ) ;
#56022=VECTOR ( 'NONE', #9835, 1000.000000000000000 ) ;
#56024=CARTESIAN_POINT ( 'NONE',  ( -5.779227145995285753, -4.155633711806640207, 54.00000000000000711 ) ) ;
#56029=CARTESIAN_POINT ( 'NONE',  ( -6.835476262117260227, 10.49297626211718359, 54.00000000000000711 ) ) ;
#56034=DIRECTION ( 'NONE',  ( -0.7071067811865500152, -0.7071067811865451302, 0.000000000000000000 ) ) ;
#56037=FACE_OUTER_BOUND ( 'NONE', #69571, .T. ) ;
#56043=LINE ( 'NONE', #39764, #15759 ) ;
#56044=LINE ( 'NONE', #12546, #54613 ) ;
#56055=DIRECTION ( 'NONE',  ( -0.7071067811865475727, 0.7071067811865475727, 2.597868168706480597E-16 ) ) ;
#56063=ADVANCED_FACE ( 'NONE', ( #6979 ), #28545, .F. ) ;
#56066=VECTOR ( 'NONE', #68381, 1000.000000000000114 ) ;
#56073=ORIENTED_EDGE ( 'NONE', *, *, #5862, .T. ) ;
#56082=ORIENTED_EDGE ( 'NONE', *, *, #59513, .T. ) ;
#56086=VERTEX_POINT ( 'NONE', #52216 ) ;
#56092=DIRECTION ( 'NONE',  ( -1.836970198721029934E-16, 1.836970198721036590E-16, -1.000000000000000000 ) ) ;
#56094=EDGE_CURVE ( 'NONE', #2486, #7598, #2380, .T. ) ;
#56100=LINE ( 'NONE', #51140, #13217 ) ;
#56107=DIRECTION ( 'NONE',  ( -1.836970198721029934E-16, 1.836970198721036590E-16, -1.000000000000000000 ) ) ;
#56109=PLANE ( 'NONE',  #64774 ) ;
#56112=EDGE_CURVE ( 'NONE', #18830, #35523, #56812, .T. ) ;
#56113=CARTESIAN_POINT ( 'NONE',  ( 3.157023737882809655, -6.501044194225480410, 54.00000000000000711 ) ) ;
#56115=VECTOR ( 'NONE', #11963, 1000.000000000000000 ) ;
#56116=CARTESIAN_POINT ( 'NONE',  ( 8.144523737882817471, -9.562023737882817898, 54.00000000000000711 ) ) ;
#56121=DIRECTION ( 'NONE',  ( 1.836970198721029934E-16, 1.836970198721010706E-16, -1.000000000000000000 ) ) ;
#56125=LINE ( 'NONE', #1669, #54897 ) ;
#56128=VECTOR ( 'NONE', #12008, 1000.000000000000000 ) ;
#56134=CARTESIAN_POINT ( 'NONE',  ( 6.836383711243005479, -4.149127210878744698, 54.00000000000000711 ) ) ;
#56146=EDGE_CURVE ( 'NONE', #31391, #19920, #12968, .T. ) ;
#56149=EDGE_CURVE ( 'NONE', #65251, #36248, #43208, .T. ) ;
#56150=DIRECTION ( 'NONE',  ( 0.7071067811865446862, 0.7071067811865503483, 0.000000000000000000 ) ) ;
#56151=AXIS2_PLACEMENT_3D ( 'NONE', #24211, #60373, #57083 ) ;
#56162=ORIENTED_EDGE ( 'NONE', *, *, #32864, .T. ) ;
#56163=ORIENTED_EDGE ( 'NONE', *, *, #22703, .T. ) ;
#56170=VERTEX_POINT ( 'NONE', #67445 ) ;
#56172=DIRECTION ( 'NONE',  ( 9.050731179009442381E-15, 1.000000000000000000, 0.000000000000000000 ) ) ;
#56174=ORIENTED_EDGE ( 'NONE', *, *, #52923, .F. ) ;
#56180=ORIENTED_EDGE ( 'NONE', *, *, #66361, .F. ) ;
#56185=DIRECTION ( 'NONE',  ( -0.000000000000000000, -0.000000000000000000, -1.000000000000000000 ) ) ;
#56196=VERTEX_POINT ( 'NONE', #30653 ) ;
#56199=ADVANCED_FACE ( 'NONE', ( #53980 ), #10483, .T. ) ;
#56203=CARTESIAN_POINT ( 'NONE',  ( 9.703773737882785966, -8.930623737882855906, 54.00000000000000711 ) ) ;
#56207=DIRECTION ( 'NONE',  ( 1.836970198721029934E-16, 1.836970198721010706E-16, -1.000000000000000000 ) ) ;
#56212=VECTOR ( 'NONE', #53132, 1000.000000000000000 ) ;
#56214=LINE ( 'NONE', #30389, #55908 ) ;
#56215=ORIENTED_EDGE ( 'NONE', *, *, #53136, .T. ) ;
#56249=EDGE_CURVE ( 'NONE', #27468, #21827, #25139, .T. ) ;
#56252=CARTESIAN_POINT ( 'NONE',  ( 10.31452373788281562, -3.664523737882816157, 26.00000000000000711 ) ) ;
#56253=ORIENTED_EDGE ( 'NONE', *, *, #22874, .F. ) ;
#56256=ORIENTED_EDGE ( 'NONE', *, *, #68874, .F. ) ;
#56259=VECTOR ( 'NONE', #8389, 1000.000000000000000 ) ;
#56263=VECTOR ( 'NONE', #18342, 1000.000000000000000 ) ;
#56266=VERTEX_POINT ( 'NONE', #4147 ) ;
#56276=EDGE_LOOP ( 'NONE', ( #17016, #10659, #60081, #66169 ) ) ;
#56277=ORIENTED_EDGE ( 'NONE', *, *, #7745, .F. ) ;
#56286=DIRECTION ( 'NONE',  ( 1.261617073437657735E-14, 1.000000000000000000, 3.673940397442059868E-16 ) ) ;
#56293=ORIENTED_EDGE ( 'NONE', *, *, #42722, .T. ) ;
#56294=DIRECTION ( 'NONE',  ( -1.000000000000000000, 0.000000000000000000, 0.000000000000000000 ) ) ;
#56301=DIRECTION ( 'NONE',  ( -1.000000000000000000, 0.000000000000000000, 0.000000000000000000 ) ) ;
#56306=AXIS2_PLACEMENT_3D ( 'NONE', #53648, #66241, #45009 ) ;
#56322=VERTEX_POINT ( 'NONE', #47270 ) ;
#56325=EDGE_CURVE ( 'NONE', #56650, #29848, #31378, .T. ) ;
#56333=LINE ( 'NONE', #39711, #60095 ) ;
#56335=VERTEX_POINT ( 'NONE', #17170 ) ;
#56336=EDGE_CURVE ( 'NONE', #66645, #47996, #21790, .T. ) ;
#56338=ORIENTED_EDGE ( 'NONE', *, *, #4775, .T. ) ;
#56341=DIRECTION ( 'NONE',  ( -0.000000000000000000, -0.000000000000000000, -1.000000000000000000 ) ) ;
#56345=EDGE_LOOP ( 'NONE', ( #29275, #37581, #35752, #16715 ) ) ;
#56346=ORIENTED_EDGE ( 'NONE', *, *, #48155, .F. ) ;
#56348=ORIENTED_EDGE ( 'NONE', *, *, #26449, .T. ) ;
#56352=ORIENTED_EDGE ( 'NONE', *, *, #993, .T. ) ;
#56356=ORIENTED_EDGE ( 'NONE', *, *, #60498, .T. ) ;
#56362=VERTEX_POINT ( 'NONE', #7241 ) ;
#56363=EDGE_LOOP ( 'NONE', ( #8772, #9348, #55235, #33007 ) ) ;
#56366=DIRECTION ( 'NONE',  ( 1.000000000000000000, -2.135044278125299371E-15, -7.844025423732057781E-31 ) ) ;
#56371=DIRECTION ( 'NONE',  ( -0.4999999999999786282, 0.8660254037844510311, 3.181725716174766844E-16 ) ) ;
#56377=CARTESIAN_POINT ( 'NONE',  ( -8.566576262117260754, 8.916576262117214213, 26.00000000000000711 ) ) ;
#56382=PLANE ( 'NONE',  #56151 ) ;
#56389=DIRECTION ( 'NONE',  ( -1.000000000000000000, 5.120954910632640039E-15, 0.000000000000000000 ) ) ;
#56391=CARTESIAN_POINT ( 'NONE',  ( -10.30047626211725742, 3.650476262117184234, 26.00000000000000711 ) ) ;
#56409=DIRECTION ( 'NONE',  ( 0.000000000000000000, 0.000000000000000000, -1.000000000000000000 ) ) ;
#56420=CARTESIAN_POINT ( 'NONE',  ( -7.342976262117288933, -6.665817930929258672, 26.00000000000000000 ) ) ;
#56430=DIRECTION ( 'NONE',  ( -0.7071067811865474617, 0.7071067811865474617, -0.000000000000000000 ) ) ;
#56431=DIRECTION ( 'NONE',  ( 1.836970198721029934E-16, 1.836970198721010706E-16, -1.000000000000000000 ) ) ;
#56441=CIRCLE ( 'NONE', #1151, 0.1749999999999998224 ) ;
#56444=LINE ( 'NONE', #3071, #15332 ) ;
#56448=CARTESIAN_POINT ( 'NONE',  ( -8.821682069070828192, -7.969523737882767911, 54.00000000000000711 ) ) ;
#56451=LINE ( 'NONE', #18978, #54683 ) ;
#56464=DIRECTION ( 'NONE',  ( -1.000000000000000000, 0.000000000000000000, 0.000000000000000000 ) ) ;
#56465=EDGE_CURVE ( 'NONE', #49178, #55278, #51120, .T. ) ;
#56468=CARTESIAN_POINT ( 'NONE',  ( 5.257023737882795977, 5.242976262117205799, 26.00000000000000711 ) ) ;
#56471=CARTESIAN_POINT ( 'NONE',  ( -9.547976262117256141, 2.530476262117183683, 26.00000000000000711 ) ) ;
#56479=DIRECTION ( 'NONE',  ( -0.000000000000000000, 3.673940397442059868E-16, -1.000000000000000000 ) ) ;
#56486=EDGE_CURVE ( 'NONE', #20807, #42575, #22143, .T. ) ;
#56487=VERTEX_POINT ( 'NONE', #43708 ) ;
#56499=VERTEX_POINT ( 'NONE', #34455 ) ;
#56500=DIRECTION ( 'NONE',  ( 0.7671651518153131954, 0.6414496315691415873, 2.587583378555109562E-16 ) ) ;
#56503=DIRECTION ( 'NONE',  ( -0.000000000000000000, 3.673940397442059868E-16, -1.000000000000000000 ) ) ;
#56506=CARTESIAN_POINT ( 'NONE',  ( -3.834182069070824816, -7.532023737882819425, 54.00000000000000711 ) ) ;
#56509=VERTEX_POINT ( 'NONE', #66997 ) ;
#56510=CARTESIAN_POINT ( 'NONE',  ( 10.05377373788278739, -9.703773737882823269, 54.00000000000000711 ) ) ;
#56512=ORIENTED_EDGE ( 'NONE', *, *, #12467, .F. ) ;
#56513=VECTOR ( 'NONE', #63189, 1000.000000000000000 ) ;
#56526=LINE ( 'NONE', #17994, #24419 ) ;
#56527=EDGE_CURVE ( 'NONE', #29684, #4835, #67358, .T. ) ;
#56529=ORIENTED_EDGE ( 'NONE', *, *, #44796, .F. ) ;
#56536=CARTESIAN_POINT ( 'NONE',  ( 6.832023737882815695, 9.897976262117191837, 54.00000000000000711 ) ) ;
#56544=CARTESIAN_POINT ( 'NONE',  ( 3.664523737882814824, 10.30047626211720768, 26.00000000000000711 ) ) ;
#56545=DIRECTION ( 'NONE',  ( -7.808916176531286882E-15, -1.000000000000000000, 0.000000000000000000 ) ) ;
#56550=DIRECTION ( 'NONE',  ( 1.836970198721029934E-16, -1.836970198721036344E-16, 1.000000000000000000 ) ) ;
#56552=CYLINDRICAL_SURFACE ( 'NONE', #50327, 0.1749999999999998224 ) ;
#56558=CARTESIAN_POINT ( 'NONE',  ( -5.242976262117280406, -5.257023737882805747, 54.00000000000000711 ) ) ;
#56564=LINE ( 'NONE', #29329, #49798 ) ;
#56565=EDGE_CURVE ( 'NONE', #63123, #43741, #34814, .T. ) ;
#56572=VERTEX_POINT ( 'NONE', #23865 ) ;
#56573=CARTESIAN_POINT ( 'NONE',  ( -7.342976262117259623, 6.651770455163663165, 54.00000000000000711 ) ) ;
#56574=ORIENTED_EDGE ( 'NONE', *, *, #13313, .F. ) ;
#56575=ORIENTED_EDGE ( 'NONE', *, *, #46161, .T. ) ;
#56582=ORIENTED_EDGE ( 'NONE', *, *, #53190, .T. ) ;
#56591=ORIENTED_EDGE ( 'NONE', *, *, #31518, .T. ) ;
#56593=DIRECTION ( 'NONE',  ( -0.000000000000000000, -0.000000000000000000, -1.000000000000000000 ) ) ;
#56609=EDGE_CURVE ( 'NONE', #16704, #26653, #18396, .T. ) ;
#56610=ADVANCED_FACE ( 'NONE', ( #35507 ), #66648, .F. ) ;
#56612=LINE ( 'NONE', #24443, #8556 ) ;
#56631=CARTESIAN_POINT ( 'NONE',  ( 5.793274621760814647, 4.141586236041038482, 54.00000000000000711 ) ) ;
#56633=DIRECTION ( 'NONE',  ( 1.836970198721029934E-16, 1.836970198721010706E-16, -1.000000000000000000 ) ) ;
#56635=DIRECTION ( 'NONE',  ( -1.000000000000000000, 1.349135440953254490E-14, -1.836970198721005282E-16 ) ) ;
#56638=DIRECTION ( 'NONE',  ( 1.047444401652940007E-14, 1.000000000000000000, 1.836970198721029934E-16 ) ) ;
#56643=LINE ( 'NONE', #8192, #68527 ) ;
#56650=VERTEX_POINT ( 'NONE', #68407 ) ;
#56658=ORIENTED_EDGE ( 'NONE', *, *, #55649, .F. ) ;
#56667=ORIENTED_EDGE ( 'NONE', *, *, #54430, .F. ) ;
#56672=ORIENTED_EDGE ( 'NONE', *, *, #33081, .T. ) ;
#56673=ADVANCED_FACE ( 'NONE', ( #4064 ), #42223, .T. ) ;
#56674=DIRECTION ( 'NONE',  ( 1.280238727658158432E-15, 1.000000000000000000, -0.000000000000000000 ) ) ;
#56683=EDGE_LOOP ( 'NONE', ( #52748, #9192, #24072, #12663 ) ) ;
#56684=ORIENTED_EDGE ( 'NONE', *, *, #1661, .T. ) ;
#56690=ADVANCED_FACE ( 'NONE', ( #52865 ), #68762, .F. ) ;
#56691=FACE_OUTER_BOUND ( 'NONE', #65150, .T. ) ;
#56699=LINE ( 'NONE', #6944, #51418 ) ;
#56705=DIRECTION ( 'NONE',  ( -0.4999999999999913958, 0.8660254037844435926, 6.723777587268537869E-17 ) ) ;
#56712=PLANE ( 'NONE',  #42514 ) ;
#56714=VERTEX_POINT ( 'NONE', #58514 ) ;
#56716=VECTOR ( 'NONE', #17116, 1000.000000000000000 ) ;
#56717=CARTESIAN_POINT ( 'NONE',  ( 7.969523737882816761, 9.722976262117187574, 54.00000000000000711 ) ) ;
#56719=ORIENTED_EDGE ( 'NONE', *, *, #67903, .F. ) ;
#56722=DIRECTION ( 'NONE',  ( 0.7671651518153087546, 0.6414496315691469164, 0.000000000000000000 ) ) ;
#56739=DIRECTION ( 'NONE',  ( -1.828336019306068695E-14, -1.000000000000000000, -1.836970198721044232E-16 ) ) ;
#56748=AXIS2_PLACEMENT_3D ( 'NONE', #23931, #7308, #18265 ) ;
#56753=LINE ( 'NONE', #62053, #14670 ) ;
#56758=VERTEX_POINT ( 'NONE', #64169 ) ;
#56775=VECTOR ( 'NONE', #41971, 1000.000000000000000 ) ;
#56779=AXIS2_PLACEMENT_3D ( 'NONE', #44113, #58999, #16211 ) ;
#56782=DIRECTION ( 'NONE',  ( 9.912705577010361640E-15, 1.000000000000000000, 0.000000000000000000 ) ) ;
#56788=DIRECTION ( 'NONE',  ( 0.000000000000000000, 0.000000000000000000, 1.000000000000000000 ) ) ;
#56789=CARTESIAN_POINT ( 'NONE',  ( -6.642976262117260333, 10.30047626211718104, 26.00000000000000711 ) ) ;
#56793=DIRECTION ( 'NONE',  ( -1.836970198721029934E-16, -1.836970198721010706E-16, 1.000000000000000000 ) ) ;
#56794=LINE ( 'NONE', #62093, #62693 ) ;
#56803=DIRECTION ( 'NONE',  ( -1.000000000000000000, 0.000000000000000000, 0.000000000000000000 ) ) ;
#56806=ORIENTED_EDGE ( 'NONE', *, *, #64567, .T. ) ;
#56807=DIRECTION ( 'NONE',  ( -0.7071067811865474617, 0.7071067811865474617, 0.000000000000000000 ) ) ;
#56811=LINE ( 'NONE', #67777, #67637 ) ;
#56812=LINE ( 'NONE', #35231, #62372 ) ;
#56814=DIRECTION ( 'NONE',  ( 1.079558018506126625E-14, 1.000000000000000000, 1.836970198721016622E-16 ) ) ;
#56835=ORIENTED_EDGE ( 'NONE', *, *, #32679, .T. ) ;
#56837=VERTEX_POINT ( 'NONE', #18379 ) ;
#56838=ORIENTED_EDGE ( 'NONE', *, *, #58222, .T. ) ;
#56844=DIRECTION ( 'NONE',  ( 1.047444401652940007E-14, 1.000000000000000000, 0.000000000000000000 ) ) ;
#56845=DIRECTION ( 'NONE',  ( -1.000000000000000000, 0.000000000000000000, 0.000000000000000000 ) ) ;
#56849=DIRECTION ( 'NONE',  ( -4.121462285523435444E-16, -1.000000000000000000, 0.000000000000000000 ) ) ;
#56852=ORIENTED_EDGE ( 'NONE', *, *, #9734, .T. ) ;
#56860=EDGE_CURVE ( 'NONE', #39038, #25974, #60481, .T. ) ;
#56866=VERTEX_POINT ( 'NONE', #60823 ) ;
#56868=AXIS2_PLACEMENT_3D ( 'NONE', #20664, #41544, #63463 ) ;
#56870=VECTOR ( 'NONE', #53007, 1000.000000000000000 ) ;
#56871=LINE ( 'NONE', #57927, #57225 ) ;
#56876=DIRECTION ( 'NONE',  ( 0.7071067811865503483, 0.7071067811865446862, 0.000000000000000000 ) ) ;
#56880=CARTESIAN_POINT ( 'NONE',  ( -4.135079735113214916, -6.836383711243002814, 54.00000000000000711 ) ) ;
#56884=DIRECTION ( 'NONE',  ( 0.000000000000000000, 1.000000000000000000, 0.000000000000000000 ) ) ;
#56885=CARTESIAN_POINT ( 'NONE',  ( -4.706725378239217328, 4.141586236041038482, 54.00000000000000711 ) ) ;
#56893=CARTESIAN_POINT ( 'NONE',  ( 7.969523737882816761, 9.722976262117187574, 54.00000000000000711 ) ) ;
#56916=CARTESIAN_POINT ( 'NONE',  ( 9.703773737882785966, -8.580623737882856261, 54.00000000000000711 ) ) ;
#56920=DIRECTION ( 'NONE',  ( -0.000000000000000000, -0.000000000000000000, -1.000000000000000000 ) ) ;
#56923=ORIENTED_EDGE ( 'NONE', *, *, #29068, .F. ) ;
#56928=DIRECTION ( 'NONE',  ( 0.7071067811865530128, 0.7071067811865421326, 0.000000000000000000 ) ) ;
#56929=CARTESIAN_POINT ( 'NONE',  ( -6.817976262117261044, 9.722976262117182245, 54.00000000000000711 ) ) ;
#56930=DIRECTION ( 'NONE',  ( 0.000000000000000000, 1.000000000000000000, 3.673940397442059868E-16 ) ) ;
#56937=CYLINDRICAL_SURFACE ( 'NONE', #66014, 0.5249999999999990230 ) ;
#56948=ORIENTED_EDGE ( 'NONE', *, *, #4342, .T. ) ;
#56951=DIRECTION ( 'NONE',  ( -0.7671651518153043137, 0.6414496315691521344, 2.587583378555129776E-16 ) ) ;
#56966=DIRECTION ( 'NONE',  ( 1.000000000000000000, -1.047444401652940007E-14, 0.000000000000000000 ) ) ;
#56968=CARTESIAN_POINT ( 'NONE',  ( 9.562023737882764607, 2.355476262117153663, 54.00000000000000711 ) ) ;
#56976=CARTESIAN_POINT ( 'NONE',  ( -9.390476262117259054, 1.466476262117183182, 54.00000000000000711 ) ) ;
#56978=FACE_OUTER_BOUND ( 'NONE', #3299, .T. ) ;
#56981=VECTOR ( 'NONE', #222, 1000.000000000000000 ) ;
#56982=CARTESIAN_POINT ( 'NONE',  ( -9.897976262117259338, 6.642976262117183950, 54.00000000000000711 ) ) ;
#56995=CYLINDRICAL_SURFACE ( 'NONE', #46576, 1.929199999999998028 ) ;
#56998=ORIENTED_EDGE ( 'NONE', *, *, #22071, .F. ) ;
#57004=CARTESIAN_POINT ( 'NONE',  ( 6.832023737882815695, 9.897976262117191837, 54.00000000000000711 ) ) ;
#57007=AXIS2_PLACEMENT_3D ( 'NONE', #6822, #28392, #39355 ) ;
#57011=CARTESIAN_POINT ( 'NONE',  ( -7.955476262117317177, -8.835729544836295801, 54.00000000000000711 ) ) ;
#57018=CIRCLE ( 'NONE', #50253, 0.1749999999999998224 ) ;
#57031=ORIENTED_EDGE ( 'NONE', *, *, #51847, .F. ) ;
#57037=DIRECTION ( 'NONE',  ( -1.000000000000000000, 0.000000000000000000, 0.000000000000000000 ) ) ;
#57038=ORIENTED_EDGE ( 'NONE', *, *, #44879, .F. ) ;
#57045=DIRECTION ( 'NONE',  ( 9.912705577010336396E-15, 1.000000000000000000, 0.000000000000000000 ) ) ;
#57073=ORIENTED_EDGE ( 'NONE', *, *, #20460, .F. ) ;
#57078=CIRCLE ( 'NONE', #7345, 1.929199999999998028 ) ;
#57081=ORIENTED_EDGE ( 'NONE', *, *, #20920, .F. ) ;
#57083=DIRECTION ( 'NONE',  ( 8.903847840905249551E-15, 1.000000000000000000, 0.000000000000000000 ) ) ;
#57102=ORIENTED_EDGE ( 'NONE', *, *, #65886, .T. ) ;
#57103=CARTESIAN_POINT ( 'NONE',  ( -8.079219948824906794, 8.697938382363059162, 54.00000000000000711 ) ) ;
#57107=DIRECTION ( 'NONE',  ( 0.000000000000000000, 1.000000000000000000, 0.000000000000000000 ) ) ;
#57111=VECTOR ( 'NONE', #49389, 1000.000000000000000 ) ;
#57113=VECTOR ( 'NONE', #34121, 1000.000000000000000 ) ;
#57118=CARTESIAN_POINT ( 'NONE',  ( 6.849523737882818430, 10.49297626211719603, 54.00000000000000711 ) ) ;
#57127=PLANE ( 'NONE',  #42557 ) ;
#57143=ORIENTED_EDGE ( 'NONE', *, *, #38427, .T. ) ;
#57144=AXIS2_PLACEMENT_3D ( 'NONE', #43784, #16574, #32821 ) ;
#57151=DIRECTION ( 'NONE',  ( 1.000000000000000000, 3.016910393003147986E-15, 1.108394896831706469E-30 ) ) ;
#57153=VERTEX_POINT ( 'NONE', #10578 ) ;
#57154=DIRECTION ( 'NONE',  ( 1.000000000000000000, 0.000000000000000000, 0.000000000000000000 ) ) ;
#57166=EDGE_CURVE ( 'NONE', #54732, #27591, #59716, .T. ) ;
#57174=CARTESIAN_POINT ( 'NONE',  ( -7.342976262117259623, 3.834182069070703580, 54.00000000000000711 ) ) ;
#57176=VECTOR ( 'NONE', #40374, 1000.000000000000000 ) ;
#57180=CARTESIAN_POINT ( 'NONE',  ( 3.848229544836329730, 7.342976262117204556, 54.00000000000000711 ) ) ;
#57182=ORIENTED_EDGE ( 'NONE', *, *, #42243, .F. ) ;
#57187=DIRECTION ( 'NONE',  ( -0.000000000000000000, -0.000000000000000000, -1.000000000000000000 ) ) ;
#57194=DIRECTION ( 'NONE',  ( 0.000000000000000000, 0.000000000000000000, 1.000000000000000000 ) ) ;
#57199=ORIENTED_EDGE ( 'NONE', *, *, #19604, .T. ) ;
#57214=ORIENTED_EDGE ( 'NONE', *, *, #58859, .F. ) ;
#57218=ORIENTED_EDGE ( 'NONE', *, *, #58852, .F. ) ;
#57225=VECTOR ( 'NONE', #9493, 1000.000000000000000 ) ;
#57231=AXIS2_PLACEMENT_3D ( 'NONE', #40331, #7789, #2840 ) ;
#57237=LINE ( 'NONE', #46270, #7981 ) ;
#57244=CARTESIAN_POINT ( 'NONE',  ( -2.617976262117293285, -6.501044194225502615, 54.00000000000000711 ) ) ;
#57253=EDGE_CURVE ( 'NONE', #31525, #28725, #66403, .T. ) ;
#57260=EDGE_CURVE ( 'NONE', #55613, #40627, #6657, .T. ) ;
#57264=DIRECTION ( 'NONE',  ( 0.000000000000000000, 1.000000000000000000, 0.000000000000000000 ) ) ;
#57266=VERTEX_POINT ( 'NONE', #33532 ) ;
#57271=EDGE_CURVE ( 'NONE', #44739, #37577, #11946, .T. ) ;
#57277=DIRECTION ( 'NONE',  ( 1.836970198721029934E-16, 1.836970198721010706E-16, -1.000000000000000000 ) ) ;
#57290=EDGE_LOOP ( 'NONE', ( #32350, #28419, #58739, #16260 ) ) ;
#57296=ORIENTED_EDGE ( 'NONE', *, *, #19656, .F. ) ;
#57302=ORIENTED_EDGE ( 'NONE', *, *, #32268, .T. ) ;
#57312=DIRECTION ( 'NONE',  ( 1.836970198721029934E-16, 1.836970198721010706E-16, -1.000000000000000000 ) ) ;
#57315=ORIENTED_EDGE ( 'NONE', *, *, #52170, .F. ) ;
#57317=AXIS2_PLACEMENT_3D ( 'NONE', #10811, #69166, #43691 ) ;
#57318=CARTESIAN_POINT ( 'NONE',  ( -3.142976262117261221, 4.031976262117183296, 54.00000000000000711 ) ) ;
#57326=CARTESIAN_POINT ( 'NONE',  ( -4.031976262117261456, 3.142976262117183506, 26.00000000000000711 ) ) ;
#57329=DIRECTION ( 'NONE',  ( -3.491481338843133355E-15, -1.000000000000000000, -1.836970198721029934E-16 ) ) ;
#57334=CARTESIAN_POINT ( 'NONE',  ( 7.532023737882817649, -6.665817930929303969, 54.00000000000000711 ) ) ;
#57336=DIRECTION ( 'NONE',  ( -0.000000000000000000, 3.673940397442059868E-16, -1.000000000000000000 ) ) ;
#57337=ORIENTED_EDGE ( 'NONE', *, *, #52217, .F. ) ;
#57338=FACE_OUTER_BOUND ( 'NONE', #8884, .T. ) ;
#57348=VERTEX_POINT ( 'NONE', #65715 ) ;
#57351=ORIENTED_EDGE ( 'NONE', *, *, #14800, .F. ) ;
#57354=ADVANCED_FACE ( 'NONE', ( #1027 ), #50488, .F. ) ;
#57377=CARTESIAN_POINT ( 'NONE',  ( -6.467976262117258734, 5.242976262117182706, 54.00000000000000711 ) ) ;
#57378=AXIS2_PLACEMENT_3D ( 'NONE', #49145, #7029, #17648 ) ;
#57388=CYLINDRICAL_SURFACE ( 'NONE', #1640, 1.929199999999998028 ) ;
#57390=AXIS2_PLACEMENT_3D ( 'NONE', #27360, #27009, #48579 ) ;
#57393=ORIENTED_EDGE ( 'NONE', *, *, #33728, .T. ) ;
#57396=VERTEX_POINT ( 'NONE', #45876 ) ;
#57405=EDGE_LOOP ( 'NONE', ( #25181, #39714, #58431, #66899, #36446, #12558, #18729, #8177 ) ) ;
#57407=CARTESIAN_POINT ( 'NONE',  ( 10.31452373788279964, 6.642976262117187503, 26.00000000000000711 ) ) ;
#57409=EDGE_CURVE ( 'NONE', #16440, #22852, #19007, .T. ) ;
#57414=FACE_OUTER_BOUND ( 'NONE', #3154, .T. ) ;
#57417=EDGE_CURVE ( 'NONE', #60243, #47516, #54472, .T. ) ;
#57418=EDGE_CURVE ( 'NONE', #53050, #32475, #19350, .T. ) ;
#57429=EDGE_CURVE ( 'NONE', #2486, #32184, #30321, .T. ) ;
#57434=CARTESIAN_POINT ( 'NONE',  ( 4.720772854004770203, 6.344366288193352688, 54.00000000000000711 ) ) ;
#57438=VECTOR ( 'NONE', #30127, 1000.000000000000000 ) ;
#57442=DIRECTION ( 'NONE',  ( 1.836970198721029934E-16, 1.836970198721010706E-16, -1.000000000000000000 ) ) ;
#57447=DIRECTION ( 'NONE',  ( 1.000000000000000000, -1.047444401652940007E-14, 1.836970198721010706E-16 ) ) ;
#57456=DIRECTION ( 'NONE',  ( 1.836970198721029934E-16, 1.836970198721010706E-16, -1.000000000000000000 ) ) ;
#57457=ORIENTED_EDGE ( 'NONE', *, *, #31398, .F. ) ;
#57466=CARTESIAN_POINT ( 'NONE',  ( -3.142976262117251451, 6.486996718459839606, 54.00000000000000711 ) ) ;
#57467=EDGE_CURVE ( 'NONE', #36712, #829, #37567, .T. ) ;
#57471=ORIENTED_EDGE ( 'NONE', *, *, #30226, .F. ) ;
#57478=ORIENTED_EDGE ( 'NONE', *, *, #6529, .F. ) ;
#57486=CIRCLE ( 'NONE', #65377, 0.1749999999999980738 ) ;
#57487=AXIS2_PLACEMENT_3D ( 'NONE', #67751, #56788, #67417 ) ;
#57488=LINE ( 'NONE', #63146, #2924 ) ;
#57492=EDGE_CURVE ( 'NONE', #37690, #46086, #44294, .T. ) ;
#57499=CYLINDRICAL_SURFACE ( 'NONE', #4247, 1.929199999999997139 ) ;
#57501=DIRECTION ( 'NONE',  ( -1.000000000000000000, 0.000000000000000000, 0.000000000000000000 ) ) ;
#57507=CIRCLE ( 'NONE', #54157, 0.1749999999999998224 ) ;
#57512=ADVANCED_FACE ( 'NONE', ( #35531 ), #3030, .F. ) ;
#57513=VECTOR ( 'NONE', #32428, 1000.000000000000000 ) ;
#57516=PLANE ( 'NONE',  #14221 ) ;
#57522=DIRECTION ( 'NONE',  ( 1.836970198721029934E-16, -1.836970198721036344E-16, 1.000000000000000000 ) ) ;
#57527=DIRECTION ( 'NONE',  ( -1.920292680692490463E-14, -1.000000000000000000, -1.836970198721045958E-16 ) ) ;
#57535=DIRECTION ( 'NONE',  ( -0.000000000000000000, 3.673940397442059868E-16, -1.000000000000000000 ) ) ;
#57536=ORIENTED_EDGE ( 'NONE', *, *, #65325, .F. ) ;
#57547=DIRECTION ( 'NONE',  ( 0.7671651518153044247, -0.6414496315691521344, 0.000000000000000000 ) ) ;
#57553=CARTESIAN_POINT ( 'NONE',  ( -2.530476262117327568, -9.737023737882829266, 54.00000000000000711 ) ) ;
#57565=EDGE_CURVE ( 'NONE', #59900, #10965, #65811, .T. ) ;
#57572=LINE ( 'NONE', #58278, #9414 ) ;
#57575=EDGE_CURVE ( 'NONE', #31525, #8587, #54611, .T. ) ;
#57584=DIRECTION ( 'NONE',  ( -1.000000000000000000, 0.000000000000000000, 0.000000000000000000 ) ) ;
#57589=CARTESIAN_POINT ( 'NONE',  ( -3.650476262117221093, 10.49297626211717116, 26.00000000000000711 ) ) ;
#57593=ORIENTED_EDGE ( 'NONE', *, *, #19268, .F. ) ;
#57595=VECTOR ( 'NONE', #61220, 1000.000000000000000 ) ;
#57607=EDGE_CURVE ( 'NONE', #19822, #96, #35247, .T. ) ;
#57614=ORIENTED_EDGE ( 'NONE', *, *, #8605, .F. ) ;
#57621=CARTESIAN_POINT ( 'NONE',  ( 6.836383711243002814, 6.350872789121261519, 54.00000000000000711 ) ) ;
#57625=VERTEX_POINT ( 'NONE', #10763 ) ;
#57626=DIRECTION ( 'NONE',  ( -1.000000000000000000, 0.000000000000000000, 0.000000000000000000 ) ) ;
#57627=VERTEX_POINT ( 'NONE', #21026 ) ;
#57631=CARTESIAN_POINT ( 'NONE',  ( 1.634292677759869639, 8.227189898828703107, 26.00000000000000711 ) ) ;
#57632=DIRECTION ( 'NONE',  ( 1.000000000000000000, -1.047444401652940007E-14, 1.836970198721010706E-16 ) ) ;
#57634=ORIENTED_EDGE ( 'NONE', *, *, #67187, .F. ) ;
#57638=EDGE_LOOP ( 'NONE', ( #11592, #61451, #10194, #42336 ) ) ;
#57640=EDGE_CURVE ( 'NONE', #32481, #8571, #54263, .T. ) ;
#57648=VECTOR ( 'NONE', #7193, 1000.000000000000114 ) ;
#57656=ADVANCED_FACE ( 'NONE', ( #885 ), #32684, .F. ) ;
#57657=DIRECTION ( 'NONE',  ( -1.000000000000000000, 1.883404846338789915E-14, 0.000000000000000000 ) ) ;
#57658=CARTESIAN_POINT ( 'NONE',  ( -8.697938382363135545, 2.406732575409538111, 54.00000000000000711 ) ) ;
#57669=CARTESIAN_POINT ( 'NONE',  ( 9.737023737882806174, 7.955476262117184838, 54.00000000000000711 ) ) ;
#57670=CIRCLE ( 'NONE', #14771, 0.5249999999999994671 ) ;
#57672=VECTOR ( 'NONE', #52376, 1000.000000000000000 ) ;
#57679=CARTESIAN_POINT ( 'NONE',  ( 9.562023737882812569, -8.144523737882813919, 26.00000000000000000 ) ) ;
#57680=DIRECTION ( 'NONE',  ( -1.836970198721029934E-16, 1.836970198721036590E-16, -1.000000000000000000 ) ) ;
#57682=AXIS2_PLACEMENT_3D ( 'NONE', #68852, #32067, #20404 ) ;
#57697=EDGE_LOOP ( 'NONE', ( #17627, #27822, #28330, #62798 ) ) ;
#57701=ORIENTED_EDGE ( 'NONE', *, *, #57429, .F. ) ;
#57707=DIRECTION ( 'NONE',  ( -1.000000000000000000, 7.304098846218132892E-15, 0.000000000000000000 ) ) ;
#57708=ORIENTED_EDGE ( 'NONE', *, *, #36107, .T. ) ;
#57710=DIRECTION ( 'NONE',  ( -0.7671651518152985405, 0.6414496315691592399, 2.587583378555132735E-16 ) ) ;
#57714=CARTESIAN_POINT ( 'NONE',  ( 5.793274621760841292, 6.344366288193348247, 54.00000000000000711 ) ) ;
#57715=ORIENTED_EDGE ( 'NONE', *, *, #43503, .T. ) ;
#57718=DIRECTION ( 'NONE',  ( 1.000000000000000000, 0.000000000000000000, 0.000000000000000000 ) ) ;
#57728=CARTESIAN_POINT ( 'NONE',  ( 8.580623737882818958, -9.703773737882825046, 54.00000000000000711 ) ) ;
#57729=ORIENTED_EDGE ( 'NONE', *, *, #13965, .F. ) ;
#57740=ADVANCED_FACE ( 'NONE', ( #27728 ), #43978, .F. ) ;
#57747=ORIENTED_EDGE ( 'NONE', *, *, #41564, .F. ) ;
#57749=ORIENTED_EDGE ( 'NONE', *, *, #12782, .F. ) ;
#57752=ORIENTED_EDGE ( 'NONE', *, *, #40773, .T. ) ;
#57754=ADVANCED_FACE ( 'NONE', ( #11792 ), #50671, .F. ) ;
#57756=CARTESIAN_POINT ( 'NONE',  ( 7.969523737882813208, 8.821682069070710952, 54.00000000000000711 ) ) ;
#57769=DIRECTION ( 'NONE',  ( 1.836970198721029934E-16, 1.836970198721010706E-16, -1.000000000000000000 ) ) ;
#57777=LINE ( 'NONE', #15000, #50567 ) ;
#57778=DIRECTION ( 'NONE',  ( 8.728482790395504563E-15, 1.000000000000000000, 3.673940397442059868E-16 ) ) ;
#57780=VECTOR ( 'NONE', #27984, 1000.000000000000000 ) ;
#57782=EDGE_LOOP ( 'NONE', ( #52424, #3561, #63816, #16723 ) ) ;
#57792=CARTESIAN_POINT ( 'NONE',  ( 3.003254798005744242, -6.872275254348413576, 54.00000000000000711 ) ) ;
#57796=CARTESIAN_POINT ( 'NONE',  ( -6.467976262117279163, -5.257023737882803083, 54.00000000000000711 ) ) ;
#57809=CARTESIAN_POINT ( 'NONE',  ( -10.03972626211731978, -8.930623737882752877, 54.00000000000000711 ) ) ;
#57811=VERTEX_POINT ( 'NONE', #49634 ) ;
#57813=ADVANCED_FACE ( 'NONE', ( #65889 ), #12485, .F. ) ;
#57820=EDGE_CURVE ( 'NONE', #64281, #1632, #2556, .T. ) ;
#57838=CARTESIAN_POINT ( 'NONE',  ( 2.369523737882793135, -8.835729544836311788, 26.00000000000000000 ) ) ;
#57842=ORIENTED_EDGE ( 'NONE', *, *, #67633, .F. ) ;
#57846=LINE ( 'NONE', #41939, #34896 ) ;
#57855=LINE ( 'NONE', #41241, #11020 ) ;
#57860=CARTESIAN_POINT ( 'NONE',  ( 8.093267424590464998, -8.711985858128699078, 54.00000000000000711 ) ) ;
#57861=CARTESIAN_POINT ( 'NONE',  ( -9.722976262117249746, -3.682023737882726522, 54.00000000000000711 ) ) ;
#57867=DIRECTION ( 'NONE',  ( 1.000000000000000000, 0.000000000000000000, 0.000000000000000000 ) ) ;
#57869=AXIS2_PLACEMENT_3D ( 'NONE', #49562, #27312, #16005 ) ;
#57870=CYLINDRICAL_SURFACE ( 'NONE', #27804, 0.3499999999999996447 ) ;
#57871=CYLINDRICAL_SURFACE ( 'NONE', #19494, 0.1750000000000002387 ) ;
#57874=EDGE_CURVE ( 'NONE', #69312, #20150, #19197, .T. ) ;
#57878=LINE ( 'NONE', #25012, #7281 ) ;
#57886=DIRECTION ( 'NONE',  ( -1.836970198721029934E-16, 1.836970198721036590E-16, -1.000000000000000000 ) ) ;
#57891=AXIS2_PLACEMENT_3D ( 'NONE', #27440, #12204, #572 ) ;
#57892=CARTESIAN_POINT ( 'NONE',  ( 3.664523737882820598, 10.49297626211720491, 54.00000000000000711 ) ) ;
#57897=VERTEX_POINT ( 'NONE', #57377 ) ;
#57904=FACE_OUTER_BOUND ( 'NONE', #38985, .T. ) ;
#57909=DIRECTION ( 'NONE',  ( 1.836970198721029934E-16, 1.836970198721010706E-16, -1.000000000000000000 ) ) ;
#57925=ORIENTED_EDGE ( 'NONE', *, *, #12459, .F. ) ;
#57927=CARTESIAN_POINT ( 'NONE',  ( -1.466476262117236029, 8.598420958951576765, 54.00000000000000711 ) ) ;
#57940=AXIS2_PLACEMENT_3D ( 'NONE', #45424, #50390, #45075 ) ;
#57947=AXIS2_PLACEMENT_3D ( 'NONE', #68482, #15084, #41601 ) ;
#57948=DIRECTION ( 'NONE',  ( 0.7071067811865401342, -0.7071067811865550112, -1.367410260514937456E-30 ) ) ;
#57949=ORIENTED_EDGE ( 'NONE', *, *, #66656, .F. ) ;
#57953=ADVANCED_FACE ( 'NONE', ( #63389 ), #14951, .F. ) ;
#57966=CARTESIAN_POINT ( 'NONE',  ( 2.369523737882786918, -9.562023737882798358, 54.00000000000000711 ) ) ;
#57968=FACE_OUTER_BOUND ( 'NONE', #50827, .T. ) ;
#57978=ORIENTED_EDGE ( 'NONE', *, *, #15845, .T. ) ;
#57984=EDGE_LOOP ( 'NONE', ( #4091, #52839, #65123, #20165 ) ) ;
#57995=VECTOR ( 'NONE', #55112, 1000.000000000000000 ) ;
#57997=CARTESIAN_POINT ( 'NONE',  ( 5.552858015815571591, 7.342976262117199227, 54.00000000000000711 ) ) ;
#58004=ORIENTED_EDGE ( 'NONE', *, *, #2056, .T. ) ;
#58011=ORIENTED_EDGE ( 'NONE', *, *, #59378, .F. ) ;
#58016=ORIENTED_EDGE ( 'NONE', *, *, #16855, .F. ) ;
#58022=LINE ( 'NONE', #20542, #57672 ) ;
#58024=AXIS2_PLACEMENT_3D ( 'NONE', #61331, #46130, #56389 ) ;
#58025=PLANE ( 'NONE',  #55454 ) ;
#58026=ORIENTED_EDGE ( 'NONE', *, *, #62526, .T. ) ;
#58030=LINE ( 'NONE', #51690, #61176 ) ;
#58032=CARTESIAN_POINT ( 'NONE',  ( 6.364920264886885448, -3.677663764522618450, 26.00000000000000711 ) ) ;
#58033=DIRECTION ( 'NONE',  ( -1.570596175624152290E-15, 1.000000000000000000, 3.673940397442059868E-16 ) ) ;
#58040=CYLINDRICAL_SURFACE ( 'NONE', #37857, 1.224999999999997868 ) ;
#58048=ORIENTED_EDGE ( 'NONE', *, *, #3134, .F. ) ;
#58061=ORIENTED_EDGE ( 'NONE', *, *, #45749, .F. ) ;
#58073=LINE ( 'NONE', #19533, #46425 ) ;
#58082=DIRECTION ( 'NONE',  ( -1.836970198721029934E-16, 1.836970198721036590E-16, -1.000000000000000000 ) ) ;
#58084=CIRCLE ( 'NONE', #27595, 0.1749999999999989342 ) ;
#58095=ORIENTED_EDGE ( 'NONE', *, *, #32099, .F. ) ;
#58097=EDGE_CURVE ( 'NONE', #25429, #34832, #43205, .T. ) ;
#58098=EDGE_CURVE ( 'NONE', #8587, #3391, #46617, .T. ) ;
#58099=FACE_OUTER_BOUND ( 'NONE', #8596, .T. ) ;
#58119=ORIENTED_EDGE ( 'NONE', *, *, #68476, .T. ) ;
#58123=LINE ( 'NONE', #62364, #64374 ) ;
#58125=DIRECTION ( 'NONE',  ( -1.836970198721029934E-16, 1.836970198721036344E-16, -1.000000000000000000 ) ) ;
#58139=AXIS2_PLACEMENT_3D ( 'NONE', #49829, #22949, #27922 ) ;
#58141=DIRECTION ( 'NONE',  ( 0.000000000000000000, -3.673940397442059868E-16, 1.000000000000000000 ) ) ;
#58144=CARTESIAN_POINT ( 'NONE',  ( -3.667976262117328190, -9.737023737882820384, 54.00000000000000711 ) ) ;
#58145=EDGE_CURVE ( 'NONE', #48513, #2608, #44238, .T. ) ;
#58149=AXIS2_PLACEMENT_3D ( 'NONE', #66069, #61105, #7363 ) ;
#58150=VERTEX_POINT ( 'NONE', #12395 ) ;
#58157=CARTESIAN_POINT ( 'NONE',  ( -8.697938382363135545, 2.406732575409538111, 54.00000000000000711 ) ) ;
#58163=DIRECTION ( 'NONE',  ( 1.836970198721029934E-16, 1.836970198721010706E-16, -1.000000000000000000 ) ) ;
#58168=AXIS2_PLACEMENT_3D ( 'NONE', #15773, #17415, #6125 ) ;
#58172=VERTEX_POINT ( 'NONE', #66158 ) ;
#58183=ORIENTED_EDGE ( 'NONE', *, *, #27808, .F. ) ;
#58189=LINE ( 'NONE', #46520, #66093 ) ;
#58190=VERTEX_POINT ( 'NONE', #33639 ) ;
#58196=DIRECTION ( 'NONE',  ( -1.000000000000000000, 0.000000000000000000, 0.000000000000000000 ) ) ;
#58198=VERTEX_POINT ( 'NONE', #1454 ) ;
#58216=CARTESIAN_POINT ( 'NONE',  ( -1.466476262117236029, 8.598420958951576765, 54.00000000000000711 ) ) ;
#58217=VERTEX_POINT ( 'NONE', #60504 ) ;
#58222=EDGE_CURVE ( 'NONE', #42575, #37879, #55211, .T. ) ;
#58223=ORIENTED_EDGE ( 'NONE', *, *, #22219, .F. ) ;
#58234=CIRCLE ( 'NONE', #67261, 0.1749999999999989342 ) ;
#58259=CARTESIAN_POINT ( 'NONE',  ( -3.842976262117327124, -10.31452373788281207, 26.00000000000000000 ) ) ;
#58271=EDGE_LOOP ( 'NONE', ( #37247, #9459, #63372, #60066 ) ) ;
#58273=ORIENTED_EDGE ( 'NONE', *, *, #786, .F. ) ;
#58278=CARTESIAN_POINT ( 'NONE',  ( 10.50702373788281996, -6.849523737882823760, 54.00000000000000711 ) ) ;
#58281=DIRECTION ( 'NONE',  ( -0.000000000000000000, -0.000000000000000000, -1.000000000000000000 ) ) ;
#58283=ORIENTED_EDGE ( 'NONE', *, *, #20637, .T. ) ;
#58288=AXIS2_PLACEMENT_3D ( 'NONE', #21805, #58944, #44056 ) ;
#58311=CARTESIAN_POINT ( 'NONE',  ( -5.242976262117280406, -5.257023737882805747, 54.00000000000000711 ) ) ;
#58318=CARTESIAN_POINT ( 'NONE',  ( 8.580623737882818958, -9.703773737882814387, 26.00000000000000000 ) ) ;
#58322=EDGE_CURVE ( 'NONE', #63857, #61547, #34239, .T. ) ;
#58332=ORIENTED_EDGE ( 'NONE', *, *, #66840, .T. ) ;
#58350=AXIS2_PLACEMENT_3D ( 'NONE', #18142, #29450, #24153 ) ;
#58360=VECTOR ( 'NONE', #49376, 1000.000000000000000 ) ;
#58361=AXIS2_PLACEMENT_3D ( 'NONE', #62465, #50817, #2387 ) ;
#58362=VECTOR ( 'NONE', #53772, 1000.000000000000000 ) ;
#58377=ADVANCED_FACE ( 'NONE', ( #603 ), #48693, .T. ) ;
#58380=VERTEX_POINT ( 'NONE', #26788 ) ;
#58381=ADVANCED_FACE ( 'NONE', ( #22174 ), #65313, .T. ) ;
#58386=ORIENTED_EDGE ( 'NONE', *, *, #20539, .F. ) ;
#58392=CARTESIAN_POINT ( 'NONE',  ( -9.722976262117258628, 6.817976262117182884, 54.00000000000000711 ) ) ;
#58393=VECTOR ( 'NONE', #28986, 1000.000000000000000 ) ;
#58394=DIRECTION ( 'NONE',  ( -1.000000000000000000, 0.000000000000000000, 0.000000000000000000 ) ) ;
#58402=LINE ( 'NONE', #31531, #43709 ) ;
#58418=CARTESIAN_POINT ( 'NONE',  ( -6.822336235477446387, 4.135079735113102117, 26.00000000000000711 ) ) ;
#58422=DIRECTION ( 'NONE',  ( 1.000000000000000000, -8.612436249475772606E-15, -1.836970198721045711E-16 ) ) ;
#58426=CARTESIAN_POINT ( 'NONE',  ( -9.547976262117304103, -8.144523737882758851, 54.00000000000000711 ) ) ;
#58427=EDGE_CURVE ( 'NONE', #26334, #65847, #64957, .T. ) ;
#58429=VECTOR ( 'NONE', #14820, 1000.000000000000000 ) ;
#58431=ORIENTED_EDGE ( 'NONE', *, *, #6491, .T. ) ;
#58437=DIRECTION ( 'NONE',  ( -0.6414496315691565753, -0.7671651518153006499, 0.000000000000000000 ) ) ;
#58438=LINE ( 'NONE', #42149, #29869 ) ;
#58441=ORIENTED_EDGE ( 'NONE', *, *, #56565, .T. ) ;
#58446=CARTESIAN_POINT ( 'NONE',  ( 3.664523737882781518, -10.31452373788281029, 54.00000000000000711 ) ) ;
#58450=FACE_OUTER_BOUND ( 'NONE', #21295, .T. ) ;
#58459=FACE_OUTER_BOUND ( 'NONE', #57984, .T. ) ;
#58466=VERTEX_POINT ( 'NONE', #32773 ) ;
#58468=EDGE_CURVE ( 'NONE', #53491, #40746, #26399, .T. ) ;
#58469=CARTESIAN_POINT ( 'NONE',  ( -5.242976262117259978, 5.242976262117182706, 54.00000000000000711 ) ) ;
#58473=EDGE_CURVE ( 'NONE', #54695, #21488, #17540, .T. ) ;
#58474=CARTESIAN_POINT ( 'NONE',  ( 6.849523737882818430, 10.49297626211719603, 54.00000000000000711 ) ) ;
#58481=CARTESIAN_POINT ( 'NONE',  ( 9.912023737882801555, 6.642976262117184838, 54.00000000000000711 ) ) ;
#58484=VECTOR ( 'NONE', #20036, 1000.000000000000000 ) ;
#58489=VERTEX_POINT ( 'NONE', #65646 ) ;
#58490=ORIENTED_EDGE ( 'NONE', *, *, #66662, .F. ) ;
#58497=DIRECTION ( 'NONE',  ( 1.000000000000000000, -1.088659024508174415E-14, 1.836970198721009966E-16 ) ) ;
#58501=AXIS2_PLACEMENT_3D ( 'NONE', #24488, #40391, #39681 ) ;
#58511=VERTEX_POINT ( 'NONE', #60324 ) ;
#58512=CARTESIAN_POINT ( 'NONE',  ( 2.632023737882806191, 6.486996718459881350, 54.00000000000000711 ) ) ;
#58513=DIRECTION ( 'NONE',  ( -1.836970198721029934E-16, 1.836970198721036590E-16, -1.000000000000000000 ) ) ;
#58514=CARTESIAN_POINT ( 'NONE',  ( 9.912023737882778462, 3.842976262117153485, 26.00000000000000711 ) ) ;
#58540=LINE ( 'NONE', #42609, #60251 ) ;
#58554=EDGE_CURVE ( 'NONE', #67915, #17187, #29544, .T. ) ;
#58556=ORIENTED_EDGE ( 'NONE', *, *, #33728, .F. ) ;
#58566=CARTESIAN_POINT ( 'NONE',  ( 1.634292677759859869, -8.241237374594282628, 54.00000000000000711 ) ) ;
#58567=EDGE_LOOP ( 'NONE', ( #15427, #7541, #58677, #56163 ) ) ;
#58569=EDGE_CURVE ( 'NONE', #17943, #69312, #51113, .T. ) ;
#58579=VERTEX_POINT ( 'NONE', #61722 ) ;
#58581=DIRECTION ( 'NONE',  ( -0.000000000000000000, 1.000000000000000000, -0.000000000000000000 ) ) ;
#58582=DIRECTION ( 'NONE',  ( 0.7071067811865436870, -0.7071067811865514585, -2.597868168706495388E-16 ) ) ;
#58584=DIRECTION ( 'NONE',  ( 9.912705577010336396E-15, 1.000000000000000000, 0.000000000000000000 ) ) ;
#58585=DIRECTION ( 'NONE',  ( 1.819560449471430698E-15, 1.000000000000000000, 1.836970198721032892E-16 ) ) ;
#58587=LINE ( 'NONE', #10140, #33495 ) ;
#58610=DIRECTION ( 'NONE',  ( -1.836970198721029934E-16, 1.836970198721036344E-16, -1.000000000000000000 ) ) ;
#58615=DIRECTION ( 'NONE',  ( 0.000000000000000000, 0.000000000000000000, -1.000000000000000000 ) ) ;
#58621=LINE ( 'NONE', #59662, #54186 ) ;
#58626=ORIENTED_EDGE ( 'NONE', *, *, #68428, .F. ) ;
#58636=VERTEX_POINT ( 'NONE', #34486 ) ;
#58637=CARTESIAN_POINT ( 'NONE',  ( 9.562023737882814345, -2.544523737882816050, 26.00000000000000711 ) ) ;
#58639=ORIENTED_EDGE ( 'NONE', *, *, #2509, .F. ) ;
#58643=ADVANCED_FACE ( 'NONE', ( #18946 ), #40502, .T. ) ;
#58649=LINE ( 'NONE', #4903, #49361 ) ;
#58655=AXIS2_PLACEMENT_3D ( 'NONE', #56976, #24105, #8536 ) ;
#58665=AXIS2_PLACEMENT_3D ( 'NONE', #54591, #59193, #37984 ) ;
#58666=DIRECTION ( 'NONE',  ( -0.7071067811865361374, 0.7071067811865588970, 2.810316974849854557E-30 ) ) ;
#58669=EDGE_CURVE ( 'NONE', #36712, #21488, #58540, .T. ) ;
#58672=AXIS2_PLACEMENT_3D ( 'NONE', #18531, #40085, #61668 ) ;
#58674=VERTEX_POINT ( 'NONE', #52527 ) ;
#58677=ORIENTED_EDGE ( 'NONE', *, *, #41463, .F. ) ;
#58683=ORIENTED_EDGE ( 'NONE', *, *, #40878, .T. ) ;
#58689=DIRECTION ( 'NONE',  ( -1.000000000000000000, 3.491481338843133355E-15, 1.836970198721036590E-16 ) ) ;
#58690=EDGE_CURVE ( 'NONE', #1782, #40074, #52171, .T. ) ;
#58692=EDGE_CURVE ( 'NONE', #44397, #17399, #15396, .T. ) ;
#58699=AXIS2_PLACEMENT_3D ( 'NONE', #38846, #32865, #49122 ) ;
#58703=CARTESIAN_POINT ( 'NONE',  ( 7.408280051175162306, 6.775514141871318508, 54.00000000000000711 ) ) ;
#58704=ADVANCED_FACE ( 'NONE', ( #4447 ), #41561, .F. ) ;
#58713=EDGE_CURVE ( 'NONE', #31923, #46792, #47226, .T. ) ;
#58717=CARTESIAN_POINT ( 'NONE',  ( -9.722976262117256852, 2.530476262117183683, 54.00000000000000711 ) ) ;
#58719=LINE ( 'NONE', #36438, #59789 ) ;
#58722=VECTOR ( 'NONE', #59169, 999.9999999999998863 ) ;
#58724=CARTESIAN_POINT ( 'NONE',  ( 10.31452373788280141, 6.835476262117187396, 26.00000000000000711 ) ) ;
#58726=ORIENTED_EDGE ( 'NONE', *, *, #42186, .F. ) ;
#58733=CARTESIAN_POINT ( 'NONE',  ( -9.781776262117313436, -9.795823737882745519, 54.00000000000000711 ) ) ;
#58738=DIRECTION ( 'NONE',  ( 0.000000000000000000, 1.000000000000000000, 0.000000000000000000 ) ) ;
#58739=ORIENTED_EDGE ( 'NONE', *, *, #990, .F. ) ;
#58742=EDGE_CURVE ( 'NONE', #59802, #35090, #53240, .T. ) ;
#58744=DIRECTION ( 'NONE',  ( -0.7671651518153006499, -0.6414496315691565753, -2.356647714346250026E-16 ) ) ;
#58753=DIRECTION ( 'NONE',  ( 4.121462285523434951E-16, 1.000000000000000000, 3.673940397442059868E-16 ) ) ;
#58756=ORIENTED_EDGE ( 'NONE', *, *, #4592, .F. ) ;
#58767=CARTESIAN_POINT ( 'NONE',  ( -8.227189898828745740, 1.620245201994245043, 26.00000000000000711 ) ) ;
#58783=ORIENTED_EDGE ( 'NONE', *, *, #4368, .F. ) ;
#58786=DIRECTION ( 'NONE',  ( -4.121462285523434951E-16, -1.000000000000000000, -0.000000000000000000 ) ) ;
#58788=CARTESIAN_POINT ( 'NONE',  ( 2.544523737882792069, -8.835729544836324223, 54.00000000000000711 ) ) ;
#58789=ADVANCED_FACE ( 'NONE', ( #69480 ), #21041, .F. ) ;
#58794=ORIENTED_EDGE ( 'NONE', *, *, #25663, .F. ) ;
#58808=AXIS2_PLACEMENT_3D ( 'NONE', #47787, #20568, #27284 ) ;
#58809=DIRECTION ( 'NONE',  ( -0.000000000000000000, -0.000000000000000000, -1.000000000000000000 ) ) ;
#58811=DIRECTION ( 'NONE',  ( -1.836970198721029934E-16, 1.836970198721036590E-16, -1.000000000000000000 ) ) ;
#58815=ORIENTED_EDGE ( 'NONE', *, *, #64535, .F. ) ;
#58824=PLANE ( 'NONE',  #30622 ) ;
#58840=LINE ( 'NONE', #10735, #11456 ) ;
#58844=AXIS2_PLACEMENT_3D ( 'NONE', #28110, #42370, #39062 ) ;
#58849=PLANE ( 'NONE',  #58665 ) ;
#58851=CARTESIAN_POINT ( 'NONE',  ( 6.657023737882821202, 10.30047626211719347, 54.00000000000000711 ) ) ;
#58852=EDGE_CURVE ( 'NONE', #27400, #8148, #65942, .T. ) ;
#58856=ORIENTED_EDGE ( 'NONE', *, *, #10801, .T. ) ;
#58859=EDGE_CURVE ( 'NONE', #34373, #43142, #5493, .T. ) ;
#58868=ORIENTED_EDGE ( 'NONE', *, *, #7106, .T. ) ;
#58877=VECTOR ( 'NONE', #68749, 1000.000000000000000 ) ;
#58879=CARTESIAN_POINT ( 'NONE',  ( 3.848229544836322180, -7.532023737882802550, 26.00000000000000000 ) ) ;
#58880=ORIENTED_EDGE ( 'NONE', *, *, #54380, .T. ) ;
#58893=ORIENTED_EDGE ( 'NONE', *, *, #4342, .F. ) ;
#58899=ADVANCED_FACE ( 'NONE', ( #64196 ), #27738, .F. ) ;
#58902=CARTESIAN_POINT ( 'NONE',  ( -9.722976262117288826, -6.832023737882753522, 26.00000000000000000 ) ) ;
#58903=EDGE_CURVE ( 'NONE', #17826, #22769, #12837, .T. ) ;
#58917=CYLINDRICAL_SURFACE ( 'NONE', #18973, 0.5250000000000001332 ) ;
#58918=CARTESIAN_POINT ( 'NONE',  ( -9.689726262117330791, -10.05377373788272699, 54.00000000000000711 ) ) ;
#58922=LINE ( 'NONE', #27436, #19727 ) ;
#58928=CARTESIAN_POINT ( 'NONE',  ( -9.722976262117258628, 6.817976262117182884, 54.00000000000000711 ) ) ;
#58938=EDGE_CURVE ( 'NONE', #28168, #51859, #17464, .T. ) ;
#58944=DIRECTION ( 'NONE',  ( -0.000000000000000000, -0.000000000000000000, -1.000000000000000000 ) ) ;
#58951=CARTESIAN_POINT ( 'NONE',  ( 9.737023737882800845, 7.955476262117190167, 26.00000000000000711 ) ) ;
#58967=EDGE_LOOP ( 'NONE', ( #25674, #41032, #26119, #54347 ) ) ;
#58968=ORIENTED_EDGE ( 'NONE', *, *, #16689, .T. ) ;
#58982=EDGE_CURVE ( 'NONE', #69650, #6870, #39032, .T. ) ;
#58984=LINE ( 'NONE', #11908, #44797 ) ;
#58985=PLANE ( 'NONE',  #40755 ) ;
#58998=CARTESIAN_POINT ( 'NONE',  ( 1.480523737882794233, -8.612468434717207799, 26.00000000000000000 ) ) ;
#58999=DIRECTION ( 'NONE',  ( 0.000000000000000000, -3.673940397442059868E-16, 1.000000000000000000 ) ) ;
#59002=DIRECTION ( 'NONE',  ( -0.000000000000000000, -0.000000000000000000, -1.000000000000000000 ) ) ;
#59009=DIRECTION ( 'NONE',  ( -1.836970198721029934E-16, -1.836970198721010706E-16, 1.000000000000000000 ) ) ;
#59015=EDGE_LOOP ( 'NONE', ( #8315, #38042, #10864, #33194 ) ) ;
#59024=EDGE_LOOP ( 'NONE', ( #56174, #25279, #48730, #26467 ) ) ;
#59026=VERTEX_POINT ( 'NONE', #49982 ) ;
#59028=ORIENTED_EDGE ( 'NONE', *, *, #2090, .F. ) ;
#59033=FACE_OUTER_BOUND ( 'NONE', #59885, .T. ) ;
#59045=DIRECTION ( 'NONE',  ( 0.7071067811865451302, -0.7071067811865500152, -2.597868168706484048E-16 ) ) ;
#59052=ORIENTED_EDGE ( 'NONE', *, *, #35787, .T. ) ;
#59057=ORIENTED_EDGE ( 'NONE', *, *, #40326, .F. ) ;
#59059=VECTOR ( 'NONE', #43357, 1000.000000000000000 ) ;
#59067=VECTOR ( 'NONE', #9791, 1000.000000000000000 ) ;
#59072=DIRECTION ( 'NONE',  ( -1.000000000000000000, 2.135044278125299371E-15, 0.000000000000000000 ) ) ;
#59078=ADVANCED_FACE ( 'NONE', ( #56691 ), #29812, .F. ) ;
#59105=VECTOR ( 'NONE', #5908, 1000.000000000000114 ) ;
#59110=ORIENTED_EDGE ( 'NONE', *, *, #34535, .T. ) ;
#59131=DIRECTION ( 'NONE',  ( 0.000000000000000000, -0.000000000000000000, -1.000000000000000000 ) ) ;
#59133=ORIENTED_EDGE ( 'NONE', *, *, #32966, .T. ) ;
#59134=DIRECTION ( 'NONE',  ( 0.000000000000000000, 3.673940397442059868E-16, -1.000000000000000000 ) ) ;
#59138=ORIENTED_EDGE ( 'NONE', *, *, #65300, .T. ) ;
#59145=CARTESIAN_POINT ( 'NONE',  ( -2.355476262117325525, -9.562023737882830332, 54.00000000000000711 ) ) ;
#59149=EDGE_CURVE ( 'NONE', #22769, #38702, #20258, .T. ) ;
#59156=AXIS2_PLACEMENT_3D ( 'NONE', #38691, #28086, #54273 ) ;
#59158=EDGE_CURVE ( 'NONE', #27929, #1782, #14604, .T. ) ;
#59166=ADVANCED_FACE ( 'NONE', ( #58459 ), #57388, .F. ) ;
#59169=DIRECTION ( 'NONE',  ( -0.7071067811865391350, 0.7071067811865560104, 1.750285133459120294E-30 ) ) ;
#59183=CARTESIAN_POINT ( 'NONE',  ( -8.821682069070824639, -7.969523737882762582, 26.00000000000000000 ) ) ;
#59186=EDGE_CURVE ( 'NONE', #18830, #36149, #51313, .T. ) ;
#59190=EDGE_CURVE ( 'NONE', #62916, #65806, #9664, .T. ) ;
#59193=DIRECTION ( 'NONE',  ( -0.7071067811865552333, -0.7071067811865398012, 2.368893831596300099E-30 ) ) ;
#59201=VECTOR ( 'NONE', #69643, 1000.000000000000000 ) ;
#59206=ORIENTED_EDGE ( 'NONE', *, *, #5254, .F. ) ;
#59208=ORIENTED_EDGE ( 'NONE', *, *, #52227, .F. ) ;
#59218=DIRECTION ( 'NONE',  ( 1.000000000000000000, -1.610765207321970913E-14, 0.000000000000000000 ) ) ;
#59222=CIRCLE ( 'NONE', #60307, 0.1749999999999998224 ) ;
#59226=ORIENTED_EDGE ( 'NONE', *, *, #66621, .T. ) ;
#59228=AXIS2_PLACEMENT_3D ( 'NONE', #8857, #25478, #46335 ) ;
#59231=VERTEX_POINT ( 'NONE', #65489 ) ;
#59234=DIRECTION ( 'NONE',  ( 1.000000000000000000, 0.000000000000000000, 0.000000000000000000 ) ) ;
#59243=EDGE_CURVE ( 'NONE', #40746, #56650, #37932, .T. ) ;
#59245=EDGE_CURVE ( 'NONE', #10498, #34600, #20956, .T. ) ;
#59255=CARTESIAN_POINT ( 'NONE',  ( 8.144523737882810366, 9.547976262117190416, 26.00000000000000711 ) ) ;
#59256=ORIENTED_EDGE ( 'NONE', *, *, #30919, .F. ) ;
#59257=CARTESIAN_POINT ( 'NONE',  ( -9.722976262117256852, 2.530476262117183683, 26.00000000000000711 ) ) ;
#59260=ADVANCED_FACE ( 'NONE', ( #32270 ), #53849, .F. ) ;
#59263=DIRECTION ( 'NONE',  ( 0.000000000000000000, -1.000000000000000000, 0.000000000000000000 ) ) ;
#59278=CARTESIAN_POINT ( 'NONE',  ( 3.664523737882819709, 10.30047626211720413, 54.00000000000000711 ) ) ;
#59283=EDGE_CURVE ( 'NONE', #7725, #45178, #43396, .T. ) ;
#59287=ORIENTED_EDGE ( 'NONE', *, *, #60547, .T. ) ;
#59299=PLANE ( 'NONE',  #23689 ) ;
#59300=LINE ( 'NONE', #4869, #38127 ) ;
#59302=AXIS2_PLACEMENT_3D ( 'NONE', #2957, #51392, #40790 ) ;
#59307=CARTESIAN_POINT ( 'NONE',  ( -3.842976262117329345, -9.912023737882817542, 54.00000000000000711 ) ) ;
#59313=ORIENTED_EDGE ( 'NONE', *, *, #17123, .T. ) ;
#59319=AXIS2_PLACEMENT_3D ( 'NONE', #43264, #47532, #63800 ) ;
#59323=VECTOR ( 'NONE', #12109, 1000.000000000000000 ) ;
#59325=CARTESIAN_POINT ( 'NONE',  ( -3.834182069070823040, -7.357023737882818715, 54.00000000000000711 ) ) ;
#59327=EDGE_CURVE ( 'NONE', #61785, #11023, #11386, .T. ) ;
#59329=DIRECTION ( 'NONE',  ( 0.000000000000000000, -3.673940397442059868E-16, 1.000000000000000000 ) ) ;
#59344=CIRCLE ( 'NONE', #69545, 0.1749999999999998224 ) ;
#59348=DIRECTION ( 'NONE',  ( 0.7071067811865446862, -0.7071067811865503483, 0.000000000000000000 ) ) ;
#59349=DIRECTION ( 'NONE',  ( -0.6414496315691617934, 0.7671651518152962090, 0.000000000000000000 ) ) ;
#59351=ORIENTED_EDGE ( 'NONE', *, *, #43762, .T. ) ;
#59352=VECTOR ( 'NONE', #41215, 1000.000000000000000 ) ;
#59356=CARTESIAN_POINT ( 'NONE',  ( -7.342976262117259623, 6.651770455163663165, 54.00000000000000711 ) ) ;
#59378=EDGE_CURVE ( 'NONE', #47169, #35057, #9543, .T. ) ;
#59382=DIRECTION ( 'NONE',  ( -0.000000000000000000, 3.673940397442059868E-16, -1.000000000000000000 ) ) ;
#59392=AXIS2_PLACEMENT_3D ( 'NONE', #26383, #26733, #52924 ) ;
#59397=ORIENTED_EDGE ( 'NONE', *, *, #57409, .T. ) ;
#59398=VERTEX_POINT ( 'NONE', #60855 ) ;
#59407=VECTOR ( 'NONE', #56951, 1000.000000000000000 ) ;
#59408=FACE_OUTER_BOUND ( 'NONE', #10409, .T. ) ;
#59419=DIRECTION ( 'NONE',  ( 1.000000000000000000, -5.120954910632640039E-15, 0.000000000000000000 ) ) ;
#59422=EDGE_CURVE ( 'NONE', #6870, #61285, #45632, .T. ) ;
#59423=ORIENTED_EDGE ( 'NONE', *, *, #3047, .T. ) ;
#59445=AXIS2_PLACEMENT_3D ( 'NONE', #55258, #6802, #28375 ) ;
#59451=ORIENTED_EDGE ( 'NONE', *, *, #38865, .F. ) ;
#59453=FACE_OUTER_BOUND ( 'NONE', #59488, .T. ) ;
#59455=SURFACE_STYLE_USAGE ( .BOTH. , #32233 ) ;
#59460=CARTESIAN_POINT ( 'NONE',  ( 10.05377373788281581, 8.916576262117182239, 54.00000000000000711 ) ) ;
#59469=PLANE ( 'NONE',  #45657 ) ;
#59476=CIRCLE ( 'NONE', #49340, 0.1749999999999998224 ) ;
#59477=CARTESIAN_POINT ( 'NONE',  ( -6.350872789121377870, -6.836383711242978833, 54.00000000000000711 ) ) ;
#59479=DIRECTION ( 'NONE',  ( -1.000000000000000000, 0.000000000000000000, 0.000000000000000000 ) ) ;
#59482=CYLINDRICAL_SURFACE ( 'NONE', #45622, 0.1749999999999989342 ) ;
#59485=CARTESIAN_POINT ( 'NONE',  ( -4.135079735113166954, 3.663616288757006512, 54.00000000000000711 ) ) ;
#59488=EDGE_LOOP ( 'NONE', ( #3468, #31715, #17459, #55868 ) ) ;
#59491=DIRECTION ( 'NONE',  ( 0.000000000000000000, 1.000000000000000000, 0.000000000000000000 ) ) ;
#59494=ORIENTED_EDGE ( 'NONE', *, *, #60505, .F. ) ;
#59499=VECTOR ( 'NONE', #67058, 1000.000000000000000 ) ;
#59501=VERTEX_POINT ( 'NONE', #39631 ) ;
#59510=AXIS2_PLACEMENT_3D ( 'NONE', #63943, #64629, #16192 ) ;
#59513=EDGE_CURVE ( 'NONE', #58466, #39629, #44250, .T. ) ;
#59517=DIRECTION ( 'NONE',  ( 1.000000000000000000, -3.491481338843133355E-15, -1.836970198721036590E-16 ) ) ;
#59523=DIRECTION ( 'NONE',  ( 0.000000000000000000, -1.000000000000000000, 0.000000000000000000 ) ) ;
#59528=VERTEX_POINT ( 'NONE', #14166 ) ;
#59535=DIRECTION ( 'NONE',  ( -1.836970198721029934E-16, -1.836970198721010706E-16, 1.000000000000000000 ) ) ;
#59537=CARTESIAN_POINT ( 'NONE',  ( -2.530476262117228092, 9.722976262117159152, 26.00000000000000711 ) ) ;
#59550=DIRECTION ( 'NONE',  ( 1.000000000000000000, 0.000000000000000000, 0.000000000000000000 ) ) ;
#59560=VECTOR ( 'NONE', #61961, 1000.000000000000000 ) ;
#59565=EDGE_LOOP ( 'NONE', ( #12376, #15988, #36120, #38208 ) ) ;
#59566=AXIS2_PLACEMENT_3D ( 'NONE', #55682, #39752, #16823 ) ;
#59568=DIRECTION ( 'NONE',  ( -1.610765207321970913E-14, -1.000000000000000000, -1.836970198721006761E-16 ) ) ;
#59583=EDGE_CURVE ( 'NONE', #69650, #20506, #9224, .T. ) ;
#59584=ORIENTED_EDGE ( 'NONE', *, *, #68525, .T. ) ;
#59585=ADVANCED_FACE ( 'NONE', ( #68627 ), #19124, .F. ) ;
#59587=VERTEX_POINT ( 'NONE', #52012 ) ;
#59591=VERTEX_POINT ( 'NONE', #68266 ) ;
#59593=FACE_OUTER_BOUND ( 'NONE', #21603, .T. ) ;
#59596=LINE ( 'NONE', #22798, #47146 ) ;
#59602=ORIENTED_EDGE ( 'NONE', *, *, #4592, .T. ) ;
#59603=FACE_BOUND ( 'NONE', #5776, .T. ) ;
#59605=AXIS2_PLACEMENT_3D ( 'NONE', #24046, #61517, #39945 ) ;
#59611=CARTESIAN_POINT ( 'NONE',  ( -8.130476262117319664, -9.562023737882764607, 26.00000000000000000 ) ) ;
#59615=CARTESIAN_POINT ( 'NONE',  ( 8.241237374594303944, -1.634292677759887846, 54.00000000000000711 ) ) ;
#59618=DIRECTION ( 'NONE',  ( -0.000000000000000000, -0.000000000000000000, -1.000000000000000000 ) ) ;
#59623=ORIENTED_EDGE ( 'NONE', *, *, #12990, .T. ) ;
#59628=VERTEX_POINT ( 'NONE', #10613 ) ;
#59632=ADVANCED_FACE ( 'NONE', ( #21240 ), #5335, .T. ) ;
#59636=VERTEX_POINT ( 'NONE', #58717 ) ;
#59637=EDGE_CURVE ( 'NONE', #52963, #58636, #37843, .T. ) ;
#59639=CARTESIAN_POINT ( 'NONE',  ( 1.634292677759859869, -8.241237374594282628, 54.00000000000000711 ) ) ;
#59647=CARTESIAN_POINT ( 'NONE',  ( 6.501044194225490180, -3.157023737882814540, 26.00000000000000711 ) ) ;
#59649=ADVANCED_FACE ( 'NONE', ( #16 ), #31502, .T. ) ;
#59652=ORIENTED_EDGE ( 'NONE', *, *, #69179, .F. ) ;
#59662=CARTESIAN_POINT ( 'NONE',  ( 9.703773737882785966, -8.580623737882856261, 54.00000000000000711 ) ) ;
#59664=VERTEX_POINT ( 'NONE', #42788 ) ;
#59673=DIRECTION ( 'NONE',  ( 0.000000000000000000, 3.673940397442059868E-16, -1.000000000000000000 ) ) ;
#59674=CARTESIAN_POINT ( 'NONE',  ( 9.703773737882785966, -9.703773737882823269, 54.00000000000000711 ) ) ;
#59682=ORIENTED_EDGE ( 'NONE', *, *, #64688, .T. ) ;
#59683=EDGE_CURVE ( 'NONE', #3920, #50336, #15593, .T. ) ;
#59686=FACE_OUTER_BOUND ( 'NONE', #44507, .T. ) ;
#59689=LINE ( 'NONE', #55426, #62206 ) ;
#59692=LINE ( 'NONE', #32815, #54324 ) ;
#59695=ORIENTED_EDGE ( 'NONE', *, *, #9495, .F. ) ;
#59696=DIRECTION ( 'NONE',  ( 1.000000000000000000, 0.000000000000000000, -0.000000000000000000 ) ) ;
#59698=AXIS2_PLACEMENT_3D ( 'NONE', #54000, #32076, #48339 ) ;
#59699=DIRECTION ( 'NONE',  ( -8.612436249475772606E-15, -1.000000000000000000, -1.836970198721020566E-16 ) ) ;
#59702=CARTESIAN_POINT ( 'NONE',  ( 1.634292677759859869, -8.241237374594271969, 26.00000000000000000 ) ) ;
#59711=DIRECTION ( 'NONE',  ( 1.836970198721029934E-16, -1.836970198721036344E-16, 1.000000000000000000 ) ) ;
#59716=LINE ( 'NONE', #5973, #61349 ) ;
#59721=CARTESIAN_POINT ( 'NONE',  ( 2.369523737882793135, -8.835729544836320670, 54.00000000000000711 ) ) ;
#59732=EDGE_CURVE ( 'NONE', #8035, #63019, #39547, .T. ) ;
#59735=ORIENTED_EDGE ( 'NONE', *, *, #4505, .F. ) ;
#59738=DIRECTION ( 'NONE',  ( 9.912705577010336396E-15, 1.000000000000000000, 0.000000000000000000 ) ) ;
#59739=ADVANCED_FACE ( 'NONE', ( #60424 ), #1388, .T. ) ;
#59744=EDGE_LOOP ( 'NONE', ( #3290, #25443, #35091, #15708 ) ) ;
#59747=ORIENTED_EDGE ( 'NONE', *, *, #57874, .T. ) ;
#59751=CIRCLE ( 'NONE', #14570, 1.929199999999997139 ) ;
#59764=VECTOR ( 'NONE', #66389, 1000.000000000000000 ) ;
#59787=LINE ( 'NONE', #31884, #29911 ) ;
#59789=VECTOR ( 'NONE', #53415, 1000.000000000000000 ) ;
#59797=CARTESIAN_POINT ( 'NONE',  ( -9.781776262117249487, 10.49297626211718359, 54.00000000000000711 ) ) ;
#59799=VECTOR ( 'NONE', #45794, 1000.000000000000000 ) ;
#59801=EDGE_CURVE ( 'NONE', #35057, #20416, #11633, .T. ) ;
#59802=VERTEX_POINT ( 'NONE', #55485 ) ;
#59809=AXIS2_PLACEMENT_3D ( 'NONE', #64333, #54076, #21206 ) ;
#59817=ORIENTED_EDGE ( 'NONE', *, *, #17034, .F. ) ;
#59834=CARTESIAN_POINT ( 'NONE',  ( -6.350872789121327244, 3.663616288756986084, 26.00000000000000711 ) ) ;
#59842=ORIENTED_EDGE ( 'NONE', *, *, #4902, .F. ) ;
#59843=ORIENTED_EDGE ( 'NONE', *, *, #16546, .T. ) ;
#59848=AXIS2_PLACEMENT_3D ( 'NONE', #34194, #66729, #49454 ) ;
#59857=DIRECTION ( 'NONE',  ( -1.000000000000000000, 0.000000000000000000, 0.000000000000000000 ) ) ;
#59858=CARTESIAN_POINT ( 'NONE',  ( -4.947141984184539432, -7.357023737882807168, 54.00000000000000711 ) ) ;
#59865=FACE_OUTER_BOUND ( 'NONE', #20001, .T. ) ;
#59869=PLANE ( 'NONE',  #43647 ) ;
#59877=LINE ( 'NONE', #49613, #5228 ) ;
#59882=ORIENTED_EDGE ( 'NONE', *, *, #42323, .F. ) ;
#59883=LINE ( 'NONE', #11438, #61753 ) ;
#59885=EDGE_LOOP ( 'NONE', ( #54009, #8657, #6907, #53878 ) ) ;
#59900=VERTEX_POINT ( 'NONE', #67126 ) ;
#59910=CARTESIAN_POINT ( 'NONE',  ( 7.357023737882817827, -4.961189459950063885, 54.00000000000000711 ) ) ;
#59919=VECTOR ( 'NONE', #46284, 1000.000000000000000 ) ;
#59920=LINE ( 'NONE', #44334, #7916 ) ;
#59931=CARTESIAN_POINT ( 'NONE',  ( 6.836383711242970840, 4.135079735113107446, 26.00000000000000711 ) ) ;
#59938=DIRECTION ( 'NONE',  ( -1.000000000000000000, 0.000000000000000000, 0.000000000000000000 ) ) ;
#59942=ORIENTED_EDGE ( 'NONE', *, *, #3174, .T. ) ;
#59947=VECTOR ( 'NONE', #36579, 1000.000000000000114 ) ;
#59956=ORIENTED_EDGE ( 'NONE', *, *, #61270, .F. ) ;
#59964=DIRECTION ( 'NONE',  ( -0.000000000000000000, -0.000000000000000000, -1.000000000000000000 ) ) ;
#59970=ORIENTED_EDGE ( 'NONE', *, *, #43807, .F. ) ;
#59973=EDGE_CURVE ( 'NONE', #12301, #47019, #37858, .T. ) ;
#59980=VERTEX_POINT ( 'NONE', #40948 ) ;
#59982=EDGE_CURVE ( 'NONE', #24664, #36931, #46254, .T. ) ;
#59987=FACE_OUTER_BOUND ( 'NONE', #55128, .T. ) ;
#59988=DIRECTION ( 'NONE',  ( -1.000000000000000000, 0.000000000000000000, 0.000000000000000000 ) ) ;
#60017=DIRECTION ( 'NONE',  ( -0.7671651518152939886, 0.6414496315691644579, 0.000000000000000000 ) ) ;
#60022=DIRECTION ( 'NONE',  ( -0.7071067811865527908, -0.7071067811865422437, 0.000000000000000000 ) ) ;
#60029=CARTESIAN_POINT ( 'NONE',  ( 7.969523737882816761, 9.547976262117186863, 54.00000000000000711 ) ) ;
#60033=DIRECTION ( 'NONE',  ( 9.912705577010386883E-15, 1.000000000000000000, 0.000000000000000000 ) ) ;
#60055=DIRECTION ( 'NONE',  ( 8.802523127157697409E-15, 1.000000000000000000, 0.000000000000000000 ) ) ;
#60063=CIRCLE ( 'NONE', #38626, 1.224999999999999423 ) ;
#60066=ORIENTED_EDGE ( 'NONE', *, *, #39139, .T. ) ;
#60067=ORIENTED_EDGE ( 'NONE', *, *, #568, .F. ) ;
#60070=ORIENTED_EDGE ( 'NONE', *, *, #25026, .T. ) ;
#60073=DIRECTION ( 'NONE',  ( -1.000000000000000000, 1.047444401652940007E-14, -1.836970198721010952E-16 ) ) ;
#60074=DIRECTION ( 'NONE',  ( -1.836970198721029934E-16, 1.836970198721036344E-16, -1.000000000000000000 ) ) ;
#60076=ORIENTED_EDGE ( 'NONE', *, *, #52253, .F. ) ;
#60077=CARTESIAN_POINT ( 'NONE',  ( -1.466476262117236029, 8.598420958951576765, 26.00000000000000711 ) ) ;
#60081=ORIENTED_EDGE ( 'NONE', *, *, #55599, .T. ) ;
#60091=ORIENTED_EDGE ( 'NONE', *, *, #30358, .T. ) ;
#60095=VECTOR ( 'NONE', #13544, 1000.000000000000000 ) ;
#60098=LINE ( 'NONE', #44175, #41390 ) ;
#60113=DIRECTION ( 'NONE',  ( 0.000000000000000000, 3.673940397442059868E-16, -1.000000000000000000 ) ) ;
#60116=ADVANCED_FACE ( 'NONE', ( #24175 ), #65330, .F. ) ;
#60131=ADVANCED_FACE ( 'NONE', ( #13913 ), #44086, .F. ) ;
#60133=CARTESIAN_POINT ( 'NONE',  ( 3.682023737882814451, 9.897976262117207824, 26.00000000000000711 ) ) ;
#60140=ORIENTED_EDGE ( 'NONE', *, *, #59186, .T. ) ;
#60164=LINE ( 'NONE', #17041, #40902 ) ;
#60167=ORIENTED_EDGE ( 'NONE', *, *, #21973, .F. ) ;
#60176=CARTESIAN_POINT ( 'NONE',  ( -8.598420958951683346, 1.466476262117183182, 26.00000000000000711 ) ) ;
#60178=VECTOR ( 'NONE', #64173, 1000.000000000000000 ) ;
#60185=EDGE_CURVE ( 'NONE', #64953, #17826, #65990, .T. ) ;
#60189=ORIENTED_EDGE ( 'NONE', *, *, #31507, .T. ) ;
#60195=EDGE_CURVE ( 'NONE', #24795, #55692, #56699, .T. ) ;
#60203=AXIS2_PLACEMENT_3D ( 'NONE', #52801, #4358, #69037 ) ;
#60206=DIRECTION ( 'NONE',  ( -8.903847840905249551E-15, -1.000000000000000000, -1.836970198721027222E-16 ) ) ;
#60210=DIRECTION ( 'NONE',  ( 1.836970198721029934E-16, 1.836970198721010706E-16, -1.000000000000000000 ) ) ;
#60211=AXIS2_PLACEMENT_3D ( 'NONE', #25582, #47147, #10017 ) ;
#60213=ORIENTED_EDGE ( 'NONE', *, *, #9797, .T. ) ;
#60232=CARTESIAN_POINT ( 'NONE',  ( -9.880476262117236175, 7.447976262117216528, 25.99999580000000421 ) ) ;
#60234=LINE ( 'NONE', #33376, #45127 ) ;
#60238=AXIS2_PLACEMENT_3D ( 'NONE', #2301, #12203, #33776 ) ;
#60240=EDGE_CURVE ( 'NONE', #42765, #40726, #46093, .T. ) ;
#60243=VERTEX_POINT ( 'NONE', #25229 ) ;
#60250=VECTOR ( 'NONE', #24391, 1000.000000000000000 ) ;
#60251=VECTOR ( 'NONE', #19631, 1000.000000000000000 ) ;
#60254=ORIENTED_EDGE ( 'NONE', *, *, #54430, .T. ) ;
#60255=CARTESIAN_POINT ( 'NONE',  ( 6.849523737882817542, -10.31452373788281207, 26.00000000000000000 ) ) ;
#60267=PLANE ( 'NONE',  #62788 ) ;
#60268=FACE_OUTER_BOUND ( 'NONE', #20871, .T. ) ;
#60269=LINE ( 'NONE', #53951, #9850 ) ;
#60272=DIRECTION ( 'NONE',  ( -1.836970198721029934E-16, 1.836970198721036590E-16, -1.000000000000000000 ) ) ;
#60273=LINE ( 'NONE', #18180, #40579 ) ;
#60275=ORIENTED_EDGE ( 'NONE', *, *, #55035, .F. ) ;
#60276=FACE_BOUND ( 'NONE', #21257, .T. ) ;
#60278=FACE_OUTER_BOUND ( 'NONE', #60732, .T. ) ;
#60279=LINE ( 'NONE', #5860, #27787 ) ;
#60280=EDGE_CURVE ( 'NONE', #34023, #16156, #33357, .T. ) ;
#60298=DIRECTION ( 'NONE',  ( -1.836970198721029934E-16, 1.836970198721036590E-16, -1.000000000000000000 ) ) ;
#60305=DIRECTION ( 'NONE',  ( 1.000000000000000000, 0.000000000000000000, 0.000000000000000000 ) ) ;
#60306=LINE ( 'NONE', #18215, #22103 ) ;
#60307=AXIS2_PLACEMENT_3D ( 'NONE', #27226, #38189, #59738 ) ;
#60308=FACE_OUTER_BOUND ( 'NONE', #9469, .T. ) ;
#60309=CARTESIAN_POINT ( 'NONE',  ( -2.989207322240233555, -6.872275254348434892, 54.00000000000000711 ) ) ;
#60311=VECTOR ( 'NONE', #23577, 1000.000000000000000 ) ;
#60324=CARTESIAN_POINT ( 'NONE',  ( -6.817976262117261044, 9.722976262117182245, 54.00000000000000711 ) ) ;
#60329=DIRECTION ( 'NONE',  ( 9.912705577010336396E-15, 1.000000000000000000, 0.000000000000000000 ) ) ;
#60331=EDGE_CURVE ( 'NONE', #51859, #14190, #62697, .T. ) ;
#60345=ORIENTED_EDGE ( 'NONE', *, *, #36674, .T. ) ;
#60373=DIRECTION ( 'NONE',  ( 1.000000000000000000, -8.903847840905249551E-15, 1.836970198721013664E-16 ) ) ;
#60374=CARTESIAN_POINT ( 'NONE',  ( 0.9555237378828180805, 9.915476262117216777, 54.00000000000000711 ) ) ;
#60387=CARTESIAN_POINT ( 'NONE',  ( 6.849523737882817542, -10.50702373788281463, 26.00000000000000000 ) ) ;
#60390=VECTOR ( 'NONE', #67574, 1000.000000000000114 ) ;
#60394=EDGE_CURVE ( 'NONE', #34404, #18663, #22018, .T. ) ;
#60396=DIRECTION ( 'NONE',  ( 1.000000000000000000, -3.491481338843133355E-15, -1.836970198721036344E-16 ) ) ;
#60398=VECTOR ( 'NONE', #38838, 1000.000000000000000 ) ;
#60404=ORIENTED_EDGE ( 'NONE', *, *, #61407, .T. ) ;
#60408=ORIENTED_EDGE ( 'NONE', *, *, #1661, .F. ) ;
#60419=CARTESIAN_POINT ( 'NONE',  ( -1.466476262117230034, 9.390476262117152473, 26.00000000000000711 ) ) ;
#60424=FACE_OUTER_BOUND ( 'NONE', #12820, .T. ) ;
#60427=EDGE_CURVE ( 'NONE', #61728, #56196, #55957, .T. ) ;
#60428=ORIENTED_EDGE ( 'NONE', *, *, #29069, .T. ) ;
#60432=EDGE_CURVE ( 'NONE', #2395, #17328, #16722, .T. ) ;
#60436=EDGE_LOOP ( 'NONE', ( #25929, #12291, #53192, #56852 ) ) ;
#60444=VECTOR ( 'NONE', #66722, 1000.000000000000000 ) ;
#60448=LINE ( 'NONE', #43849, #14777 ) ;
#60451=CARTESIAN_POINT ( 'NONE',  ( -6.822336235477446387, 4.135079735113102117, 54.00000000000000711 ) ) ;
#60461=DIRECTION ( 'NONE',  ( -1.260948829465469904E-14, -1.000000000000000000, -1.836970198721033632E-16 ) ) ;
#60462=EDGE_CURVE ( 'NONE', #42050, #20416, #42881, .T. ) ;
#60470=DIRECTION ( 'NONE',  ( 1.836970198721029934E-16, 1.836970198721010706E-16, -1.000000000000000000 ) ) ;
#60471=CIRCLE ( 'NONE', #49183, 1.224999999999998757 ) ;
#60473=ORIENTED_EDGE ( 'NONE', *, *, #65625, .T. ) ;
#60476=EDGE_CURVE ( 'NONE', #67341, #59636, #45812, .T. ) ;
#60481=LINE ( 'NONE', #17705, #16158 ) ;
#60484=ORIENTED_EDGE ( 'NONE', *, *, #57820, .F. ) ;
#60485=AXIS2_PLACEMENT_3D ( 'NONE', #9417, #68817, #64564 ) ;
#60496=ORIENTED_EDGE ( 'NONE', *, *, #13414, .F. ) ;
#60498=EDGE_CURVE ( 'NONE', #42074, #41827, #26631, .T. ) ;
#60504=CARTESIAN_POINT ( 'NONE',  ( -8.566576262117260754, 8.916576262117214213, 54.00000000000000711 ) ) ;
#60505=EDGE_CURVE ( 'NONE', #53865, #50705, #36807, .T. ) ;
#60515=ORIENTED_EDGE ( 'NONE', *, *, #41851, .T. ) ;
#60522=DIRECTION ( 'NONE',  ( -1.000000000000000000, 1.254221251785257731E-14, 1.836970198721053107E-16 ) ) ;
#60523=ORIENTED_EDGE ( 'NONE', *, *, #10437, .F. ) ;
#60524=ORIENTED_EDGE ( 'NONE', *, *, #32301, .T. ) ;
#60525=VECTOR ( 'NONE', #8450, 1000.000000000000000 ) ;
#60527=CARTESIAN_POINT ( 'NONE',  ( -3.650476262117221093, 10.49297626211717116, 54.00000000000000711 ) ) ;
#60528=ORIENTED_EDGE ( 'NONE', *, *, #62482, .T. ) ;
#60530=ORIENTED_EDGE ( 'NONE', *, *, #30172, .F. ) ;
#60543=CARTESIAN_POINT ( 'NONE',  ( -9.722976262117237312, 7.605476262117214503, 26.00000000000000711 ) ) ;
#60546=VECTOR ( 'NONE', #49298, 1000.000000000000000 ) ;
#60547=EDGE_CURVE ( 'NONE', #22546, #45122, #2866, .T. ) ;
#60553=AXIS2_PLACEMENT_3D ( 'NONE', #68314, #68675, #14928 ) ;
#60554=VECTOR ( 'NONE', #26541, 1000.000000000000000 ) ;
#60559=AXIS2_PLACEMENT_3D ( 'NONE', #5783, #32300, #59523 ) ;
#60563=ORIENTED_EDGE ( 'NONE', *, *, #24043, .F. ) ;
#60566=DIRECTION ( 'NONE',  ( 1.000000000000000000, 2.135044278125301343E-15, -0.000000000000000000 ) ) ;
#60570=DIRECTION ( 'NONE',  ( -0.6414496315691420314, 0.7671651518153128624, 2.587583378555127804E-16 ) ) ;
#60576=LINE ( 'NONE', #55285, #52536 ) ;
#60578=CARTESIAN_POINT ( 'NONE',  ( 9.912023737882782015, 3.667976262117150998, 54.00000000000000711 ) ) ;
#60597=EDGE_CURVE ( 'NONE', #15946, #62916, #56612, .T. ) ;
#60604=CARTESIAN_POINT ( 'NONE',  ( 6.789561617636943325, -7.408280051175178293, 54.00000000000000711 ) ) ;
#60605=DIRECTION ( 'NONE',  ( 1.836970198721029934E-16, 1.836970198721010706E-16, -1.000000000000000000 ) ) ;
#60619=CARTESIAN_POINT ( 'NONE',  ( -4.135079735113166954, 3.663616288757006512, 26.00000000000000711 ) ) ;
#60626=CARTESIAN_POINT ( 'NONE',  ( -6.350872789121327244, 3.663616288756986084, 26.00000000000000711 ) ) ;
#60629=DIRECTION ( 'NONE',  ( 1.000000000000000000, 0.000000000000000000, 0.000000000000000000 ) ) ;
#60641=CARTESIAN_POINT ( 'NONE',  ( 2.369523737882811787, 9.547976262117209956, 26.00000000000000711 ) ) ;
#60643=EDGE_CURVE ( 'NONE', #9302, #42510, #7814, .T. ) ;
#60646=VECTOR ( 'NONE', #63534, 1000.000000000000000 ) ;
#60650=CARTESIAN_POINT ( 'NONE',  ( -6.467976262117258734, 5.242976262117182706, 54.00000000000000711 ) ) ;
#60652=CYLINDRICAL_SURFACE ( 'NONE', #33411, 0.1749999999999980738 ) ;
#60677=CARTESIAN_POINT ( 'NONE',  ( -2.355476262117320640, -9.562023737882825003, 26.00000000000000711 ) ) ;
#60681=ADVANCED_FACE ( 'NONE', ( #62974 ), #14530, .F. ) ;
#60687=ORIENTED_EDGE ( 'NONE', *, *, #33224, .T. ) ;
#60696=CIRCLE ( 'NONE', #6508, 0.5249999999999994671 ) ;
#60698=CARTESIAN_POINT ( 'NONE',  ( -6.350872789121319251, -3.677663764522589140, 54.00000000000000711 ) ) ;
#60707=AXIS2_PLACEMENT_3D ( 'NONE', #49274, #5794, #38314 ) ;
#60715=VERTEX_POINT ( 'NONE', #9231 ) ;
#60722=EDGE_CURVE ( 'NONE', #43786, #1825, #41746, .T. ) ;
#60725=DIRECTION ( 'NONE',  ( -1.836970198721029934E-16, 1.836970198721036590E-16, -1.000000000000000000 ) ) ;
#60731=CARTESIAN_POINT ( 'NONE',  ( 0.9555237378827876604, -9.404523737882790613, 54.00000000000000711 ) ) ;
#60732=EDGE_LOOP ( 'NONE', ( #4709, #45113, #3795, #66949 ) ) ;
#60759=CIRCLE ( 'NONE', #57390, 1.929199999999998916 ) ;
#60763=CARTESIAN_POINT ( 'NONE',  ( -9.390476262117209316, -1.480523737882732060, 54.00000000000000711 ) ) ;
#60767=LINE ( 'NONE', #34924, #19882 ) ;
#60771=CARTESIAN_POINT ( 'NONE',  ( 4.155633711806658859, -4.720772854004808394, 54.00000000000000711 ) ) ;
#60818=DIRECTION ( 'NONE',  ( -1.000000000000000000, 0.000000000000000000, 0.000000000000000000 ) ) ;
#60820=FACE_OUTER_BOUND ( 'NONE', #18252, .T. ) ;
#60823=CARTESIAN_POINT ( 'NONE',  ( -9.689726262117330791, -10.05377373788272699, 54.00000000000000711 ) ) ;
#60832=CIRCLE ( 'NONE', #30364, 0.5250000000000003553 ) ;
#60839=VECTOR ( 'NONE', #18392, 1000.000000000000000 ) ;
#60841=DIRECTION ( 'NONE',  ( 2.478176394252584099E-15, 1.000000000000000000, 0.000000000000000000 ) ) ;
#60843=DIRECTION ( 'NONE',  ( -1.836970198721029934E-16, 1.836970198721036590E-16, -1.000000000000000000 ) ) ;
#60845=DIRECTION ( 'NONE',  ( -1.836970198721029934E-16, 1.836970198721036590E-16, -1.000000000000000000 ) ) ;
#60846=CARTESIAN_POINT ( 'NONE',  ( 3.724485858128685045, 7.394232575409559693, 54.00000000000000711 ) ) ;
#60847=CARTESIAN_POINT ( 'NONE',  ( -10.03972626211722918, 8.916576262117214213, 26.00000000000000711 ) ) ;
#60852=ORIENTED_EDGE ( 'NONE', *, *, #17026, .F. ) ;
#60855=CARTESIAN_POINT ( 'NONE',  ( -0.9414762621173243806, -9.929523737882846035, 26.00000000000000711 ) ) ;
#60859=DIRECTION ( 'NONE',  ( -0.000000000000000000, -0.000000000000000000, -1.000000000000000000 ) ) ;
#60865=DIRECTION ( 'NONE',  ( 1.000000000000000000, 0.000000000000000000, 0.000000000000000000 ) ) ;
#60880=AXIS2_PLACEMENT_3D ( 'NONE', #49534, #405, #21965 ) ;
#60883=ORIENTED_EDGE ( 'NONE', *, *, #65234, .F. ) ;
#60885=VECTOR ( 'NONE', #4615, 1000.000000000000000 ) ;
#60892=EDGE_CURVE ( 'NONE', #20669, #3213, #20880, .T. ) ;
#60897=ORIENTED_EDGE ( 'NONE', *, *, #26200, .T. ) ;
#60915=PLANE ( 'NONE',  #57007 ) ;
#60918=DIRECTION ( 'NONE',  ( 0.000000000000000000, 3.673940397442059868E-16, -1.000000000000000000 ) ) ;
#60923=PLANE ( 'NONE',  #59698 ) ;
#60944=VERTEX_POINT ( 'NONE', #58724 ) ;
#60947=ORIENTED_EDGE ( 'NONE', *, *, #9528, .F. ) ;
#60955=CARTESIAN_POINT ( 'NONE',  ( -8.566576262117260754, 9.689726262117185129, 54.00000000000000711 ) ) ;
#60966=EDGE_CURVE ( 'NONE', #39317, #44931, #56526, .T. ) ;
#60970=DIRECTION ( 'NONE',  ( -0.7071067811865474617, 0.7071067811865474617, 2.597868168706479611E-16 ) ) ;
#60973=DIRECTION ( 'NONE',  ( -1.000000000000000000, 1.047444401652940007E-14, -1.836970198721010706E-16 ) ) ;
#60977=DIRECTION ( 'NONE',  ( 0.000000000000000000, 0.000000000000000000, 1.000000000000000000 ) ) ;
#60984=CIRCLE ( 'NONE', #44092, 0.3499999999999996447 ) ;
#60985=ORIENTED_EDGE ( 'NONE', *, *, #25157, .T. ) ;
#60990=LINE ( 'NONE', #941, #53873 ) ;
#60996=VECTOR ( 'NONE', #53299, 1000.000000000000114 ) ;
#60998=CARTESIAN_POINT ( 'NONE',  ( -9.722976262117244417, -3.682023737882722081, 26.00000000000000000 ) ) ;
#61001=VERTEX_POINT ( 'NONE', #29291 ) ;
#61009=DIRECTION ( 'NONE',  ( 1.000000000000000000, 0.000000000000000000, 0.000000000000000000 ) ) ;
#61012=DIRECTION ( 'NONE',  ( 1.000000000000000000, -1.047444401652940007E-14, 1.836970198721010706E-16 ) ) ;
#61029=ORIENTED_EDGE ( 'NONE', *, *, #28756, .T. ) ;
#61037=VECTOR ( 'NONE', #61432, 1000.000000000000000 ) ;
#61049=CARTESIAN_POINT ( 'NONE',  ( 9.737023737882815055, -7.969523737882825642, 54.00000000000000711 ) ) ;
#61054=CARTESIAN_POINT ( 'NONE',  ( 8.612468434717188259, 1.991476262117162888, 54.00000000000000711 ) ) ;
#61055=EDGE_CURVE ( 'NONE', #20187, #55919, #17657, .T. ) ;
#61068=LINE ( 'NONE', #23592, #32101 ) ;
#61071=CARTESIAN_POINT ( 'NONE',  ( -3.710438382363177912, -7.408280051175174741, 54.00000000000000711 ) ) ;
#61095=DIRECTION ( 'NONE',  ( -1.836970198721029934E-16, -1.836970198721010706E-16, 1.000000000000000000 ) ) ;
#61100=EDGE_CURVE ( 'NONE', #10947, #35367, #7729, .T. ) ;
#61105=DIRECTION ( 'NONE',  ( 1.836970198721029934E-16, 1.836970198721010706E-16, -1.000000000000000000 ) ) ;
#61110=EDGE_CURVE ( 'NONE', #58198, #9849, #62890, .T. ) ;
#61114=LINE ( 'NONE', #16969, #25801 ) ;
#61120=VERTEX_POINT ( 'NONE', #25059 ) ;
#61124=AXIS2_PLACEMENT_3D ( 'NONE', #64827, #16380, #53527 ) ;
#61135=AXIS2_PLACEMENT_3D ( 'NONE', #5027, #26593, #32244 ) ;
#61137=LINE ( 'NONE', #7401, #6806 ) ;
#61140=DIRECTION ( 'NONE',  ( -1.836970198721029934E-16, -1.836970198721010706E-16, 1.000000000000000000 ) ) ;
#61149=ADVANCED_FACE ( 'NONE', ( #51932 ), #19734, .F. ) ;
#61150=CARTESIAN_POINT ( 'NONE',  ( -9.547976262117254365, 8.130476262117182884, 54.00000000000000711 ) ) ;
#61155=CARTESIAN_POINT ( 'NONE',  ( 6.501044194225443995, 2.617976262117186703, 54.00000000000000711 ) ) ;
#61166=VECTOR ( 'NONE', #14624, 1000.000000000000000 ) ;
#61171=AXIS2_PLACEMENT_3D ( 'NONE', #49451, #5622, #1015 ) ;
#61174=ORIENTED_EDGE ( 'NONE', *, *, #7745, .T. ) ;
#61175=ORIENTED_EDGE ( 'NONE', *, *, #65569, .F. ) ;
#61176=VECTOR ( 'NONE', #36108, 1000.000000000000000 ) ;
#61192=DIRECTION ( 'NONE',  ( -0.000000000000000000, -0.000000000000000000, -1.000000000000000000 ) ) ;
#61199=VECTOR ( 'NONE', #54063, 1000.000000000000000 ) ;
#61206=ADVANCED_FACE ( 'NONE', ( #51584 ), #30003, .T. ) ;
#61211=VERTEX_POINT ( 'NONE', #67841 ) ;
#61213=LINE ( 'NONE', #1488, #67180 ) ;
#61218=EDGE_CURVE ( 'NONE', #58489, #2756, #62827, .T. ) ;
#61220=DIRECTION ( 'NONE',  ( -0.000000000000000000, -0.000000000000000000, -1.000000000000000000 ) ) ;
#61233=EDGE_CURVE ( 'NONE', #64674, #68234, #56871, .T. ) ;
#61234=VERTEX_POINT ( 'NONE', #19392 ) ;
#61239=DIRECTION ( 'NONE',  ( -1.836970198721029934E-16, 1.836970198721036590E-16, -1.000000000000000000 ) ) ;
#61241=FACE_OUTER_BOUND ( 'NONE', #62695, .T. ) ;
#61247=CYLINDRICAL_SURFACE ( 'NONE', #24522, 0.1749999999999980738 ) ;
#61256=ORIENTED_EDGE ( 'NONE', *, *, #41200, .T. ) ;
#61260=LINE ( 'NONE', #55294, #35969 ) ;
#61266=CARTESIAN_POINT ( 'NONE',  ( -8.916576262117361651, -10.05377373788273587, 54.00000000000000711 ) ) ;
#61267=CIRCLE ( 'NONE', #69225, 0.1749999999999998224 ) ;
#61270=EDGE_CURVE ( 'NONE', #21681, #49752, #61705, .T. ) ;
#61282=EDGE_CURVE ( 'NONE', #59628, #28450, #65122, .T. ) ;
#61284=VERTEX_POINT ( 'NONE', #59325 ) ;
#61285=VERTEX_POINT ( 'NONE', #10887 ) ;
#61290=DIRECTION ( 'NONE',  ( 0.000000000000000000, -3.673940397442059868E-16, 1.000000000000000000 ) ) ;
#61295=DIRECTION ( 'NONE',  ( -3.596772705736694889E-15, -1.000000000000000000, 0.000000000000000000 ) ) ;
#61311=EDGE_CURVE ( 'NONE', #18067, #59587, #6365, .T. ) ;
#61316=EDGE_LOOP ( 'NONE', ( #40809, #30401, #47892, #57393 ) ) ;
#61317=FACE_OUTER_BOUND ( 'NONE', #11411, .T. ) ;
#61323=CARTESIAN_POINT ( 'NONE',  ( -6.858227778582841161, -3.003254798005709603, 26.00000000000000711 ) ) ;
#61330=DIRECTION ( 'NONE',  ( 1.000000000000000000, -3.491481338843133355E-15, -1.836970198721036344E-16 ) ) ;
#61331=CARTESIAN_POINT ( 'NONE',  ( -0.9414762621172249046, 9.915476262117151052, 54.00000000000000711 ) ) ;
#61332=CARTESIAN_POINT ( 'NONE',  ( 10.31452373788280497, 6.642976262117183062, 54.00000000000000711 ) ) ;
#61336=PLANE ( 'NONE',  #62616 ) ;
#61345=AXIS2_PLACEMENT_3D ( 'NONE', #39116, #257, #54696 ) ;
#61347=DIRECTION ( 'NONE',  ( -1.000000000000000000, 0.000000000000000000, 0.000000000000000000 ) ) ;
#61349=VECTOR ( 'NONE', #27536, 1000.000000000000227 ) ;
#61350=CARTESIAN_POINT ( 'NONE',  ( -7.290476262117262962, 9.722976262117180468, 54.00000000000000711 ) ) ;
#61364=ORIENTED_EDGE ( 'NONE', *, *, #69401, .T. ) ;
#61365=EDGE_CURVE ( 'NONE', #43477, #9283, #26899, .T. ) ;
#61376=CARTESIAN_POINT ( 'NONE',  ( -9.915476262117259409, 0.9414762621171833823, 54.00000000000000711 ) ) ;
#61380=EDGE_CURVE ( 'NONE', #58636, #44788, #32552, .T. ) ;
#61384=VECTOR ( 'NONE', #3527, 1000.000000000000000 ) ;
#61385=VECTOR ( 'NONE', #63484, 1000.000000000000000 ) ;
#61390=ORIENTED_EDGE ( 'NONE', *, *, #32864, .F. ) ;
#61394=CIRCLE ( 'NONE', #8314, 1.224999999999998757 ) ;
#61395=DIRECTION ( 'NONE',  ( -3.016910393003147986E-15, 1.000000000000000000, 3.673940397442059868E-16 ) ) ;
#61396=AXIS2_PLACEMENT_3D ( 'NONE', #53838, #38938, #60841 ) ;
#61397=VECTOR ( 'NONE', #20223, 999.9999999999998863 ) ;
#61407=EDGE_CURVE ( 'NONE', #26866, #50489, #66260, .T. ) ;
#61410=DIRECTION ( 'NONE',  ( -3.491481338843133355E-15, -1.000000000000000000, -1.836970198721029934E-16 ) ) ;
#61425=VECTOR ( 'NONE', #63805, 1000.000000000000000 ) ;
#61428=CARTESIAN_POINT ( 'NONE',  ( 7.532023737882817649, -3.848229544836335947, 26.00000000000000711 ) ) ;
#61431=VERTEX_POINT ( 'NONE', #16973 ) ;
#61432=DIRECTION ( 'NONE',  ( -1.356437060717832013E-15, -1.000000000000000000, -1.836970198721033878E-16 ) ) ;
#61439=VECTOR ( 'NONE', #17737, 1000.000000000000114 ) ;
#61446=VECTOR ( 'NONE', #63670, 1000.000000000000000 ) ;
#61451=ORIENTED_EDGE ( 'NONE', *, *, #52313, .F. ) ;
#61453=ORIENTED_EDGE ( 'NONE', *, *, #53715, .T. ) ;
#61456=VECTOR ( 'NONE', #45534, 1000.000000000000000 ) ;
#61458=EDGE_CURVE ( 'NONE', #42896, #55318, #44510, .T. ) ;
#61460=ORIENTED_EDGE ( 'NONE', *, *, #34098, .T. ) ;
#61462=ADVANCED_FACE ( 'NONE', ( #34604 ), #22958, .F. ) ;
#61465=ORIENTED_EDGE ( 'NONE', *, *, #31572, .T. ) ;
#61471=PLANE ( 'NONE',  #47054 ) ;
#61473=ORIENTED_EDGE ( 'NONE', *, *, #63353, .F. ) ;
#61476=DIRECTION ( 'NONE',  ( 3.491481338843133355E-15, 1.000000000000000000, 1.836970198721029934E-16 ) ) ;
#61480=CARTESIAN_POINT ( 'NONE',  ( 8.711985858128693749, -8.093267424590470327, 54.00000000000000711 ) ) ;
#61481=CARTESIAN_POINT ( 'NONE',  ( -8.227189898828745740, 1.620245201994245487, 54.00000000000000711 ) ) ;
#61483=LINE ( 'NONE', #56544, #35842 ) ;
#61489=DIRECTION ( 'NONE',  ( 0.000000000000000000, -1.000000000000000000, 0.000000000000000000 ) ) ;
#61491=ORIENTED_EDGE ( 'NONE', *, *, #23918, .F. ) ;
#61501=CARTESIAN_POINT ( 'NONE',  ( 6.849523737882817542, -10.31452373788282095, 54.00000000000000711 ) ) ;
#61503=ADVANCED_FACE ( 'NONE', ( #12327 ), #65750, .F. ) ;
#61507=VECTOR ( 'NONE', #29120, 1000.000000000000114 ) ;
#61517=DIRECTION ( 'NONE',  ( 1.836970198721029934E-16, 1.836970198721010706E-16, -1.000000000000000000 ) ) ;
#61530=DIRECTION ( 'NONE',  ( -0.000000000000000000, -0.000000000000000000, -1.000000000000000000 ) ) ;
#61534=ORIENTED_EDGE ( 'NONE', *, *, #39349, .T. ) ;
#61542=VECTOR ( 'NONE', #59699, 1000.000000000000000 ) ;
#61544=DIRECTION ( 'NONE',  ( 0.000000000000000000, 0.000000000000000000, 1.000000000000000000 ) ) ;
#61547=VERTEX_POINT ( 'NONE', #40263 ) ;
#61551=DIRECTION ( 'NONE',  ( -0.000000000000000000, 3.673940397442059868E-16, -1.000000000000000000 ) ) ;
#61557=DIRECTION ( 'NONE',  ( -1.000000000000000000, 5.120954910632640039E-15, 1.881408311965255020E-30 ) ) ;
#61560=CARTESIAN_POINT ( 'NONE',  ( -7.342976262117259623, 6.651770455163663165, 54.00000000000000711 ) ) ;
#61563=ORIENTED_EDGE ( 'NONE', *, *, #63829, .F. ) ;
#61567=DIRECTION ( 'NONE',  ( 1.000000000000000000, -5.626525616968433909E-15, -1.836970198721040534E-16 ) ) ;
#61568=CARTESIAN_POINT ( 'NONE',  ( 2.544523737882785852, -9.737023737882799068, 54.00000000000000711 ) ) ;
#61572=CARTESIAN_POINT ( 'NONE',  ( -6.822336235477446387, 6.350872789121265072, 54.00000000000000711 ) ) ;
#61589=DIRECTION ( 'NONE',  ( -0.000000000000000000, -0.000000000000000000, -1.000000000000000000 ) ) ;
#61599=AXIS2_PLACEMENT_3D ( 'NONE', #22471, #44014, #60629 ) ;
#61603=ADVANCED_FACE ( 'NONE', ( #38872 ), #6693, .F. ) ;
#61604=ORIENTED_EDGE ( 'NONE', *, *, #47376, .F. ) ;
#61611=EDGE_LOOP ( 'NONE', ( #67838, #14092, #34726, #56582 ) ) ;
#61616=VECTOR ( 'NONE', #38496, 999.9999999999998863 ) ;
#61631=EDGE_CURVE ( 'NONE', #47150, #53417, #39556, .T. ) ;
#61641=ADVANCED_FACE ( 'NONE', ( #42976 ), #10111, .F. ) ;
#61643=ORIENTED_EDGE ( 'NONE', *, *, #54541, .F. ) ;
#61668=DIRECTION ( 'NONE',  ( -1.000000000000000000, 0.000000000000000000, 0.000000000000000000 ) ) ;
#61672=DIRECTION ( 'NONE',  ( 1.000000000000000000, 0.000000000000000000, 0.000000000000000000 ) ) ;
#61685=PLANE ( 'NONE',  #5614 ) ;
#61687=AXIS2_PLACEMENT_3D ( 'NONE', #50289, #29416, #23429 ) ;
#61698=EDGE_CURVE ( 'NONE', #68424, #49997, #40307, .T. ) ;
#61700=ORIENTED_EDGE ( 'NONE', *, *, #21028, .F. ) ;
#61705=CIRCLE ( 'NONE', #7549, 0.1749999999999998224 ) ;
#61709=ORIENTED_EDGE ( 'NONE', *, *, #38535, .F. ) ;
#61710=EDGE_CURVE ( 'NONE', #53664, #47169, #47935, .T. ) ;
#61722=CARTESIAN_POINT ( 'NONE',  ( 6.501044194225444883, 3.142976262117191943, 26.00000000000000711 ) ) ;
#61728=VERTEX_POINT ( 'NONE', #58902 ) ;
#61737=EDGE_CURVE ( 'NONE', #61284, #27400, #21411, .T. ) ;
#61738=CARTESIAN_POINT ( 'NONE',  ( -9.897976262117248680, -3.682023737882723857, 54.00000000000000711 ) ) ;
#61745=ORIENTED_EDGE ( 'NONE', *, *, #37622, .F. ) ;
#61753=VECTOR ( 'NONE', #32669, 1000.000000000000000 ) ;
#61759=ORIENTED_EDGE ( 'NONE', *, *, #10798, .T. ) ;
#61760=ORIENTED_EDGE ( 'NONE', *, *, #44785, .T. ) ;
#61761=CARTESIAN_POINT ( 'NONE',  ( 6.358413763958968623, -4.720772854004790631, 54.00000000000000711 ) ) ;
#61778=DIRECTION ( 'NONE',  ( 3.540251991789408222E-15, 1.000000000000000000, 0.000000000000000000 ) ) ;
#61782=LINE ( 'NONE', #8020, #43340 ) ;
#61785=VERTEX_POINT ( 'NONE', #60626 ) ;
#61789=CYLINDRICAL_SURFACE ( 'NONE', #35305, 0.5249999999999994671 ) ;
#61790=EDGE_CURVE ( 'NONE', #56837, #52982, #60269, .T. ) ;
#61803=EDGE_CURVE ( 'NONE', #56322, #60944, #59596, .T. ) ;
#61807=CARTESIAN_POINT ( 'NONE',  ( 6.657023737882816761, 9.897976262117193613, 54.00000000000000711 ) ) ;
#61808=ORIENTED_EDGE ( 'NONE', *, *, #16289, .F. ) ;
#61813=EDGE_CURVE ( 'NONE', #25655, #58150, #27065, .T. ) ;
#61817=DIRECTION ( 'NONE',  ( -6.508391731846281342E-15, -1.000000000000000000, -1.836970198721024757E-16 ) ) ;
#61822=VECTOR ( 'NONE', #4480, 1000.000000000000000 ) ;
#61833=ORIENTED_EDGE ( 'NONE', *, *, #68188, .F. ) ;
#61843=LINE ( 'NONE', #51934, #21145 ) ;
#61845=PLANE ( 'NONE',  #21538 ) ;
#61846=EDGE_LOOP ( 'NONE', ( #8937, #44822, #51296, #33340 ) ) ;
#61850=ORIENTED_EDGE ( 'NONE', *, *, #43807, .T. ) ;
#61851=LINE ( 'NONE', #51946, #16259 ) ;
#61856=CARTESIAN_POINT ( 'NONE',  ( 3.664523737882781518, -10.31452373788279964, 26.00000000000000000 ) ) ;
#61857=DIRECTION ( 'NONE',  ( -0.000000000000000000, -0.000000000000000000, -1.000000000000000000 ) ) ;
#61861=LINE ( 'NONE', #13419, #53736 ) ;
#61862=AXIS2_PLACEMENT_3D ( 'NONE', #10672, #57710, #30844 ) ;
#61865=VERTEX_POINT ( 'NONE', #55331 ) ;
#61869=VECTOR ( 'NONE', #22401, 1000.000000000000000 ) ;
#61871=EDGE_LOOP ( 'NONE', ( #64144, #34338, #9360, #47076, #28351, #26299, #58639, #11652 ) ) ;
#61878=CARTESIAN_POINT ( 'NONE',  ( 3.157023737882809655, -6.501044194225480410, 54.00000000000000711 ) ) ;
#61879=EDGE_CURVE ( 'NONE', #50336, #1385, #51625, .T. ) ;
#61888=CARTESIAN_POINT ( 'NONE',  ( -3.142976262117261221, 4.031976262117183296, 54.00000000000000711 ) ) ;
#61895=LINE ( 'NONE', #56929, #66267 ) ;
#61898=AXIS2_PLACEMENT_3D ( 'NONE', #44554, #2821, #45964 ) ;
#61901=CARTESIAN_POINT ( 'NONE',  ( -9.547976262117304103, -8.144523737882758851, 54.00000000000000711 ) ) ;
#61902=FACE_OUTER_BOUND ( 'NONE', #41638, .T. ) ;
#61926=ORIENTED_EDGE ( 'NONE', *, *, #17746, .F. ) ;
#61931=DIRECTION ( 'NONE',  ( 0.000000000000000000, 0.000000000000000000, 1.000000000000000000 ) ) ;
#61942=DIRECTION ( 'NONE',  ( -1.836970198721029934E-16, 1.836970198721036590E-16, -1.000000000000000000 ) ) ;
#61943=CARTESIAN_POINT ( 'NONE',  ( 10.05377373788281048, 8.916576262117187568, 26.00000000000000711 ) ) ;
#61947=VERTEX_POINT ( 'NONE', #45391 ) ;
#61952=DIRECTION ( 'NONE',  ( -8.359604446858500663E-15, -1.000000000000000000, 0.000000000000000000 ) ) ;
#61953=VECTOR ( 'NONE', #41629, 1000.000000000000000 ) ;
#61961=DIRECTION ( 'NONE',  ( 1.000000000000000000, 0.000000000000000000, 0.000000000000000000 ) ) ;
#61966=DIRECTION ( 'NONE',  ( 0.000000000000000000, 0.000000000000000000, 1.000000000000000000 ) ) ;
#61973=VECTOR ( 'NONE', #27874, 1000.000000000000000 ) ;
#61986=DIRECTION ( 'NONE',  ( 0.000000000000000000, 1.000000000000000000, 0.000000000000000000 ) ) ;
#61988=ORIENTED_EDGE ( 'NONE', *, *, #3622, .T. ) ;
#61993=DIRECTION ( 'NONE',  ( 1.000000000000000000, 0.000000000000000000, 0.000000000000000000 ) ) ;
#62001=CARTESIAN_POINT ( 'NONE',  ( -7.342976262117259623, 3.834182069070703580, 54.00000000000000711 ) ) ;
#62011=AXIS2_PLACEMENT_3D ( 'NONE', #49265, #33677, #17077 ) ;
#62018=VECTOR ( 'NONE', #45778, 1000.000000000000000 ) ;
#62022=CARTESIAN_POINT ( 'NONE',  ( 8.930623737882845248, 8.916576262117187568, 54.00000000000000711 ) ) ;
#62024=DIRECTION ( 'NONE',  ( 0.000000000000000000, 0.000000000000000000, 1.000000000000000000 ) ) ;
#62030=ADVANCED_FACE ( 'NONE', ( #8260 ), #29835, .F. ) ;
#62052=AXIS2_PLACEMENT_3D ( 'NONE', #14866, #36425, #25829 ) ;
#62053=CARTESIAN_POINT ( 'NONE',  ( -9.547976262117254365, 8.130476262117182884, 54.00000000000000711 ) ) ;
#62068=ORIENTED_EDGE ( 'NONE', *, *, #19273, .T. ) ;
#62077=ORIENTED_EDGE ( 'NONE', *, *, #9114, .T. ) ;
#62093=CARTESIAN_POINT ( 'NONE',  ( -6.651770455163781293, -7.357023737882790293, 54.00000000000000711 ) ) ;
#62100=DIRECTION ( 'NONE',  ( -1.000000000000000000, -3.016910393003147986E-15, 0.000000000000000000 ) ) ;
#62120=EDGE_LOOP ( 'NONE', ( #60404, #9885, #54773, #62339 ) ) ;
#62131=CARTESIAN_POINT ( 'NONE',  ( -6.835476262117260227, 10.30047626211718104, 26.00000000000000711 ) ) ;
#62135=FACE_OUTER_BOUND ( 'NONE', #9132, .T. ) ;
#62140=EDGE_LOOP ( 'NONE', ( #53053, #627, #34211, #1607 ) ) ;
#62144=ORIENTED_EDGE ( 'NONE', *, *, #55462, .T. ) ;
#62152=VECTOR ( 'NONE', #43337, 1000.000000000000000 ) ;
#62154=DIRECTION ( 'NONE',  ( 1.836970198721029934E-16, 1.836970198721010706E-16, -1.000000000000000000 ) ) ;
#62156=VERTEX_POINT ( 'NONE', #9326 ) ;
#62170=EDGE_CURVE ( 'NONE', #47387, #60243, #41843, .T. ) ;
#62176=DIRECTION ( 'NONE',  ( 3.491481338843133355E-15, 1.000000000000000000, 0.000000000000000000 ) ) ;
#62179=DIRECTION ( 'NONE',  ( 1.000000000000000000, 0.000000000000000000, 0.000000000000000000 ) ) ;
#62182=VECTOR ( 'NONE', #69928, 1000.000000000000000 ) ;
#62186=VERTEX_POINT ( 'NONE', #5773 ) ;
#62196=LINE ( 'NONE', #51238, #26064 ) ;
#62203=LINE ( 'NONE', #13766, #38922 ) ;
#62206=VECTOR ( 'NONE', #39488, 1000.000000000000000 ) ;
#62213=CARTESIAN_POINT ( 'NONE',  ( -7.342976262117259623, 3.834182069070703580, 54.00000000000000711 ) ) ;
#62215=ORIENTED_EDGE ( 'NONE', *, *, #13042, .F. ) ;
#62233=DIRECTION ( 'NONE',  ( -0.6414496315691698980, -0.7671651518152895477, -2.587583378555116957E-16 ) ) ;
#62235=EDGE_LOOP ( 'NONE', ( #36777, #802, #52284, #24590 ) ) ;
#62238=FACE_OUTER_BOUND ( 'NONE', #41196, .T. ) ;
#62239=AXIS2_PLACEMENT_3D ( 'NONE', #55330, #22111, #65257 ) ;
#62241=VERTEX_POINT ( 'NONE', #1155 ) ;
#62244=DIRECTION ( 'NONE',  ( 0.000000000000000000, 1.000000000000000000, 0.000000000000000000 ) ) ;
#62251=VECTOR ( 'NONE', #34344, 1000.000000000000114 ) ;
#62252=EDGE_CURVE ( 'NONE', #9398, #45363, #5421, .T. ) ;
#62255=ORIENTED_EDGE ( 'NONE', *, *, #9058, .T. ) ;
#62256=ORIENTED_EDGE ( 'NONE', *, *, #28703, .T. ) ;
#62262=VECTOR ( 'NONE', #22345, 1000.000000000000000 ) ;
#62263=ORIENTED_EDGE ( 'NONE', *, *, #42186, .T. ) ;
#62267=ORIENTED_EDGE ( 'NONE', *, *, #50059, .T. ) ;
#62268=AXIS2_PLACEMENT_3D ( 'NONE', #37562, #22678, #7786 ) ;
#62270=DIRECTION ( 'NONE',  ( 1.836970198721029934E-16, 1.836970198721010706E-16, -1.000000000000000000 ) ) ;
#62271=LINE ( 'NONE', #46710, #32893 ) ;
#62272=ORIENTED_EDGE ( 'NONE', *, *, #27890, .F. ) ;
#62276=FACE_OUTER_BOUND ( 'NONE', #34929, .T. ) ;
#62281=CARTESIAN_POINT ( 'NONE',  ( -9.722976262117226653, -2.544523737882726344, 54.00000000000000711 ) ) ;
#62285=LINE ( 'NONE', #13503, #55930 ) ;
#62286=VERTEX_POINT ( 'NONE', #37603 ) ;
#62325=DIRECTION ( 'NONE',  ( -0.000000000000000000, -0.000000000000000000, -1.000000000000000000 ) ) ;
#62326=DIRECTION ( 'NONE',  ( 1.836970198721029934E-16, 1.836970198721010706E-16, -1.000000000000000000 ) ) ;
#62332=DIRECTION ( 'NONE',  ( 1.836970198721029934E-16, 1.836970198721010706E-16, -1.000000000000000000 ) ) ;
#62336=ORIENTED_EDGE ( 'NONE', *, *, #44448, .T. ) ;
#62337=ORIENTED_EDGE ( 'NONE', *, *, #16010, .F. ) ;
#62339=ORIENTED_EDGE ( 'NONE', *, *, #67184, .T. ) ;
#62345=ORIENTED_EDGE ( 'NONE', *, *, #61311, .F. ) ;
#62358=CARTESIAN_POINT ( 'NONE',  ( -9.915476262117200790, -0.9555237378827209360, 54.00000000000000711 ) ) ;
#62361=LINE ( 'NONE', #33748, #27201 ) ;
#62364=CARTESIAN_POINT ( 'NONE',  ( 3.857023737882779635, -10.31452373788281029, 54.00000000000000711 ) ) ;
#62367=DIRECTION ( 'NONE',  ( -0.000000000000000000, 3.673940397442059868E-16, -1.000000000000000000 ) ) ;
#62371=DIRECTION ( 'NONE',  ( 0.000000000000000000, 1.000000000000000000, 0.000000000000000000 ) ) ;
#62372=VECTOR ( 'NONE', #8017, 1000.000000000000000 ) ;
#62376=CARTESIAN_POINT ( 'NONE',  ( 3.664523737882819709, 10.30047626211720413, 54.00000000000000711 ) ) ;
#62378=ORIENTED_EDGE ( 'NONE', *, *, #59973, .T. ) ;
#62387=CARTESIAN_POINT ( 'NONE',  ( -10.30047626211725031, -3.857023737882713466, 54.00000000000000711 ) ) ;
#62391=EDGE_CURVE ( 'NONE', #28477, #34023, #34336, .T. ) ;
#62392=PLANE ( 'NONE',  #35360 ) ;
#62404=ORIENTED_EDGE ( 'NONE', *, *, #11062, .F. ) ;
#62418=ORIENTED_EDGE ( 'NONE', *, *, #57166, .T. ) ;
#62419=VERTEX_POINT ( 'NONE', #45300 ) ;
#62421=CIRCLE ( 'NONE', #38716, 0.1749999999999998224 ) ;
#62425=LINE ( 'NONE', #61376, #26614 ) ;
#62426=AXIS2_PLACEMENT_3D ( 'NONE', #39224, #33234, #11646 ) ;
#62427=LINE ( 'NONE', #13999, #18222 ) ;
#62443=CARTESIAN_POINT ( 'NONE',  ( 10.05377373788281048, 8.916576262117187568, 26.00000000000000711 ) ) ;
#62447=DIRECTION ( 'NONE',  ( 3.510749891857827507E-15, 1.000000000000000000, 0.000000000000000000 ) ) ;
#62461=DIRECTION ( 'NONE',  ( 1.836970198721029934E-16, 1.836970198721010706E-16, -1.000000000000000000 ) ) ;
#62465=CARTESIAN_POINT ( 'NONE',  ( 10.50702373788281996, -6.849523737882823760, 54.00000000000000711 ) ) ;
#62469=VECTOR ( 'NONE', #42296, 1000.000000000000114 ) ;
#62472=CARTESIAN_POINT ( 'NONE',  ( 6.364920264886885448, -6.836383711243021466, 54.00000000000000711 ) ) ;
#62473=ORIENTED_EDGE ( 'NONE', *, *, #37024, .F. ) ;
#62474=LINE ( 'NONE', #17352, #19154 ) ;
#62482=EDGE_CURVE ( 'NONE', #67667, #15946, #28698, .T. ) ;
#62497=ORIENTED_EDGE ( 'NONE', *, *, #25579, .T. ) ;
#62499=ORIENTED_EDGE ( 'NONE', *, *, #56860, .T. ) ;
#62503=CARTESIAN_POINT ( 'NONE',  ( 10.31452373788277654, 3.650476262117150483, 26.00000000000000711 ) ) ;
#62504=CARTESIAN_POINT ( 'NONE',  ( 5.257023737882795977, 5.242976262117205799, 26.00000000000000711 ) ) ;
#62506=EDGE_CURVE ( 'NONE', #28450, #19822, #67232, .T. ) ;
#62514=VERTEX_POINT ( 'NONE', #41405 ) ;
#62516=VECTOR ( 'NONE', #61672, 1000.000000000000000 ) ;
#62519=ORIENTED_EDGE ( 'NONE', *, *, #54393, .T. ) ;
#62521=DIRECTION ( 'NONE',  ( -1.047444401652940007E-14, -1.000000000000000000, -1.836970198721029934E-16 ) ) ;
#62522=DIRECTION ( 'NONE',  ( 9.912705577010312730E-15, 1.000000000000000000, 0.000000000000000000 ) ) ;
#62526=EDGE_CURVE ( 'NONE', #34832, #45723, #28946, .T. ) ;
#62527=CARTESIAN_POINT ( 'NONE',  ( -7.447976262117260049, 9.880476262117177555, 25.99999580000000421 ) ) ;
#62534=CARTESIAN_POINT ( 'NONE',  ( 4.720772854004780861, 4.141586236041042923, 54.00000000000000711 ) ) ;
#62536=DIRECTION ( 'NONE',  ( -0.7071067811865475727, -0.7071067811865475727, -2.597868168706480597E-16 ) ) ;
#62546=ORIENTED_EDGE ( 'NONE', *, *, #68882, .F. ) ;
#62548=EDGE_CURVE ( 'NONE', #54687, #23129, #22201, .T. ) ;
#62552=LINE ( 'NONE', #25095, #6887 ) ;
#62559=ADVANCED_FACE ( 'NONE', ( #42461 ), #25152, .T. ) ;
#62561=AXIS2_PLACEMENT_3D ( 'NONE', #66393, #29948, #33858 ) ;
#62576=ORIENTED_EDGE ( 'NONE', *, *, #55462, .F. ) ;
#62577=DIRECTION ( 'NONE',  ( 0.000000000000000000, 1.000000000000000000, 0.000000000000000000 ) ) ;
#62584=ADVANCED_FACE ( 'NONE', ( #20891 ), #14897, .F. ) ;
#62592=LINE ( 'NONE', #30433, #39828 ) ;
#62599=DIRECTION ( 'NONE',  ( 1.883404846338789915E-14, 1.000000000000000000, 1.836970198721045465E-16 ) ) ;
#62600=EDGE_CURVE ( 'NONE', #42804, #30522, #63690, .T. ) ;
#62603=ORIENTED_EDGE ( 'NONE', *, *, #33697, .T. ) ;
#62606=CARTESIAN_POINT ( 'NONE',  ( -7.342976262117293373, -6.665817930929262225, 54.00000000000000711 ) ) ;
#62608=VECTOR ( 'NONE', #26072, 1000.000000000000000 ) ;
#62616=AXIS2_PLACEMENT_3D ( 'NONE', #50394, #7947, #29523 ) ;
#62620=CARTESIAN_POINT ( 'NONE',  ( 6.832023737882818359, -9.737023737882822161, 54.00000000000000711 ) ) ;
#62624=AXIS2_PLACEMENT_3D ( 'NONE', #44496, #17635, #49133 ) ;
#62628=DIRECTION ( 'NONE',  ( 0.7071067811865500152, 0.7071067811865451302, -4.683861624749757595E-31 ) ) ;
#62629=DIRECTION ( 'NONE',  ( 1.836970198721029934E-16, -1.836970198721036344E-16, 1.000000000000000000 ) ) ;
#62632=CARTESIAN_POINT ( 'NONE',  ( 5.257023737882819070, -5.257023737882825287, 54.00000000000000711 ) ) ;
#62639=CARTESIAN_POINT ( 'NONE',  ( -5.242976262117259978, 5.242976262117182706, 54.00000000000000711 ) ) ;
#62640=CIRCLE ( 'NONE', #32174, 0.1749999999999998224 ) ;
#62641=VECTOR ( 'NONE', #44495, 1000.000000000000000 ) ;
#62646=DIRECTION ( 'NONE',  ( 0.000000000000000000, 1.000000000000000000, 0.000000000000000000 ) ) ;
#62647=EDGE_LOOP ( 'NONE', ( #12916, #18634, #41476, #51816 ) ) ;
#62657=CARTESIAN_POINT ( 'NONE',  ( 3.682023737882786918, -9.737023737882811503, 54.00000000000000711 ) ) ;
#62660=VECTOR ( 'NONE', #10752, 1000.000000000000000 ) ;
#62661=CARTESIAN_POINT ( 'NONE',  ( -4.706725378239251967, -6.358413763958955300, 26.00000000000000711 ) ) ;
#62665=ORIENTED_EDGE ( 'NONE', *, *, #59683, .F. ) ;
#62673=CARTESIAN_POINT ( 'NONE',  ( 8.612468434717184707, 1.991476262117167995, 26.00000000000000711 ) ) ;
#62681=VERTEX_POINT ( 'NONE', #48466 ) ;
#62693=VECTOR ( 'NONE', #8001, 1000.000000000000000 ) ;
#62695=EDGE_LOOP ( 'NONE', ( #62972, #34083, #7268, #52994 ) ) ;
#62697=LINE ( 'NONE', #58474, #35606 ) ;
#62707=LINE ( 'NONE', #57407, #16033 ) ;
#62712=PLANE ( 'NONE',  #69391 ) ;
#62726=DIRECTION ( 'NONE',  ( -1.836970198721029934E-16, -1.836970198721010706E-16, 1.000000000000000000 ) ) ;
#62731=ORIENTED_EDGE ( 'NONE', *, *, #16847, .F. ) ;
#62732=VECTOR ( 'NONE', #58281, 1000.000000000000000 ) ;
#62733=DIRECTION ( 'NONE',  ( 1.000000000000000000, -3.491481338843133355E-15, 0.000000000000000000 ) ) ;
#62742=AXIS2_PLACEMENT_3D ( 'NONE', #42477, #68302, #19853 ) ;
#62745=DIRECTION ( 'NONE',  ( 0.6414496315691494699, -0.7671651518153064231, 0.000000000000000000 ) ) ;
#62764=CIRCLE ( 'NONE', #37950, 0.1749999999999998224 ) ;
#62770=EDGE_LOOP ( 'NONE', ( #39541, #58794, #31185, #18773 ) ) ;
#62782=AXIS2_PLACEMENT_3D ( 'NONE', #35487, #56366, #2278 ) ;
#62788=AXIS2_PLACEMENT_3D ( 'NONE', #11479, #54290, #21758 ) ;
#62798=ORIENTED_EDGE ( 'NONE', *, *, #19737, .T. ) ;
#62815=DIRECTION ( 'NONE',  ( -1.836970198721029934E-16, 1.836970198721036590E-16, -1.000000000000000000 ) ) ;
#62820=CARTESIAN_POINT ( 'NONE',  ( -3.650476262117221093, 10.49297626211717116, 26.00000000000000711 ) ) ;
#62823=DIRECTION ( 'NONE',  ( -0.000000000000000000, -0.000000000000000000, -1.000000000000000000 ) ) ;
#62827=CIRCLE ( 'NONE', #56014, 0.3499999999999996447 ) ;
#62831=CIRCLE ( 'NONE', #15406, 0.1749999999999993783 ) ;
#62832=DIRECTION ( 'NONE',  ( -0.000000000000000000, -0.000000000000000000, -1.000000000000000000 ) ) ;
#62853=DIRECTION ( 'NONE',  ( 3.491481338843133355E-15, 1.000000000000000000, 1.836970198721029934E-16 ) ) ;
#62855=CYLINDRICAL_SURFACE ( 'NONE', #18710, 1.224999999999999423 ) ;
#62856=ORIENTED_EDGE ( 'NONE', *, *, #32900, .T. ) ;
#62858=CARTESIAN_POINT ( 'NONE',  ( 7.186223737882800222, 5.242976262117193365, 54.00000000000000711 ) ) ;
#62873=VERTEX_POINT ( 'NONE', #39909 ) ;
#62875=VECTOR ( 'NONE', #13748, 1000.000000000000000 ) ;
#62878=VERTEX_POINT ( 'NONE', #45567 ) ;
#62880=AXIS2_PLACEMENT_3D ( 'NONE', #18691, #56185, #27927 ) ;
#62887=EDGE_CURVE ( 'NONE', #40074, #40825, #35297, .T. ) ;
#62890=LINE ( 'NONE', #8074, #28951 ) ;
#62891=ORIENTED_EDGE ( 'NONE', *, *, #31245, .F. ) ;
#62897=ORIENTED_EDGE ( 'NONE', *, *, #3274, .T. ) ;
#62898=AXIS2_PLACEMENT_3D ( 'NONE', #16567, #66017, #33507 ) ;
#62900=DIRECTION ( 'NONE',  ( -1.000000000000000000, 0.000000000000000000, 0.000000000000000000 ) ) ;
#62903=DIRECTION ( 'NONE',  ( 1.000000000000000000, 0.000000000000000000, 0.000000000000000000 ) ) ;
#62906=FACE_OUTER_BOUND ( 'NONE', #20282, .T. ) ;
#62916=VERTEX_POINT ( 'NONE', #35658 ) ;
#62918=CIRCLE ( 'NONE', #33582, 0.5249999999999990230 ) ;
#62924=DIRECTION ( 'NONE',  ( -0.000000000000000000, -0.000000000000000000, -1.000000000000000000 ) ) ;
#62925=AXIS2_PLACEMENT_3D ( 'NONE', #10196, #36012, #32113 ) ;
#62934=VERTEX_POINT ( 'NONE', #14463 ) ;
#62935=EDGE_CURVE ( 'NONE', #62681, #3213, #68560, .T. ) ;
#62936=DIRECTION ( 'NONE',  ( -0.000000000000000000, 0.000000000000000000, -1.000000000000000000 ) ) ;
#62943=CIRCLE ( 'NONE', #25657, 0.1749999999999989342 ) ;
#62952=EDGE_CURVE ( 'NONE', #26808, #18477, #22253, .T. ) ;
#62956=LINE ( 'NONE', #64020, #60885 ) ;
#62963=CARTESIAN_POINT ( 'NONE',  ( -7.342976262117259623, 5.538810540049946773, 54.00000000000000711 ) ) ;
#62964=ORIENTED_EDGE ( 'NONE', *, *, #22874, .T. ) ;
#62972=ORIENTED_EDGE ( 'NONE', *, *, #59982, .T. ) ;
#62974=FACE_OUTER_BOUND ( 'NONE', #63287, .T. ) ;
#62986=DIRECTION ( 'NONE',  ( 2.135044278125301343E-15, -1.000000000000000000, -3.673940397442059868E-16 ) ) ;
#62988=EDGE_LOOP ( 'NONE', ( #69009, #15066, #36042, #57302 ) ) ;
#62992=DIRECTION ( 'NONE',  ( 1.836970198721029934E-16, 1.836970198721010706E-16, -1.000000000000000000 ) ) ;
#62995=CARTESIAN_POINT ( 'NONE',  ( -4.135079735113215804, -6.836383711243002814, 54.00000000000000711 ) ) ;
#63009=LINE ( 'NONE', #63717, #68128 ) ;
#63014=PLANE ( 'NONE',  #2034 ) ;
#63015=CARTESIAN_POINT ( 'NONE',  ( -4.135079735113167843, 6.822336235477362010, 26.00000000000000711 ) ) ;
#63019=VERTEX_POINT ( 'NONE', #69249 ) ;
#63022=LINE ( 'NONE', #9631, #56212 ) ;
#63029=ORIENTED_EDGE ( 'NONE', *, *, #69566, .T. ) ;
#63036=CARTESIAN_POINT ( 'NONE',  ( -3.663616288757055806, 6.350872789121238426, 26.00000000000000711 ) ) ;
#63042=ORIENTED_EDGE ( 'NONE', *, *, #35934, .T. ) ;
#63043=EDGE_CURVE ( 'NONE', #24327, #52649, #58649, .T. ) ;
#63046=EDGE_LOOP ( 'NONE', ( #41727, #30611, #27867, #63849 ) ) ;
#63047=FACE_OUTER_BOUND ( 'NONE', #56363, .T. ) ;
#63056=ORIENTED_EDGE ( 'NONE', *, *, #47627, .T. ) ;
#63060=ADVANCED_FACE ( 'NONE', ( #37087 ), #64636, .F. ) ;
#63077=FACE_OUTER_BOUND ( 'NONE', #24538, .T. ) ;
#63079=ORIENTED_EDGE ( 'NONE', *, *, #11672, .T. ) ;
#63084=ORIENTED_EDGE ( 'NONE', *, *, #27409, .T. ) ;
#63086=DIRECTION ( 'NONE',  ( -0.6414496315691539108, 0.7671651518153028704, 0.000000000000000000 ) ) ;
#63091=EDGE_CURVE ( 'NONE', #27495, #3937, #5260, .T. ) ;
#63093=VERTEX_POINT ( 'NONE', #42721 ) ;
#63123=VERTEX_POINT ( 'NONE', #291 ) ;
#63127=DIRECTION ( 'NONE',  ( 1.000000000000000000, -1.047444401652940007E-14, 1.836970198721010706E-16 ) ) ;
#63130=ORIENTED_EDGE ( 'NONE', *, *, #50396, .F. ) ;
#63146=CARTESIAN_POINT ( 'NONE',  ( -4.141586236041130853, -5.793274621760842180, 54.00000000000000711 ) ) ;
#63149=ADVANCED_FACE ( 'NONE', ( #27505 ), #638, .F. ) ;
#63150=ORIENTED_EDGE ( 'NONE', *, *, #34059, .T. ) ;
#63161=ORIENTED_EDGE ( 'NONE', *, *, #15423, .F. ) ;
#63164=DIRECTION ( 'NONE',  ( 3.491481338843133355E-15, 1.000000000000000000, 1.836970198721029934E-16 ) ) ;
#63167=CARTESIAN_POINT ( 'NONE',  ( 0.9555237378828111972, 9.390476262117219974, 26.00000000000000711 ) ) ;
#63176=CARTESIAN_POINT ( 'NONE',  ( 5.257023737882819070, -5.257023737882825287, 54.00000000000000711 ) ) ;
#63181=CARTESIAN_POINT ( 'NONE',  ( -6.651770455163778628, -7.532023737882784786, 26.00000000000000000 ) ) ;
#63185=DIRECTION ( 'NONE',  ( 0.000000000000000000, 1.000000000000000000, 0.000000000000000000 ) ) ;
#63186=VECTOR ( 'NONE', #13073, 1000.000000000000000 ) ;
#63189=DIRECTION ( 'NONE',  ( -1.000000000000000000, 6.308085367188447236E-15, 0.000000000000000000 ) ) ;
#63194=DIRECTION ( 'NONE',  ( -0.000000000000000000, -0.000000000000000000, -1.000000000000000000 ) ) ;
#63199=VECTOR ( 'NONE', #26797, 1000.000000000000000 ) ;
#63232=ORIENTED_EDGE ( 'NONE', *, *, #58569, .T. ) ;
#63235=DIRECTION ( 'NONE',  ( 0.000000000000000000, -3.673940397442059868E-16, 1.000000000000000000 ) ) ;
#63243=DIRECTION ( 'NONE',  ( 1.047444401652940007E-14, 1.000000000000000000, 1.836970198721029934E-16 ) ) ;
#63250=CARTESIAN_POINT ( 'NONE',  ( -5.242976262117275077, -5.257023737882800418, 26.00000000000000711 ) ) ;
#63253=CYLINDRICAL_SURFACE ( 'NONE', #46730, 0.5249999999999994671 ) ;
#63255=CARTESIAN_POINT ( 'NONE',  ( 7.357023737882817827, -4.961189459950063885, 54.00000000000000711 ) ) ;
#63261=PLANE ( 'NONE',  #42103 ) ;
#63264=CARTESIAN_POINT ( 'NONE',  ( -4.947141984184481700, 7.342976262117180575, 54.00000000000000711 ) ) ;
#63275=ORIENTED_EDGE ( 'NONE', *, *, #42176, .T. ) ;
#63279=CARTESIAN_POINT ( 'NONE',  ( 4.155633711806658859, -5.793274621760842180, 54.00000000000000711 ) ) ;
#63282=VECTOR ( 'NONE', #26409, 1000.000000000000114 ) ;
#63287=EDGE_LOOP ( 'NONE', ( #45020, #708, #10035, #10830 ) ) ;
#63291=CARTESIAN_POINT ( 'NONE',  ( 3.664523737882820598, 10.49297626211720491, 54.00000000000000711 ) ) ;
#63303=FACE_OUTER_BOUND ( 'NONE', #271, .T. ) ;
#63311=LINE ( 'NONE', #4278, #23147 ) ;
#63321=LINE ( 'NONE', #9579, #28506 ) ;
#63336=VERTEX_POINT ( 'NONE', #67427 ) ;
#63337=LINE ( 'NONE', #31869, #66203 ) ;
#63344=DIRECTION ( 'NONE',  ( -9.912705577010336396E-15, -1.000000000000000000, 0.000000000000000000 ) ) ;
#63347=AXIS2_PLACEMENT_3D ( 'NONE', #68158, #30688, #3809 ) ;
#63353=EDGE_CURVE ( 'NONE', #17119, #46858, #20029, .T. ) ;
#63356=ORIENTED_EDGE ( 'NONE', *, *, #67786, .F. ) ;
#63358=CYLINDRICAL_SURFACE ( 'NONE', #32394, 1.224999999999999423 ) ;
#63366=DIRECTION ( 'NONE',  ( 0.000000000000000000, -1.000000000000000000, 0.000000000000000000 ) ) ;
#63367=PLANE ( 'NONE',  #53997 ) ;
#63372=ORIENTED_EDGE ( 'NONE', *, *, #15360, .F. ) ;
#63375=DIRECTION ( 'NONE',  ( 1.221996412923863792E-14, 1.000000000000000000, 1.836970198721013910E-16 ) ) ;
#63377=EDGE_CURVE ( 'NONE', #47907, #5174, #60696, .T. ) ;
#63386=VECTOR ( 'NONE', #53876, 1000.000000000000000 ) ;
#63388=DIRECTION ( 'NONE',  ( -0.000000000000000000, 1.000000000000000000, -0.000000000000000000 ) ) ;
#63389=FACE_OUTER_BOUND ( 'NONE', #69755, .T. ) ;
#63403=CARTESIAN_POINT ( 'NONE',  ( -6.835476262117260227, 10.49297626211718359, 54.00000000000000711 ) ) ;
#63404=VECTOR ( 'NONE', #21986, 1000.000000000000114 ) ;
#63405=DIRECTION ( 'NONE',  ( 1.836970198721029934E-16, 1.836970198721010706E-16, -1.000000000000000000 ) ) ;
#63411=EDGE_LOOP ( 'NONE', ( #12800, #49343, #59226, #17566 ) ) ;
#63412=ORIENTED_EDGE ( 'NONE', *, *, #64017, .F. ) ;
#63413=DIRECTION ( 'NONE',  ( 1.836970198721029934E-16, 1.836970198721010706E-16, -1.000000000000000000 ) ) ;
#63414=EDGE_CURVE ( 'NONE', #39526, #6741, #4127, .T. ) ;
#63419=ORIENTED_EDGE ( 'NONE', *, *, #37191, .T. ) ;
#63423=ADVANCED_FACE ( 'NONE', ( #35214 ), #24981, .F. ) ;
#63424=DIRECTION ( 'NONE',  ( -0.6414496315691473605, -0.7671651518153083105, -2.309356642089130002E-17 ) ) ;
#63431=CARTESIAN_POINT ( 'NONE',  ( -6.642976262117334940, -10.31452373788278898, 54.00000000000000711 ) ) ;
#63432=CARTESIAN_POINT ( 'NONE',  ( -2.530476262117228092, 9.722976262117159152, 54.00000000000000711 ) ) ;
#63442=CARTESIAN_POINT ( 'NONE',  ( -3.834182069070765309, 7.342976262117170805, 26.00000000000000711 ) ) ;
#63452=ADVANCED_FACE ( 'NONE', ( #35942 ), #57499, .F. ) ;
#63455=VECTOR ( 'NONE', #27280, 1000.000000000000114 ) ;
#63461=CARTESIAN_POINT ( 'NONE',  ( -3.710438382363119736, 7.394232575409525943, 26.00000000000000711 ) ) ;
#63463=DIRECTION ( 'NONE',  ( 0.4999999999999755196, -0.8660254037844528074, 0.000000000000000000 ) ) ;
#63467=ORIENTED_EDGE ( 'NONE', *, *, #43284, .T. ) ;
#63469=CARTESIAN_POINT ( 'NONE',  ( 9.912023737882815766, -6.657023737882824754, 54.00000000000000711 ) ) ;
#63474=ADVANCED_FACE ( 'NONE', ( #64911 ), #11154, .F. ) ;
#63477=EDGE_CURVE ( 'NONE', #28520, #1459, #22124, .T. ) ;
#63478=VECTOR ( 'NONE', #56814, 1000.000000000000000 ) ;
#63480=ORIENTED_EDGE ( 'NONE', *, *, #53453, .F. ) ;
#63484=DIRECTION ( 'NONE',  ( -0.000000000000000000, -0.000000000000000000, -1.000000000000000000 ) ) ;
#63491=DIRECTION ( 'NONE',  ( 1.836970198721029934E-16, 1.836970198721010706E-16, -1.000000000000000000 ) ) ;
#63516=VECTOR ( 'NONE', #37796, 1000.000000000000000 ) ;
#63523=CARTESIAN_POINT ( 'NONE',  ( 10.31452373788281562, -3.857023737882814718, 26.00000000000000711 ) ) ;
#63524=PLANE ( 'NONE',  #58168 ) ;
#63534=DIRECTION ( 'NONE',  ( 1.000000000000000000, 0.000000000000000000, 0.000000000000000000 ) ) ;
#63537=FACE_OUTER_BOUND ( 'NONE', #33452, .T. ) ;
#63544=VERTEX_POINT ( 'NONE', #59255 ) ;
#63552=ORIENTED_EDGE ( 'NONE', *, *, #35873, .T. ) ;
#63568=EDGE_CURVE ( 'NONE', #86, #25606, #67952, .T. ) ;
#63572=DIRECTION ( 'NONE',  ( 9.912705577010336396E-15, 1.000000000000000000, 0.000000000000000000 ) ) ;
#63590=ORIENTED_EDGE ( 'NONE', *, *, #65234, .T. ) ;
#63591=DIRECTION ( 'NONE',  ( -0.7671651518153038696, 0.6414496315691526895, -2.309356642089022458E-17 ) ) ;
#63596=CARTESIAN_POINT ( 'NONE',  ( -5.242976262117259978, 5.242976262117182706, 54.00000000000000711 ) ) ;
#63599=DIRECTION ( 'NONE',  ( -0.7671651518153105309, 0.6414496315691445849, 2.356647714346206145E-16 ) ) ;
#63609=EDGE_LOOP ( 'NONE', ( #61745, #38011, #55521, #20365 ) ) ;
#63610=CYLINDRICAL_SURFACE ( 'NONE', #25294, 0.1749999999999998224 ) ;
#63614=AXIS2_PLACEMENT_3D ( 'NONE', #69888, #9450, #21451 ) ;
#63629=CARTESIAN_POINT ( 'NONE',  ( 9.737023737882777752, 3.667976262117157660, 26.00000000000000711 ) ) ;
#63630=ORIENTED_EDGE ( 'NONE', *, *, #58427, .T. ) ;
#63631=FACE_OUTER_BOUND ( 'NONE', #25475, .T. ) ;
#63635=LINE ( 'NONE', #69280, #33352 ) ;
#63639=ADVANCED_FACE ( 'NONE', ( #2194 ), #24103, .F. ) ;
#63642=ORIENTED_EDGE ( 'NONE', *, *, #65404, .F. ) ;
#63648=LINE ( 'NONE', #52334, #965 ) ;
#63663=VECTOR ( 'NONE', #964, 1000.000000000000000 ) ;
#63665=ADVANCED_FACE ( 'NONE', ( #1849 ), #2887, .T. ) ;
#63669=CARTESIAN_POINT ( 'NONE',  ( 6.364920264886885448, -6.836383711243021466, 54.00000000000000711 ) ) ;
#63670=DIRECTION ( 'NONE',  ( 0.7671651518152985405, 0.6414496315691592399, -2.309356642088639737E-17 ) ) ;
#63677=VECTOR ( 'NONE', #66242, 1000.000000000000000 ) ;
#63682=CARTESIAN_POINT ( 'NONE',  ( 9.795823737882805915, -9.795823737882802362, 26.00000000000000000 ) ) ;
#63687=DIRECTION ( 'NONE',  ( 1.000000000000000000, -2.309061475090597584E-14, 1.836970198720987533E-16 ) ) ;
#63690=LINE ( 'NONE', #31520, #54971 ) ;
#63696=ORIENTED_EDGE ( 'NONE', *, *, #65796, .F. ) ;
#63704=DIRECTION ( 'NONE',  ( 1.000000000000000000, -1.047444401652940007E-14, 1.836970198721010706E-16 ) ) ;
#63705=VERTEX_POINT ( 'NONE', #52759 ) ;
#63712=DIRECTION ( 'NONE',  ( -1.000000000000000000, 0.000000000000000000, 0.000000000000000000 ) ) ;
#63715=AXIS2_PLACEMENT_3D ( 'NONE', #17495, #45057, #24200 ) ;
#63717=CARTESIAN_POINT ( 'NONE',  ( 3.664523737882819709, 10.30047626211720413, 54.00000000000000711 ) ) ;
#63720=CARTESIAN_POINT ( 'NONE',  ( -7.342976262117282715, -5.552858015815545834, 54.00000000000000711 ) ) ;
#63727=FACE_OUTER_BOUND ( 'NONE', #11542, .T. ) ;
#63729=VERTEX_POINT ( 'NONE', #15621 ) ;
#63732=LINE ( 'NONE', #59721, #46909 ) ;
#63733=CARTESIAN_POINT ( 'NONE',  ( -5.779227145995285753, 6.344366288193340253, 54.00000000000000711 ) ) ;
#63740=EDGE_LOOP ( 'NONE', ( #10055, #13028, #19890, #18418, #66407, #69479, #7003, #22799 ) ) ;
#63741=DIRECTION ( 'NONE',  ( -1.000000000000000000, 0.000000000000000000, 0.000000000000000000 ) ) ;
#63753=DIRECTION ( 'NONE',  ( -0.000000000000000000, -0.000000000000000000, -1.000000000000000000 ) ) ;
#63763=LINE ( 'NONE', #30179, #21525 ) ;
#63764=ORIENTED_EDGE ( 'NONE', *, *, #35587, .T. ) ;
#63768=ORIENTED_EDGE ( 'NONE', *, *, #29347, .F. ) ;
#63777=CARTESIAN_POINT ( 'NONE',  ( -9.689726262117227762, 8.566576262117216345, 26.00000000000000711 ) ) ;
#63778=EDGE_CURVE ( 'NONE', #1459, #54522, #47352, .T. ) ;
#63786=EDGE_CURVE ( 'NONE', #37400, #27400, #41421, .T. ) ;
#63800=DIRECTION ( 'NONE',  ( -0.8660254037844322683, 0.5000000000000111022, 0.000000000000000000 ) ) ;
#63805=DIRECTION ( 'NONE',  ( -0.000000000000000000, -0.000000000000000000, -1.000000000000000000 ) ) ;
#63812=DIRECTION ( 'NONE',  ( 1.000000000000000000, 0.000000000000000000, 0.000000000000000000 ) ) ;
#63816=ORIENTED_EDGE ( 'NONE', *, *, #17453, .T. ) ;
#63826=EDGE_CURVE ( 'NONE', #53491, #40788, #26565, .T. ) ;
#63827=AXIS2_PLACEMENT_3D ( 'NONE', #18806, #66886, #45668 ) ;
#63828=CARTESIAN_POINT ( 'NONE',  ( 7.357023737882817827, -3.848229544836346605, 54.00000000000000711 ) ) ;
#63829=EDGE_CURVE ( 'NONE', #10010, #10380, #20556, .T. ) ;
#63830=ORIENTED_EDGE ( 'NONE', *, *, #39145, .T. ) ;
#63844=ORIENTED_EDGE ( 'NONE', *, *, #55078, .F. ) ;
#63849=ORIENTED_EDGE ( 'NONE', *, *, #51494, .T. ) ;
#63857=VERTEX_POINT ( 'NONE', #19850 ) ;
#63862=CIRCLE ( 'NONE', #27768, 0.5249999999999990230 ) ;
#63865=CARTESIAN_POINT ( 'NONE',  ( -5.242976262117259978, 5.242976262117182706, 26.00000000000000711 ) ) ;
#63879=CARTESIAN_POINT ( 'NONE',  ( -6.817976262117261044, 9.722976262117182245, 54.00000000000000711 ) ) ;
#63880=PLANE ( 'NONE',  #49216 ) ;
#63899=VECTOR ( 'NONE', #50001, 1000.000000000000000 ) ;
#63901=VECTOR ( 'NONE', #32631, 1000.000000000000114 ) ;
#63904=EDGE_CURVE ( 'NONE', #53029, #27929, #54489, .T. ) ;
#63914=ORIENTED_EDGE ( 'NONE', *, *, #50547, .T. ) ;
#63918=ORIENTED_EDGE ( 'NONE', *, *, #20801, .F. ) ;
#63919=ADVANCED_FACE ( 'NONE', ( #64401 ), #49516, .F. ) ;
#63932=ORIENTED_EDGE ( 'NONE', *, *, #29851, .F. ) ;
#63943=CARTESIAN_POINT ( 'NONE',  ( 9.404523737882819034, -0.9555237378828154160, 26.00000000000000711 ) ) ;
#63945=EDGE_LOOP ( 'NONE', ( #13946, #34249, #28107, #54367 ) ) ;
#63953=CIRCLE ( 'NONE', #34595, 0.5249999999999990230 ) ;
#63961=VERTEX_POINT ( 'NONE', #16660 ) ;
#63964=AXIS2_PLACEMENT_3D ( 'NONE', #41855, #3681, #16041 ) ;
#63975=DIRECTION ( 'NONE',  ( 1.000000000000000000, -3.491481338843133355E-15, 0.000000000000000000 ) ) ;
#63982=CARTESIAN_POINT ( 'NONE',  ( 4.155633711806655306, 4.706725378239160484, 54.00000000000000711 ) ) ;
#63989=DIRECTION ( 'NONE',  ( -0.000000000000000000, -0.000000000000000000, -1.000000000000000000 ) ) ;
#63991=CARTESIAN_POINT ( 'NONE',  ( -4.141586236041100655, 5.779227145995200488, 54.00000000000000711 ) ) ;
#63994=DIRECTION ( 'NONE',  ( -4.121462285523434951E-16, -1.000000000000000000, -0.000000000000000000 ) ) ;
#63995=CARTESIAN_POINT ( 'NONE',  ( 2.005523737882813240, 8.598420958951633608, 54.00000000000000711 ) ) ;
#63999=ORIENTED_EDGE ( 'NONE', *, *, #22703, .F. ) ;
#64001=CARTESIAN_POINT ( 'NONE',  ( -9.547976262117254365, 2.355476262117183417, 26.00000000000000711 ) ) ;
#64004=EDGE_LOOP ( 'NONE', ( #51124, #16901, #36417, #66238 ) ) ;
#64006=VECTOR ( 'NONE', #25567, 1000.000000000000000 ) ;
#64012=ORIENTED_EDGE ( 'NONE', *, *, #50062, .T. ) ;
#64017=EDGE_CURVE ( 'NONE', #59398, #12520, #52978, .T. ) ;
#64020=CARTESIAN_POINT ( 'NONE',  ( -9.547976262117254365, 2.355476262117183417, 54.00000000000000711 ) ) ;
#64022=DIRECTION ( 'NONE',  ( -0.7071067811865527908, -0.7071067811865422437, 0.000000000000000000 ) ) ;
#64026=AXIS2_PLACEMENT_3D ( 'NONE', #20201, #62629, #26562 ) ;
#64030=ORIENTED_EDGE ( 'NONE', *, *, #37438, .T. ) ;
#64058=LINE ( 'NONE', #4991, #17138 ) ;
#64062=LINE ( 'NONE', #48134, #32412 ) ;
#64063=PLANE ( 'NONE',  #46333 ) ;
#64064=AXIS2_PLACEMENT_3D ( 'NONE', #649, #59696, #37441 ) ;
#64068=DIRECTION ( 'NONE',  ( 0.000000000000000000, -3.673940397442059868E-16, 1.000000000000000000 ) ) ;
#64076=CARTESIAN_POINT ( 'NONE',  ( -5.242976262117280406, -5.257023737882805747, 54.00000000000000711 ) ) ;
#64079=VECTOR ( 'NONE', #60970, 1000.000000000000114 ) ;
#64089=ORIENTED_EDGE ( 'NONE', *, *, #39823, .T. ) ;
#64092=VERTEX_POINT ( 'NONE', #19069 ) ;
#64103=DIRECTION ( 'NONE',  ( 0.000000000000000000, 1.000000000000000000, 0.000000000000000000 ) ) ;
#64104=CARTESIAN_POINT ( 'NONE',  ( -6.835476262117260227, 10.49297626211718359, 54.00000000000000711 ) ) ;
#64112=ORIENTED_EDGE ( 'NONE', *, *, #18629, .F. ) ;
#64116=VECTOR ( 'NONE', #48645, 1000.000000000000114 ) ;
#64118=CARTESIAN_POINT ( 'NONE',  ( -8.697938382363103571, -2.420780051175099423, 54.00000000000000711 ) ) ;
#64123=EDGE_CURVE ( 'NONE', #28168, #68940, #64198, .T. ) ;
#64127=CARTESIAN_POINT ( 'NONE',  ( -10.03972626211722918, 9.689726262117183353, 54.00000000000000711 ) ) ;
#64130=EDGE_LOOP ( 'NONE', ( #46060, #59817, #59842, #59584 ) ) ;
#64144=ORIENTED_EDGE ( 'NONE', *, *, #68616, .F. ) ;
#64146=DIRECTION ( 'NONE',  ( 0.000000000000000000, 1.000000000000000000, 0.000000000000000000 ) ) ;
#64147=EDGE_CURVE ( 'NONE', #9849, #1721, #62421, .T. ) ;
#64169=CARTESIAN_POINT ( 'NONE',  ( 6.657023737882821202, 10.30047626211719347, 54.00000000000000711 ) ) ;
#64171=PLANE ( 'NONE',  #69715 ) ;
#64173=DIRECTION ( 'NONE',  ( -0.000000000000000000, 3.673940397442059868E-16, -1.000000000000000000 ) ) ;
#64175=CARTESIAN_POINT ( 'NONE',  ( -7.955476262117259445, 8.821682069070703847, 54.00000000000000711 ) ) ;
#64182=EDGE_LOOP ( 'NONE', ( #2939, #68519, #41698, #18585 ) ) ;
#64187=ORIENTED_EDGE ( 'NONE', *, *, #54716, .F. ) ;
#64195=ORIENTED_EDGE ( 'NONE', *, *, #58669, .T. ) ;
#64196=FACE_OUTER_BOUND ( 'NONE', #23549, .T. ) ;
#64198=LINE ( 'NONE', #15745, #33657 ) ;
#64201=CARTESIAN_POINT ( 'NONE',  ( 9.562023737882801910, 8.130476262117189989, 26.00000000000000711 ) ) ;
#64215=VECTOR ( 'NONE', #5168, 1000.000000000000000 ) ;
#64221=DIRECTION ( 'NONE',  ( -1.000000000000000000, 0.000000000000000000, 0.000000000000000000 ) ) ;
#64232=DIRECTION ( 'NONE',  ( -1.000000000000000000, 1.047444401652940007E-14, 0.000000000000000000 ) ) ;
#64235=CARTESIAN_POINT ( 'NONE',  ( 9.737023737882816832, -6.832023737882813919, 26.00000000000000000 ) ) ;
#64236=FACE_OUTER_BOUND ( 'NONE', #44845, .T. ) ;
#64237=DIRECTION ( 'NONE',  ( 0.000000000000000000, 3.673940397442059868E-16, -1.000000000000000000 ) ) ;
#64241=DIRECTION ( 'NONE',  ( 1.836970198721029934E-16, -1.836970198721036344E-16, 1.000000000000000000 ) ) ;
#64246=FACE_OUTER_BOUND ( 'NONE', #13112, .T. ) ;
#64247=CARTESIAN_POINT ( 'NONE',  ( -8.916576262117258622, 10.03972626211718477, 54.00000000000000711 ) ) ;
#64248=DIRECTION ( 'NONE',  ( 0.6414496315691446959, -0.7671651518153106419, 0.000000000000000000 ) ) ;
#64251=ORIENTED_EDGE ( 'NONE', *, *, #32988, .T. ) ;
#64256=LINE ( 'NONE', #51894, #15338 ) ;
#64272=DIRECTION ( 'NONE',  ( -1.836970198721029934E-16, -1.836970198721010706E-16, 1.000000000000000000 ) ) ;
#64274=ORIENTED_EDGE ( 'NONE', *, *, #49603, .F. ) ;
#64281=VERTEX_POINT ( 'NONE', #58318 ) ;
#64285=CARTESIAN_POINT ( 'NONE',  ( -9.781776262117249487, 10.49297626211718359, 54.00000000000000711 ) ) ;
#64287=LINE ( 'NONE', #15148, #62732 ) ;
#64302=ADVANCED_FACE ( 'NONE', ( #68570 ), #63261, .F. ) ;
#64313=EDGE_CURVE ( 'NONE', #14190, #56758, #4571, .T. ) ;
#64316=LINE ( 'NONE', #20474, #37305 ) ;
#64317=CARTESIAN_POINT ( 'NONE',  ( -4.031976262117257903, -3.157023737882818981, 54.00000000000000711 ) ) ;
#64320=CARTESIAN_POINT ( 'NONE',  ( -8.227189898828699555, -1.634292677759815904, 54.00000000000000711 ) ) ;
#64326=ORIENTED_EDGE ( 'NONE', *, *, #34231, .F. ) ;
#64333=CARTESIAN_POINT ( 'NONE',  ( -8.598420958951642490, -2.005523737882745738, 54.00000000000000711 ) ) ;
#64352=LINE ( 'NONE', #38521, #39442 ) ;
#64354=DIRECTION ( 'NONE',  ( -0.7071067811865422437, 0.7071067811865527908, 2.597868168706499332E-16 ) ) ;
#64355=VERTEX_POINT ( 'NONE', #53360 ) ;
#64356=EDGE_CURVE ( 'NONE', #64674, #46952, #21515, .T. ) ;
#64359=FACE_OUTER_BOUND ( 'NONE', #28136, .T. ) ;
#64360=CARTESIAN_POINT ( 'NONE',  ( -8.916576262117352769, -9.703773737882729122, 26.00000000000000000 ) ) ;
#64365=ORIENTED_EDGE ( 'NONE', *, *, #21781, .F. ) ;
#64367=EDGE_CURVE ( 'NONE', #47595, #54695, #10457, .T. ) ;
#64372=EDGE_CURVE ( 'NONE', #48826, #43831, #300, .T. ) ;
#64374=VECTOR ( 'NONE', #13932, 1000.000000000000000 ) ;
#64380=EDGE_CURVE ( 'NONE', #22852, #6870, #35309, .T. ) ;
#64385=CARTESIAN_POINT ( 'NONE',  ( -9.722976262117258628, 3.667976262117184749, 54.00000000000000711 ) ) ;
#64401=FACE_OUTER_BOUND ( 'NONE', #17121, .T. ) ;
#64406=CARTESIAN_POINT ( 'NONE',  ( -3.663616288757055806, 6.350872789121238426, 26.00000000000000711 ) ) ;
#64415=ORIENTED_EDGE ( 'NONE', *, *, #67903, .T. ) ;
#64427=AXIS2_PLACEMENT_3D ( 'NONE', #12697, #7053, #32907 ) ;
#64429=DIRECTION ( 'NONE',  ( 7.665540703601096574E-15, 1.000000000000000000, -0.000000000000000000 ) ) ;
#64431=VERTEX_POINT ( 'NONE', #5609 ) ;
#64434=ORIENTED_EDGE ( 'NONE', *, *, #32434, .T. ) ;
#64435=ORIENTED_EDGE ( 'NONE', *, *, #69912, .T. ) ;
#64444=LINE ( 'NONE', #15305, #40202 ) ;
#64447=DIRECTION ( 'NONE',  ( -0.000000000000000000, -0.000000000000000000, -1.000000000000000000 ) ) ;
#64454=DIRECTION ( 'NONE',  ( 1.062075597536821205E-14, 1.000000000000000000, 0.000000000000000000 ) ) ;
#64458=VECTOR ( 'NONE', #22295, 1000.000000000000000 ) ;
#64461=ORIENTED_EDGE ( 'NONE', *, *, #62526, .F. ) ;
#64464=ORIENTED_EDGE ( 'NONE', *, *, #21973, .T. ) ;
#64466=DIRECTION ( 'NONE',  ( -0.000000000000000000, -0.000000000000000000, -1.000000000000000000 ) ) ;
#64468=VECTOR ( 'NONE', #38083, 1000.000000000000000 ) ;
#64472=CARTESIAN_POINT ( 'NONE',  ( -1.466476262117318630, -9.404523737882838574, 26.00000000000000711 ) ) ;
#64473=VERTEX_POINT ( 'NONE', #51153 ) ;
#64482=CARTESIAN_POINT ( 'NONE',  ( 9.404523737882817258, -1.480523737882815993, 26.00000000000000711 ) ) ;
#64486=EDGE_LOOP ( 'NONE', ( #53412, #18827, #36346, #16037 ) ) ;
#64496=CARTESIAN_POINT ( 'NONE',  ( -8.916576262117345664, -8.580623737882765667, 54.00000000000000711 ) ) ;
#64505=CARTESIAN_POINT ( 'NONE',  ( -6.350872789121313922, -3.677663764522584255, 26.00000000000000711 ) ) ;
#64510=VERTEX_POINT ( 'NONE', #23581 ) ;
#64511=CARTESIAN_POINT ( 'NONE',  ( 8.093267424590459669, 8.697938382363064491, 54.00000000000000711 ) ) ;
#64518=ORIENTED_EDGE ( 'NONE', *, *, #57640, .T. ) ;
#64522=CARTESIAN_POINT ( 'NONE',  ( -9.897976262117259338, 3.842976262117183683, 54.00000000000000711 ) ) ;
#64524=CARTESIAN_POINT ( 'NONE',  ( 9.404523737882758638, 1.466476262117154983, 54.00000000000000711 ) ) ;
#64532=ORIENTED_EDGE ( 'NONE', *, *, #13414, .T. ) ;
#64535=EDGE_CURVE ( 'NONE', #15613, #59398, #13326, .T. ) ;
#64537=DIRECTION ( 'NONE',  ( 1.034072152899300274E-14, 1.000000000000000000, 0.000000000000000000 ) ) ;
#64542=ORIENTED_EDGE ( 'NONE', *, *, #52129, .T. ) ;
#64543=ORIENTED_EDGE ( 'NONE', *, *, #33580, .F. ) ;
#64545=ORIENTED_EDGE ( 'NONE', *, *, #17161, .T. ) ;
#64546=ORIENTED_EDGE ( 'NONE', *, *, #18820, .T. ) ;
#64550=CIRCLE ( 'NONE', #4685, 0.5249999999999994671 ) ;
#64563=CARTESIAN_POINT ( 'NONE',  ( 10.31452373788278187, 3.842976262117144159, 54.00000000000000711 ) ) ;
#64564=DIRECTION ( 'NONE',  ( 1.000000000000000000, 0.000000000000000000, 0.000000000000000000 ) ) ;
#64567=EDGE_CURVE ( 'NONE', #44397, #56086, #18408, .T. ) ;
#64573=LINE ( 'NONE', #26743, #20703 ) ;
#64576=DIRECTION ( 'NONE',  ( -1.000000000000000000, 0.000000000000000000, 0.000000000000000000 ) ) ;
#64577=DIRECTION ( 'NONE',  ( -1.000000000000000000, 3.491481338843133355E-15, 0.000000000000000000 ) ) ;
#64598=EDGE_LOOP ( 'NONE', ( #7889, #6781, #48583, #3116 ) ) ;
#64611=ADVANCED_FACE ( 'NONE', ( #18623 ), #66382, .F. ) ;
#64624=ORIENTED_EDGE ( 'NONE', *, *, #24946, .F. ) ;
#64625=DIRECTION ( 'NONE',  ( 1.000000000000000000, 0.000000000000000000, 0.000000000000000000 ) ) ;
#64629=DIRECTION ( 'NONE',  ( 0.000000000000000000, 3.673940397442059868E-16, -1.000000000000000000 ) ) ;
#64633=VECTOR ( 'NONE', #60022, 1000.000000000000000 ) ;
#64634=ORIENTED_EDGE ( 'NONE', *, *, #47067, .F. ) ;
#64635=CARTESIAN_POINT ( 'NONE',  ( 2.420780051175163816, 8.697938382363089360, 26.00000000000000711 ) ) ;
#64636=CYLINDRICAL_SURFACE ( 'NONE', #4192, 0.3499999999999996447 ) ;
#64637=CARTESIAN_POINT ( 'NONE',  ( -9.722976262117256852, 7.955476262117183062, 26.00000000000000711 ) ) ;
#64640=AXIS2_PLACEMENT_3D ( 'NONE', #440, #11381, #59134 ) ;
#64649=FACE_OUTER_BOUND ( 'NONE', #104, .T. ) ;
#64650=PLANE ( 'NONE',  #15790 ) ;
#64663=DIRECTION ( 'NONE',  ( 1.000000000000000000, 0.000000000000000000, 0.000000000000000000 ) ) ;
#64672=CIRCLE ( 'NONE', #24026, 1.929199999999998028 ) ;
#64674=VERTEX_POINT ( 'NONE', #58216 ) ;
#64676=VERTEX_POINT ( 'NONE', #8729 ) ;
#64677=ORIENTED_EDGE ( 'NONE', *, *, #51335, .T. ) ;
#64683=EDGE_LOOP ( 'NONE', ( #60345, #26877, #58386, #4810 ) ) ;
#64688=EDGE_CURVE ( 'NONE', #10538, #11799, #46896, .T. ) ;
#64692=ADVANCED_FACE ( 'NONE', ( #52573 ), #8360, .F. ) ;
#64693=EDGE_CURVE ( 'NONE', #15959, #27077, #30299, .T. ) ;
#64697=LINE ( 'NONE', #32871, #64889 ) ;
#64702=EDGE_CURVE ( 'NONE', #31249, #39691, #41036, .T. ) ;
#64709=LINE ( 'NONE', #66352, #42872 ) ;
#64710=AXIS2_PLACEMENT_3D ( 'NONE', #58788, #37918, #59479 ) ;
#64722=FACE_OUTER_BOUND ( 'NONE', #51346, .T. ) ;
#64723=ORIENTED_EDGE ( 'NONE', *, *, #29409, .F. ) ;
#64724=CIRCLE ( 'NONE', #62426, 0.3499999999999996447 ) ;
#64727=DIRECTION ( 'NONE',  ( 0.000000000000000000, 1.000000000000000000, 0.000000000000000000 ) ) ;
#64733=DIRECTION ( 'NONE',  ( 0.6414496315691494699, -0.7671651518153064231, 0.000000000000000000 ) ) ;
#64736=CARTESIAN_POINT ( 'NONE',  ( 6.657023737882818537, -9.912023737882819319, 54.00000000000000711 ) ) ;
#64737=EDGE_CURVE ( 'NONE', #18477, #57396, #19328, .T. ) ;
#64744=ORIENTED_EDGE ( 'NONE', *, *, #42128, .T. ) ;
#64748=VECTOR ( 'NONE', #2421, 1000.000000000000000 ) ;
#64752=DIRECTION ( 'NONE',  ( -0.000000000000000000, -1.000000000000000000, -0.000000000000000000 ) ) ;
#64755=DIRECTION ( 'NONE',  ( 1.836970198721029934E-16, -1.836970198721036344E-16, 1.000000000000000000 ) ) ;
#64756=FILL_AREA_STYLE_COLOUR ( '', #35913 ) ;
#64760=CARTESIAN_POINT ( 'NONE',  ( -3.142976262117262998, -4.046023737882823212, 26.00000000000000711 ) ) ;
#64771=ADVANCED_FACE ( 'NONE', ( #31708 ), #21086, .F. ) ;
#64772=ADVANCED_FACE ( 'NONE', ( #42649 ), #26391, .T. ) ;
#64774=AXIS2_PLACEMENT_3D ( 'NONE', #7659, #38798, #60017 ) ;
#64781=EDGE_CURVE ( 'NONE', #829, #15324, #69867, .T. ) ;
#64787=ADVANCED_FACE ( 'NONE', ( #10130 ), #54312, .F. ) ;
#64788=CARTESIAN_POINT ( 'NONE',  ( 9.912023737882783792, 3.842976262117149044, 54.00000000000000711 ) ) ;
#64798=ADVANCED_FACE ( 'NONE', ( #16481 ), #69524, .F. ) ;
#64805=ORIENTED_EDGE ( 'NONE', *, *, #54001, .T. ) ;
#64811=ORIENTED_EDGE ( 'NONE', *, *, #60394, .T. ) ;
#64816=EDGE_LOOP ( 'NONE', ( #45886, #31262, #21529, #8318, #13884, #42216, #4061, #2159, #19202, #29704, #33200, #56338, #11556, #50533, #4889, #44811, #48954 ) ) ;
#64817=AXIS2_PLACEMENT_3D ( 'NONE', #27878, #2039, #24656 ) ;
#64818=VECTOR ( 'NONE', #50678, 1000.000000000000000 ) ;
#64822=VERTEX_POINT ( 'NONE', #43335 ) ;
#64823=CARTESIAN_POINT ( 'NONE',  ( 8.711985858128644011, 2.406732575409517239, 54.00000000000000711 ) ) ;
#64827=CARTESIAN_POINT ( 'NONE',  ( -5.242976262117275077, -5.257023737882800418, 26.00000000000000711 ) ) ;
#64829=EDGE_CURVE ( 'NONE', #49752, #42154, #64573, .T. ) ;
#64830=CARTESIAN_POINT ( 'NONE',  ( 8.580623737882818958, -8.930623737882845248, 26.00000000000000000 ) ) ;
#64831=VECTOR ( 'NONE', #38265, 1000.000000000000114 ) ;
#64834=CARTESIAN_POINT ( 'NONE',  ( -9.722976262117294155, -6.832023737882757963, 54.00000000000000711 ) ) ;
#64839=CARTESIAN_POINT ( 'NONE',  ( -3.142976262117261221, 4.031976262117183296, 26.00000000000000711 ) ) ;
#64842=LINE ( 'NONE', #43610, #41949 ) ;
#64843=LINE ( 'NONE', #64496, #34766 ) ;
#64844=EDGE_CURVE ( 'NONE', #28520, #64473, #32401, .T. ) ;
#64868=CARTESIAN_POINT ( 'NONE',  ( 3.157023737882804770, 6.486996718459879574, 54.00000000000000711 ) ) ;
#64874=LINE ( 'NONE', #12151, #65752 ) ;
#64875=AXIS2_PLACEMENT_3D ( 'NONE', #46807, #51778, #56722 ) ;
#64879=VERTEX_POINT ( 'NONE', #66303 ) ;
#64889=VECTOR ( 'NONE', #16255, 1000.000000000000000 ) ;
#64891=VERTEX_POINT ( 'NONE', #61323 ) ;
#64893=ORIENTED_EDGE ( 'NONE', *, *, #67296, .F. ) ;
#64894=ORIENTED_EDGE ( 'NONE', *, *, #59243, .T. ) ;
#64911=FACE_OUTER_BOUND ( 'NONE', #64130, .T. ) ;
#64919=EDGE_CURVE ( 'NONE', #20150, #22770, #10612, .T. ) ;
#64921=DIRECTION ( 'NONE',  ( -1.214636490590110272E-14, -1.000000000000000000, 0.000000000000000000 ) ) ;
#64928=EDGE_CURVE ( 'NONE', #36809, #3920, #33768, .T. ) ;
#64932=CIRCLE ( 'NONE', #63827, 1.929199999999998916 ) ;
#64935=EDGE_LOOP ( 'NONE', ( #39637, #4267, #5659, #38096 ) ) ;
#64938=CARTESIAN_POINT ( 'NONE',  ( -6.651770455163739548, 7.517976262117183062, 54.00000000000000711 ) ) ;
#64941=CARTESIAN_POINT ( 'NONE',  ( -5.242976262117259978, 5.242976262117182706, 54.00000000000000711 ) ) ;
#64951=ORIENTED_EDGE ( 'NONE', *, *, #23564, .T. ) ;
#64953=VERTEX_POINT ( 'NONE', #33434 ) ;
#64957=LINE ( 'NONE', #5563, #59105 ) ;
#64964=ORIENTED_EDGE ( 'NONE', *, *, #31245, .T. ) ;
#64975=ORIENTED_EDGE ( 'NONE', *, *, #31250, .F. ) ;
#64995=CARTESIAN_POINT ( 'NONE',  ( -2.530476262117318242, -8.835729544836354421, 54.00000000000000711 ) ) ;
#65004=DIRECTION ( 'NONE',  ( 7.665540703601096574E-15, 1.000000000000000000, -0.000000000000000000 ) ) ;
#65012=VECTOR ( 'NONE', #30188, 1000.000000000000000 ) ;
#65020=AXIS2_PLACEMENT_3D ( 'NONE', #54875, #55213, #436 ) ;
#65022=ORIENTED_EDGE ( 'NONE', *, *, #48558, .F. ) ;
#65026=DIRECTION ( 'NONE',  ( 1.836970198721029934E-16, 1.836970198721010706E-16, -1.000000000000000000 ) ) ;
#65031=VECTOR ( 'NONE', #27881, 1000.000000000000114 ) ;
#65036=FACE_OUTER_BOUND ( 'NONE', #41766, .T. ) ;
#65047=FACE_OUTER_BOUND ( 'NONE', #25841, .T. ) ;
#65049=LINE ( 'NONE', #58703, #51275 ) ;
#65052=ADVANCED_FACE ( 'NONE', ( #5059 ), #21324, .F. ) ;
#65056=DIRECTION ( 'NONE',  ( -1.836970198721029934E-16, 1.836970198721036590E-16, -1.000000000000000000 ) ) ;
#65057=LINE ( 'NONE', #65737, #27663 ) ;
#65060=DIRECTION ( 'NONE',  ( 0.000000000000000000, 0.000000000000000000, 1.000000000000000000 ) ) ;
#65062=AXIS2_PLACEMENT_3D ( 'NONE', #27115, #54341, #27459 ) ;
#65064=EDGE_CURVE ( 'NONE', #7367, #51302, #27665, .T. ) ;
#65066=CARTESIAN_POINT ( 'NONE',  ( 1.480523737882813773, 8.598420958951637161, 54.00000000000000711 ) ) ;
#65067=VECTOR ( 'NONE', #27783, 1000.000000000000000 ) ;
#65069=PLANE ( 'NONE',  #57378 ) ;
#65072=AXIS2_PLACEMENT_3D ( 'NONE', #31692, #47252, #20022 ) ;
#65073=AXIS2_PLACEMENT_3D ( 'NONE', #55721, #45802, #7624 ) ;
#65077=ORIENTED_EDGE ( 'NONE', *, *, #67633, .T. ) ;
#65093=DIRECTION ( 'NONE',  ( 0.000000000000000000, 0.000000000000000000, 1.000000000000000000 ) ) ;
#65098=ORIENTED_EDGE ( 'NONE', *, *, #27409, .F. ) ;
#65109=CARTESIAN_POINT ( 'NONE',  ( -2.406732575409671337, -8.711985858128709737, 54.00000000000000711 ) ) ;
#65122=CIRCLE ( 'NONE', #59510, 0.5249999999999994671 ) ;
#65123=ORIENTED_EDGE ( 'NONE', *, *, #15233, .T. ) ;
#65138=VERTEX_POINT ( 'NONE', #60176 ) ;
#65150=EDGE_LOOP ( 'NONE', ( #1303, #57471, #40512, #59110 ) ) ;
#65163=DIRECTION ( 'NONE',  ( -1.836970198721029934E-16, -1.836970198721010706E-16, 1.000000000000000000 ) ) ;
#65165=EDGE_LOOP ( 'NONE', ( #4976, #7473, #59052, #52175 ) ) ;
#65168=CARTESIAN_POINT ( 'NONE',  ( 8.612468434717241550, -1.480523737882825985, 54.00000000000000711 ) ) ;
#65172=AXIS2_PLACEMENT_3D ( 'NONE', #27096, #37711, #31719 ) ;
#65179=ORIENTED_EDGE ( 'NONE', *, *, #36331, .F. ) ;
#65180=CARTESIAN_POINT ( 'NONE',  ( -9.897976262117257562, 6.817976262117182884, 54.00000000000000711 ) ) ;
#65186=DIRECTION ( 'NONE',  ( -1.000000000000000000, -2.135044278125301343E-15, -7.844025423732065664E-31 ) ) ;
#65191=ORIENTED_EDGE ( 'NONE', *, *, #64372, .F. ) ;
#65209=CARTESIAN_POINT ( 'NONE',  ( -6.817976262117325881, -9.737023737882786634, 54.00000000000000711 ) ) ;
#65214=CIRCLE ( 'NONE', #62925, 0.1749999999999998224 ) ;
#65215=AXIS2_PLACEMENT_3D ( 'NONE', #57860, #35225, #56807 ) ;
#65216=VECTOR ( 'NONE', #57151, 1000.000000000000000 ) ;
#65219=ORIENTED_EDGE ( 'NONE', *, *, #65957, .T. ) ;
#65228=AXIS2_PLACEMENT_3D ( 'NONE', #62022, #68040, #35494 ) ;
#65231=CARTESIAN_POINT ( 'NONE',  ( -8.697938382363135545, 2.406732575409538111, 26.00000000000000711 ) ) ;
#65232=VERTEX_POINT ( 'NONE', #38958 ) ;
#65233=ORIENTED_EDGE ( 'NONE', *, *, #47376, .T. ) ;
#65234=EDGE_CURVE ( 'NONE', #69196, #45686, #7115, .T. ) ;
#65251=VERTEX_POINT ( 'NONE', #49915 ) ;
#65253=EDGE_CURVE ( 'NONE', #55364, #6741, #45290, .T. ) ;
#65257=DIRECTION ( 'NONE',  ( -0.000000000000000000, 0.000000000000000000, -1.000000000000000000 ) ) ;
#65274=ORIENTED_EDGE ( 'NONE', *, *, #62252, .F. ) ;
#65280=LINE ( 'NONE', #49007, #16658 ) ;
#65287=VERTEX_POINT ( 'NONE', #62606 ) ;
#65294=DIRECTION ( 'NONE',  ( 1.836970198721029934E-16, 1.836970198721010706E-16, -1.000000000000000000 ) ) ;
#65300=EDGE_CURVE ( 'NONE', #45407, #12591, #44447, .T. ) ;
#65304=STYLED_ITEM ( 'NONE', ( #6061 ), #21410 ) ;
#65313=CYLINDRICAL_SURFACE ( 'NONE', #61345, 0.1749999999999998224 ) ;
#65320=EDGE_CURVE ( 'NONE', #4176, #45981, #7205, .T. ) ;
#65325=EDGE_CURVE ( 'NONE', #24174, #523, #63321, .T. ) ;
#65328=ORIENTED_EDGE ( 'NONE', *, *, #32268, .F. ) ;
#65330=PLANE ( 'NONE',  #12986 ) ;
#65334=DIRECTION ( 'NONE',  ( -1.000000000000000000, 0.000000000000000000, 0.000000000000000000 ) ) ;
#65340=DIRECTION ( 'NONE',  ( -0.000000000000000000, 3.673940397442059868E-16, -1.000000000000000000 ) ) ;
#65347=CARTESIAN_POINT ( 'NONE',  ( 6.849523737882818430, 10.30047626211719169, 54.00000000000000711 ) ) ;
#65349=CARTESIAN_POINT ( 'NONE',  ( 10.31452373788281562, -3.857023737882824932, 54.00000000000000711 ) ) ;
#65357=DIRECTION ( 'NONE',  ( 1.836970198721029934E-16, 1.836970198721010706E-16, -1.000000000000000000 ) ) ;
#65360=EDGE_CURVE ( 'NONE', #7067, #65973, #35379, .T. ) ;
#65362=LINE ( 'NONE', #43087, #61973 ) ;
#65371=LINE ( 'NONE', #16924, #61616 ) ;
#65373=AXIS2_PLACEMENT_3D ( 'NONE', #20923, #5387, #21633 ) ;
#65377=AXIS2_PLACEMENT_3D ( 'NONE', #11250, #39170, #32826 ) ;
#65383=ORIENTED_EDGE ( 'NONE', *, *, #19041, .F. ) ;
#65399=DIRECTION ( 'NONE',  ( -0.7071067811865474617, 0.7071067811865474617, 0.000000000000000000 ) ) ;
#65401=ORIENTED_EDGE ( 'NONE', *, *, #8550, .F. ) ;
#65404=EDGE_CURVE ( 'NONE', #68798, #6502, #16113, .T. ) ;
#65405=EDGE_LOOP ( 'NONE', ( #18892, #1360, #38199, #60189 ) ) ;
#65418=ORIENTED_EDGE ( 'NONE', *, *, #1313, .T. ) ;
#65428=CARTESIAN_POINT ( 'NONE',  ( 5.552858015815566262, 7.342976262117203667, 26.00000000000000711 ) ) ;
#65429=ORIENTED_EDGE ( 'NONE', *, *, #16546, .F. ) ;
#65433=CARTESIAN_POINT ( 'NONE',  ( -2.530476262117322239, -9.737023737882823937, 26.00000000000000711 ) ) ;
#65437=ORIENTED_EDGE ( 'NONE', *, *, #6491, .F. ) ;
#65449=DIRECTION ( 'NONE',  ( -1.836970198721029934E-16, 1.836970198721036590E-16, -1.000000000000000000 ) ) ;
#65471=CARTESIAN_POINT ( 'NONE',  ( 3.724485858128677940, -7.408280051175156977, 26.00000000000000000 ) ) ;
#65484=ORIENTED_EDGE ( 'NONE', *, *, #26234, .F. ) ;
#65485=ORIENTED_EDGE ( 'NONE', *, *, #43454, .T. ) ;
#65489=CARTESIAN_POINT ( 'NONE',  ( -9.722976262117249746, -3.682023737882726522, 54.00000000000000711 ) ) ;
#65494=DIRECTION ( 'NONE',  ( 0.000000000000000000, -1.000000000000000000, 0.000000000000000000 ) ) ;
#65496=ADVANCED_FACE ( 'NONE', ( #17783 ), #56995, .F. ) ;
#65505=VECTOR ( 'NONE', #32341, 1000.000000000000000 ) ;
#65515=CARTESIAN_POINT ( 'NONE',  ( 9.737023737882804397, 6.817976262117185549, 54.00000000000000711 ) ) ;
#65518=DIRECTION ( 'NONE',  ( 0.5000000000000019984, 0.8660254037844375974, 3.181725716174716554E-16 ) ) ;
#65521=CARTESIAN_POINT ( 'NONE',  ( 2.420780051175147829, -8.711985858128667104, 26.00000000000000000 ) ) ;
#65525=CARTESIAN_POINT ( 'NONE',  ( -6.486996718459931088, 2.617976262117183150, 54.00000000000000711 ) ) ;
#65532=ADVANCED_FACE ( 'NONE', ( #61241 ), #29426, .F. ) ;
#65536=VECTOR ( 'NONE', #32969, 1000.000000000000000 ) ;
#65537=FACE_OUTER_BOUND ( 'NONE', #60436, .T. ) ;
#65543=VERTEX_POINT ( 'NONE', #46048 ) ;
#65546=DIRECTION ( 'NONE',  ( -1.836970198721029934E-16, 1.836970198721036590E-16, -1.000000000000000000 ) ) ;
#65550=CIRCLE ( 'NONE', #42981, 1.929199999999998028 ) ;
#65557=ORIENTED_EDGE ( 'NONE', *, *, #36821, .F. ) ;
#65560=DIRECTION ( 'NONE',  ( -0.7071067811865474617, -0.7071067811865474617, -0.000000000000000000 ) ) ;
#65565=VERTEX_POINT ( 'NONE', #58767 ) ;
#65567=CARTESIAN_POINT ( 'NONE',  ( -6.651770455163739548, 7.517976262117183062, 54.00000000000000711 ) ) ;
#65569=EDGE_CURVE ( 'NONE', #57625, #15217, #46391, .T. ) ;
#65570=EDGE_CURVE ( 'NONE', #330, #11541, #10321, .T. ) ;
#65573=ADVANCED_FACE ( 'NONE', ( #4672 ), #31896, .F. ) ;
#65595=VERTEX_POINT ( 'NONE', #3971 ) ;
#65597=DIRECTION ( 'NONE',  ( -1.836970198721029934E-16, 1.836970198721036590E-16, -1.000000000000000000 ) ) ;
#65603=CARTESIAN_POINT ( 'NONE',  ( 8.711985858128693749, -8.093267424590470327, 54.00000000000000711 ) ) ;
#65612=DIRECTION ( 'NONE',  ( 1.000000000000000000, -8.540177112501197482E-15, 0.000000000000000000 ) ) ;
#65620=ORIENTED_EDGE ( 'NONE', *, *, #4812, .F. ) ;
#65622=PLANE ( 'NONE',  #9066 ) ;
#65625=EDGE_CURVE ( 'NONE', #43292, #19689, #4337, .T. ) ;
#65635=CARTESIAN_POINT ( 'NONE',  ( 9.795823737882804139, 9.781776262117173104, 54.00000000000000711 ) ) ;
#65637=ORIENTED_EDGE ( 'NONE', *, *, #46625, .T. ) ;
#65639=ADVANCED_FACE ( 'NONE', ( #34199 ), #5970, .F. ) ;
#65646=CARTESIAN_POINT ( 'NONE',  ( 9.703773737882785966, -10.05377373788282469, 54.00000000000000711 ) ) ;
#65653=ORIENTED_EDGE ( 'NONE', *, *, #43609, .F. ) ;
#65654=CARTESIAN_POINT ( 'NONE',  ( 10.31452373788281562, -3.664523737882816157, 26.00000000000000711 ) ) ;
#65675=FACE_OUTER_BOUND ( 'NONE', #16629, .T. ) ;
#65676=ORIENTED_EDGE ( 'NONE', *, *, #30358, .F. ) ;
#65679=CIRCLE ( 'NONE', #12605, 1.224999999999998757 ) ;
#65691=VECTOR ( 'NONE', #40282, 999.9999999999998863 ) ;
#65692=FACE_OUTER_BOUND ( 'NONE', #53635, .T. ) ;
#65694=CARTESIAN_POINT ( 'NONE',  ( 8.930623737882818602, -10.05377373788282469, 54.00000000000000711 ) ) ;
#65695=CIRCLE ( 'NONE', #20526, 0.1749999999999998224 ) ;
#65696=DIRECTION ( 'NONE',  ( -0.000000000000000000, -0.000000000000000000, -1.000000000000000000 ) ) ;
#65715=CARTESIAN_POINT ( 'NONE',  ( -9.722976262117258628, 7.290476262117218553, 54.00000000000000711 ) ) ;
#65718=ORIENTED_EDGE ( 'NONE', *, *, #3313, .F. ) ;
#65719=FACE_OUTER_BOUND ( 'NONE', #43272, .T. ) ;
#65727=CARTESIAN_POINT ( 'NONE',  ( 9.737023737882799068, 6.817976262117189989, 26.00000000000000711 ) ) ;
#65728=EDGE_LOOP ( 'NONE', ( #53546, #69201, #22089, #15334 ) ) ;
#65732=CARTESIAN_POINT ( 'NONE',  ( 8.144523737882815695, 9.547976262117185087, 54.00000000000000711 ) ) ;
#65736=DIRECTION ( 'NONE',  ( 0.000000000000000000, 1.000000000000000000, 0.000000000000000000 ) ) ;
#65737=CARTESIAN_POINT ( 'NONE',  ( -6.835476262117260227, 10.30047626211718104, 54.00000000000000711 ) ) ;
#65739=LINE ( 'NONE', #39542, #21840 ) ;
#65741=AXIS2_PLACEMENT_3D ( 'NONE', #56471, #8018, #29592 ) ;
#65742=ORIENTED_EDGE ( 'NONE', *, *, #53014, .F. ) ;
#65749=VECTOR ( 'NONE', #64447, 1000.000000000000000 ) ;
#65750=CYLINDRICAL_SURFACE ( 'NONE', #62880, 0.1749999999999998224 ) ;
#65752=VECTOR ( 'NONE', #55301, 1000.000000000000000 ) ;
#65761=ORIENTED_EDGE ( 'NONE', *, *, #41744, .T. ) ;
#65762=CARTESIAN_POINT ( 'NONE',  ( 5.257023737882819070, -5.257023737882825287, 54.00000000000000711 ) ) ;
#65780=EDGE_CURVE ( 'NONE', #19808, #51221, #48927, .T. ) ;
#65786=EDGE_CURVE ( 'NONE', #47516, #53330, #2389, .T. ) ;
#65787=ORIENTED_EDGE ( 'NONE', *, *, #9033, .T. ) ;
#65789=CARTESIAN_POINT ( 'NONE',  ( 8.930623737882845248, 8.916576262117187568, 54.00000000000000711 ) ) ;
#65793=VECTOR ( 'NONE', #40539, 1000.000000000000000 ) ;
#65796=EDGE_CURVE ( 'NONE', #18995, #26808, #41621, .T. ) ;
#65797=ORIENTED_EDGE ( 'NONE', *, *, #60432, .F. ) ;
#65806=VERTEX_POINT ( 'NONE', #19687 ) ;
#65811=CIRCLE ( 'NONE', #13820, 0.1749999999999998224 ) ;
#65821=VERTEX_POINT ( 'NONE', #67793 ) ;
#65825=CARTESIAN_POINT ( 'NONE',  ( 9.404523737882758638, 1.466476262117154983, 54.00000000000000711 ) ) ;
#65827=DIRECTION ( 'NONE',  ( -1.836970198721029934E-16, 1.836970198721036344E-16, -1.000000000000000000 ) ) ;
#65831=EDGE_LOOP ( 'NONE', ( #8326, #9480, #15662, #18932 ) ) ;
#65832=EDGE_CURVE ( 'NONE', #12339, #59528, #34898, .T. ) ;
#65833=ADVANCED_FACE ( 'NONE', ( #35966 ), #61789, .T. ) ;
#65847=VERTEX_POINT ( 'NONE', #46916 ) ;
#65848=FACE_OUTER_BOUND ( 'NONE', #3554, .T. ) ;
#65854=LINE ( 'NONE', #65521, #29236 ) ;
#65859=DIRECTION ( 'NONE',  ( -0.000000000000000000, -0.000000000000000000, -1.000000000000000000 ) ) ;
#65864=CIRCLE ( 'NONE', #4910, 0.5249999999999990230 ) ;
#65870=FACE_OUTER_BOUND ( 'NONE', #3568, .T. ) ;
#65871=EDGE_CURVE ( 'NONE', #8868, #2504, #40912, .T. ) ;
#65886=EDGE_CURVE ( 'NONE', #4021, #24174, #53298, .T. ) ;
#65889=FACE_OUTER_BOUND ( 'NONE', #4966, .T. ) ;
#65900=VECTOR ( 'NONE', #6926, 1000.000000000000000 ) ;
#65903=EDGE_LOOP ( 'NONE', ( #37735, #36704, #28767, #25156 ) ) ;
#65909=ORIENTED_EDGE ( 'NONE', *, *, #48091, .T. ) ;
#65916=LINE ( 'NONE', #62001, #63899 ) ;
#65922=DIRECTION ( 'NONE',  ( 1.261617073437657735E-14, 1.000000000000000000, 0.000000000000000000 ) ) ;
#65924=DIRECTION ( 'NONE',  ( -1.000000000000000000, -2.135044278125301343E-15, -7.844025423732065664E-31 ) ) ;
#65925=EDGE_CURVE ( 'NONE', #65138, #65565, #26308, .T. ) ;
#65927=PLANE ( 'NONE',  #5511 ) ;
#65928=FACE_OUTER_BOUND ( 'NONE', #68674, .T. ) ;
#65929=LINE ( 'NONE', #33425, #69533 ) ;
#65939=CARTESIAN_POINT ( 'NONE',  ( 2.369523737882817116, 9.547976262117204627, 54.00000000000000711 ) ) ;
#65941=CIRCLE ( 'NONE', #44490, 0.1749999999999998224 ) ;
#65942=CIRCLE ( 'NONE', #59156, 0.1749999999999998224 ) ;
#65943=EDGE_CURVE ( 'NONE', #46756, #96, #53640, .T. ) ;
#65951=ORIENTED_EDGE ( 'NONE', *, *, #17534, .T. ) ;
#65956=CARTESIAN_POINT ( 'NONE',  ( 5.793274621760810206, 4.141586236041043811, 26.00000000000000711 ) ) ;
#65957=EDGE_CURVE ( 'NONE', #12566, #68940, #54581, .T. ) ;
#65963=VERTEX_POINT ( 'NONE', #31014 ) ;
#65967=DIRECTION ( 'NONE',  ( 1.836970198721029934E-16, 1.836970198721010706E-16, -1.000000000000000000 ) ) ;
#65970=DIRECTION ( 'NONE',  ( 0.000000000000000000, 1.000000000000000000, 0.000000000000000000 ) ) ;
#65973=VERTEX_POINT ( 'NONE', #22502 ) ;
#65975=DIRECTION ( 'NONE',  ( 9.912705577010336396E-15, 1.000000000000000000, 0.000000000000000000 ) ) ;
#65976=CARTESIAN_POINT ( 'NONE',  ( 3.677663764522614454, -6.364920264886879231, 54.00000000000000711 ) ) ;
#65990=LINE ( 'NONE', #60698, #68335 ) ;
#66014=AXIS2_PLACEMENT_3D ( 'NONE', #1456, #23024, #66163 ) ;
#66016=DIRECTION ( 'NONE',  ( -0.000000000000000000, 3.673940397442059868E-16, -1.000000000000000000 ) ) ;
#66017=DIRECTION ( 'NONE',  ( 1.000000000000000000, -1.356437060717832013E-15, -1.836970198721032646E-16 ) ) ;
#66019=DIRECTION ( 'NONE',  ( 1.000000000000000000, 0.000000000000000000, 0.000000000000000000 ) ) ;
#66049=CARTESIAN_POINT ( 'NONE',  ( 2.420780051175148273, -8.711985858128667104, 26.00000000000000000 ) ) ;
#66069=CARTESIAN_POINT ( 'NONE',  ( -6.486996718459903555, -2.632023737882784431, 54.00000000000000711 ) ) ;
#66070=ORIENTED_EDGE ( 'NONE', *, *, #51138, .T. ) ;
#66077=ADVANCED_FACE ( 'NONE', ( #60308 ), #49708, .F. ) ;
#66078=CARTESIAN_POINT ( 'NONE',  ( -9.390476262117259054, 1.466476262117183182, 54.00000000000000711 ) ) ;
#66082=DIRECTION ( 'NONE',  ( 0.000000000000000000, 1.000000000000000000, 0.000000000000000000 ) ) ;
#66086=ORIENTED_EDGE ( 'NONE', *, *, #44047, .F. ) ;
#66093=VECTOR ( 'NONE', #41924, 1000.000000000000000 ) ;
#66107=CARTESIAN_POINT ( 'NONE',  ( 8.930623737882818602, -9.703773737882825046, 54.00000000000000711 ) ) ;
#66112=CARTESIAN_POINT ( 'NONE',  ( -3.650476262117335668, -10.50702373788282173, 54.00000000000000711 ) ) ;
#66120=LINE ( 'NONE', #27604, #34384 ) ;
#66132=FACE_BOUND ( 'NONE', #35847, .T. ) ;
#66134=ADVANCED_FACE ( 'NONE', ( #35890 ), #62392, .F. ) ;
#66142=ORIENTED_EDGE ( 'NONE', *, *, #67296, .T. ) ;
#66146=DIRECTION ( 'NONE',  ( 1.000000000000000000, -1.115702204244422993E-14, -1.836970198721050395E-16 ) ) ;
#66150=ORIENTED_EDGE ( 'NONE', *, *, #17196, .T. ) ;
#66153=AXIS2_PLACEMENT_3D ( 'NONE', #57756, #3669, #68370 ) ;
#66157=CARTESIAN_POINT ( 'NONE',  ( -9.689726262117309474, -8.580623737882753232, 26.00000000000000000 ) ) ;
#66158=CARTESIAN_POINT ( 'NONE',  ( 9.737023737882763541, 2.530476262117156594, 26.00000000000000711 ) ) ;
#66159=LINE ( 'NONE', #64788, #16465 ) ;
#66160=VECTOR ( 'NONE', #60272, 1000.000000000000000 ) ;
#66161=CIRCLE ( 'NONE', #27813, 0.1749999999999998224 ) ;
#66163=DIRECTION ( 'NONE',  ( -1.000000000000000000, 0.000000000000000000, 0.000000000000000000 ) ) ;
#66169=ORIENTED_EDGE ( 'NONE', *, *, #38186, .T. ) ;
#66170=VECTOR ( 'NONE', #14710, 1000.000000000000000 ) ;
#66172=EDGE_CURVE ( 'NONE', #58217, #7028, #34463, .T. ) ;
#66173=DIRECTION ( 'NONE',  ( 1.000000000000000000, 0.000000000000000000, 0.000000000000000000 ) ) ;
#66184=EDGE_LOOP ( 'NONE', ( #11553, #46042, #20498, #15774 ) ) ;
#66186=PLANE ( 'NONE',  #36182 ) ;
#66189=LINE ( 'NONE', #39982, #7444 ) ;
#66196=DIRECTION ( 'NONE',  ( -1.836970198721029934E-16, 1.836970198721036344E-16, -1.000000000000000000 ) ) ;
#66197=CARTESIAN_POINT ( 'NONE',  ( -3.650476262117221093, 10.49297626211717116, 54.00000000000000711 ) ) ;
#66202=LINE ( 'NONE', #17766, #57595 ) ;
#66203=VECTOR ( 'NONE', #37518, 1000.000000000000000 ) ;
#66204=AXIS2_PLACEMENT_3D ( 'NONE', #35481, #2614, #2271 ) ;
#66209=VECTOR ( 'NONE', #50277, 1000.000000000000000 ) ;
#66223=DIRECTION ( 'NONE',  ( -1.000000000000000000, 0.000000000000000000, 0.000000000000000000 ) ) ;
#66225=VECTOR ( 'NONE', #36311, 1000.000000000000000 ) ;
#66231=ORIENTED_EDGE ( 'NONE', *, *, #27795, .T. ) ;
#66236=DIRECTION ( 'NONE',  ( 1.836970198721029934E-16, 1.836970198721010706E-16, -1.000000000000000000 ) ) ;
#66238=ORIENTED_EDGE ( 'NONE', *, *, #32508, .T. ) ;
#66241=DIRECTION ( 'NONE',  ( -0.000000000000000000, -0.000000000000000000, -1.000000000000000000 ) ) ;
#66242=DIRECTION ( 'NONE',  ( 1.836970198721029934E-16, 1.836970198721010706E-16, -1.000000000000000000 ) ) ;
#66244=CARTESIAN_POINT ( 'NONE',  ( 8.930623737882818602, -9.703773737882814387, 26.00000000000000000 ) ) ;
#66245=EDGE_LOOP ( 'NONE', ( #48756, #37123, #68625, #61850 ) ) ;
#66247=CARTESIAN_POINT ( 'NONE',  ( -7.342976262117293373, -6.665817930929262225, 54.00000000000000711 ) ) ;
#66248=CARTESIAN_POINT ( 'NONE',  ( 7.969523737882811432, 9.547976262117192192, 26.00000000000000711 ) ) ;
#66252=AXIS2_PLACEMENT_3D ( 'NONE', #12003, #28278, #49847 ) ;
#66260=CIRCLE ( 'NONE', #17704, 0.1749999999999989342 ) ;
#66263=EDGE_LOOP ( 'NONE', ( #6138, #37052, #3456, #9827 ) ) ;
#66265=CYLINDRICAL_SURFACE ( 'NONE', #68962, 0.5249999999999994671 ) ;
#66267=VECTOR ( 'NONE', #14511, 1000.000000000000000 ) ;
#66277=PLANE ( 'NONE',  #50301 ) ;
#66279=CARTESIAN_POINT ( 'NONE',  ( 5.257023737882819070, -5.257023737882815517, 26.00000000000000711 ) ) ;
#66283=ADVANCED_FACE ( 'NONE', ( #41889 ), #15727, .F. ) ;
#66292=CARTESIAN_POINT ( 'NONE',  ( -6.350872789121377870, -6.836383711242978833, 54.00000000000000711 ) ) ;
#66295=VECTOR ( 'NONE', #8822, 1000.000000000000000 ) ;
#66300=ORIENTED_EDGE ( 'NONE', *, *, #5524, .T. ) ;
#66303=CARTESIAN_POINT ( 'NONE',  ( 3.682023737882814007, 9.722976262117208890, 26.00000000000000711 ) ) ;
#66306=LINE ( 'NONE', #17513, #65067 ) ;
#66313=EDGE_CURVE ( 'NONE', #56866, #44739, #37293, .T. ) ;
#66317=FACE_OUTER_BOUND ( 'NONE', #41719, .T. ) ;
#66324=EDGE_CURVE ( 'NONE', #3393, #28592, #25292, .T. ) ;
#66333=LINE ( 'NONE', #48684, #53310 ) ;
#66334=ORIENTED_EDGE ( 'NONE', *, *, #65943, .T. ) ;
#66345=CARTESIAN_POINT ( 'NONE',  ( 8.144523737882817471, -9.562023737882817898, 54.00000000000000711 ) ) ;
#66348=ORIENTED_EDGE ( 'NONE', *, *, #4647, .F. ) ;
#66352=CARTESIAN_POINT ( 'NONE',  ( 8.241237374594303944, -1.634292677759888068, 54.00000000000000711 ) ) ;
#66354=ORIENTED_EDGE ( 'NONE', *, *, #51271, .F. ) ;
#66361=EDGE_CURVE ( 'NONE', #68364, #21659, #165, .T. ) ;
#66364=AXIS2_PLACEMENT_3D ( 'NONE', #28722, #59535, #29417 ) ;
#66366=ADVANCED_FACE ( 'NONE', ( #17439 ), #6509, .T. ) ;
#66379=DIRECTION ( 'NONE',  ( -0.7671651518153105309, -0.6414496315691445849, 0.000000000000000000 ) ) ;
#66382=PLANE ( 'NONE',  #13934 ) ;
#66385=PLANE ( 'NONE',  #41779 ) ;
#66386=DIRECTION ( 'NONE',  ( 1.836970198721029934E-16, 1.836970198721010706E-16, -1.000000000000000000 ) ) ;
#66389=DIRECTION ( 'NONE',  ( -0.000000000000000000, -0.000000000000000000, -1.000000000000000000 ) ) ;
#66393=CARTESIAN_POINT ( 'NONE',  ( -9.547976262117256141, 7.955476262117183062, 54.00000000000000711 ) ) ;
#66394=CARTESIAN_POINT ( 'NONE',  ( -5.242976262117259978, 3.142976262117183062, 54.00000000000000711 ) ) ;
#66397=CARTESIAN_POINT ( 'NONE',  ( 7.969523737882816761, 9.547976262117186863, 54.00000000000000711 ) ) ;
#66400=CARTESIAN_POINT ( 'NONE',  ( -9.915476262117259409, 0.9414762621171833823, 54.00000000000000711 ) ) ;
#66403=LINE ( 'NONE', #7690, #57995 ) ;
#66406=DIRECTION ( 'NONE',  ( -1.836970198721029934E-16, -1.836970198721010706E-16, 1.000000000000000000 ) ) ;
#66407=ORIENTED_EDGE ( 'NONE', *, *, #11903, .F. ) ;
#66410=AXIS2_PLACEMENT_3D ( 'NONE', #8687, #67029, #24950 ) ;
#66423=CARTESIAN_POINT ( 'NONE',  ( 7.357023737882797398, 4.947141984184415087, 54.00000000000000711 ) ) ;
#66425=PLANE ( 'NONE',  #26710 ) ;
#66428=ORIENTED_EDGE ( 'NONE', *, *, #66993, .T. ) ;
#66431=EDGE_LOOP ( 'NONE', ( #14892, #54707, #48170, #252 ) ) ;
#66440=VERTEX_POINT ( 'NONE', #33022 ) ;
#66454=ORIENTED_EDGE ( 'NONE', *, *, #44796, .T. ) ;
#66460=LINE ( 'NONE', #66112, #11363 ) ;
#66473=LINE ( 'NONE', #62213, #50096 ) ;
#66476=EDGE_CURVE ( 'NONE', #36864, #57348, #40751, .T. ) ;
#66477=DIRECTION ( 'NONE',  ( -1.836970198721029934E-16, 1.836970198721036590E-16, -1.000000000000000000 ) ) ;
#66484=DIRECTION ( 'NONE',  ( -0.7671651518152963201, 0.6414496315691619044, 0.000000000000000000 ) ) ;
#66487=ORIENTED_EDGE ( 'NONE', *, *, #61270, .T. ) ;
#66489=EDGE_CURVE ( 'NONE', #64510, #32481, #23450, .T. ) ;
#66512=EDGE_CURVE ( 'NONE', #3798, #48826, #30147, .T. ) ;
#66530=DIRECTION ( 'NONE',  ( -1.000000000000000000, 4.745709458399858621E-16, 1.836970198721030674E-16 ) ) ;
#66533=EDGE_LOOP ( 'NONE', ( #51668, #44407, #41902, #11967 ) ) ;
#66535=DIRECTION ( 'NONE',  ( -1.000000000000000000, 1.260948829465470062E-14, -1.836970198721007008E-16 ) ) ;
#66538=ORIENTED_EDGE ( 'NONE', *, *, #45281, .F. ) ;
#66541=DIRECTION ( 'NONE',  ( -0.000000000000000000, -0.000000000000000000, -1.000000000000000000 ) ) ;
#66550=VECTOR ( 'NONE', #56928, 1000.000000000000000 ) ;
#66563=DIRECTION ( 'NONE',  ( 0.000000000000000000, 1.000000000000000000, 0.000000000000000000 ) ) ;
#66569=VERTEX_POINT ( 'NONE', #62661 ) ;
#66579=EDGE_CURVE ( 'NONE', #66440, #64822, #52422, .T. ) ;
#66583=VERTEX_POINT ( 'NONE', #68326 ) ;
#66594=ORIENTED_EDGE ( 'NONE', *, *, #25767, .F. ) ;
#66597=VECTOR ( 'NONE', #50747, 1000.000000000000000 ) ;
#66615=DIRECTION ( 'NONE',  ( -0.8660254037844435926, -0.4999999999999913958, 0.000000000000000000 ) ) ;
#66621=EDGE_CURVE ( 'NONE', #9302, #3011, #15985, .T. ) ;
#66622=DIRECTION ( 'NONE',  ( -3.016910393003147986E-15, -1.000000000000000000, -3.673940397442059868E-16 ) ) ;
#66623=ORIENTED_EDGE ( 'NONE', *, *, #61790, .T. ) ;
#66630=DIRECTION ( 'NONE',  ( -1.000000000000000000, 0.000000000000000000, 0.000000000000000000 ) ) ;
#66634=ORIENTED_EDGE ( 'NONE', *, *, #32359, .T. ) ;
#66639=CARTESIAN_POINT ( 'NONE',  ( 1.480523737882816437, 9.390476262117212869, 54.00000000000000711 ) ) ;
#66645=VERTEX_POINT ( 'NONE', #3631 ) ;
#66648=PLANE ( 'NONE',  #48925 ) ;
#66656=EDGE_CURVE ( 'NONE', #68234, #2701, #58438, .T. ) ;
#66662=EDGE_CURVE ( 'NONE', #12591, #43731, #36143, .T. ) ;
#66665=DIRECTION ( 'NONE',  ( -1.000000000000000000, 0.000000000000000000, 0.000000000000000000 ) ) ;
#66669=CARTESIAN_POINT ( 'NONE',  ( -9.722976262117258628, 6.817976262117182884, 26.00000000000000711 ) ) ;
#66688=EDGE_LOOP ( 'NONE', ( #19570, #21049, #55675, #52196 ) ) ;
#66689=ORIENTED_EDGE ( 'NONE', *, *, #64356, .F. ) ;
#66722=DIRECTION ( 'NONE',  ( 1.836970198721029934E-16, 1.836970198721010706E-16, -1.000000000000000000 ) ) ;
#66729=DIRECTION ( 'NONE',  ( -0.000000000000000000, -0.000000000000000000, -1.000000000000000000 ) ) ;
#66732=DIRECTION ( 'NONE',  ( -1.836970198721029934E-16, 1.836970198721036590E-16, -1.000000000000000000 ) ) ;
#66734=CARTESIAN_POINT ( 'NONE',  ( 5.257023737882819070, -5.257023737882825287, 54.00000000000000711 ) ) ;
#66757=ORIENTED_EDGE ( 'NONE', *, *, #21906, .T. ) ;
#66759=CARTESIAN_POINT ( 'NONE',  ( -6.350872789121373430, -6.836383711242974393, 26.00000000000000711 ) ) ;
#66760=FACE_OUTER_BOUND ( 'NONE', #68135, .T. ) ;
#66763=DIRECTION ( 'NONE',  ( -1.000000000000000000, 1.261617073437657735E-14, 4.635105932205236432E-30 ) ) ;
#66775=ORIENTED_EDGE ( 'NONE', *, *, #55803, .F. ) ;
#66778=CARTESIAN_POINT ( 'NONE',  ( -9.547976262117300550, -8.144523737882753522, 26.00000000000000000 ) ) ;
#66788=CARTESIAN_POINT ( 'NONE',  ( -8.130476262117324993, -9.562023737882769936, 54.00000000000000711 ) ) ;
#66795=CARTESIAN_POINT ( 'NONE',  ( 3.664523737882819709, 10.30047626211720413, 54.00000000000000711 ) ) ;
#66796=LINE ( 'NONE', #2796, #41443 ) ;
#66797=CIRCLE ( 'NONE', #12581, 0.1749999999999998224 ) ;
#66798=CIRCLE ( 'NONE', #207, 0.1749999999999998224 ) ;
#66799=DIRECTION ( 'NONE',  ( 1.000000000000000000, -6.308085367188447236E-15, -2.317552966102676720E-30 ) ) ;
#66805=DIRECTION ( 'NONE',  ( 1.000000000000000000, -2.990116172375847553E-15, -1.836970198721035357E-16 ) ) ;
#66806=DIRECTION ( 'NONE',  ( 0.000000000000000000, -1.000000000000000000, 0.000000000000000000 ) ) ;
#66811=ORIENTED_EDGE ( 'NONE', *, *, #32366, .F. ) ;
#66812=DIRECTION ( 'NONE',  ( -0.000000000000000000, -1.000000000000000000, -0.000000000000000000 ) ) ;
#66826=ADVANCED_FACE ( 'NONE', ( #783 ), #59469, .T. ) ;
#66831=EDGE_CURVE ( 'NONE', #56086, #58466, #17356, .T. ) ;
#66837=ORIENTED_EDGE ( 'NONE', *, *, #24363, .F. ) ;
#66839=CARTESIAN_POINT ( 'NONE',  ( -6.642976262117329611, -10.31452373788278365, 26.00000000000000000 ) ) ;
#66840=EDGE_CURVE ( 'NONE', #40034, #5797, #67188, .T. ) ;
#66842=DIRECTION ( 'NONE',  ( 0.000000000000000000, -3.673940397442059868E-16, 1.000000000000000000 ) ) ;
#66852=ORIENTED_EDGE ( 'NONE', *, *, #37612, .T. ) ;
#66859=ORIENTED_EDGE ( 'NONE', *, *, #47102, .F. ) ;
#66864=ORIENTED_EDGE ( 'NONE', *, *, #47627, .F. ) ;
#66869=ORIENTED_EDGE ( 'NONE', *, *, #13263, .F. ) ;
#66874=CARTESIAN_POINT ( 'NONE',  ( -6.817976262117261044, 9.722976262117182245, 54.00000000000000711 ) ) ;
#66880=CARTESIAN_POINT ( 'NONE',  ( -4.135079735113208699, -3.677663764522613121, 54.00000000000000711 ) ) ;
#66886=DIRECTION ( 'NONE',  ( 0.000000000000000000, 0.000000000000000000, 1.000000000000000000 ) ) ;
#66896=ORIENTED_EDGE ( 'NONE', *, *, #15181, .T. ) ;
#66899=ORIENTED_EDGE ( 'NONE', *, *, #68299, .T. ) ;
#66908=EDGE_LOOP ( 'NONE', ( #2264, #29825, #27227, #14380 ) ) ;
#66928=CARTESIAN_POINT ( 'NONE',  ( -6.835476262117333057, -10.31452373788278543, 54.00000000000000711 ) ) ;
#66929=CARTESIAN_POINT ( 'NONE',  ( -10.49297626211732748, -9.795823737882738413, 54.00000000000000711 ) ) ;
#66938=CARTESIAN_POINT ( 'NONE',  ( -7.955476262117326947, -9.737023737882770646, 54.00000000000000711 ) ) ;
#66945=ORIENTED_EDGE ( 'NONE', *, *, #47526, .T. ) ;
#66946=VERTEX_POINT ( 'NONE', #20504 ) ;
#66948=VERTEX_POINT ( 'NONE', #41008 ) ;
#66949=ORIENTED_EDGE ( 'NONE', *, *, #41959, .T. ) ;
#66955=ORIENTED_EDGE ( 'NONE', *, *, #42269, .T. ) ;
#66970=CYLINDRICAL_SURFACE ( 'NONE', #58672, 0.1749999999999989342 ) ;
#66976=DIRECTION ( 'NONE',  ( 1.836970198721029934E-16, 1.836970198721010706E-16, -1.000000000000000000 ) ) ;
#66980=CARTESIAN_POINT ( 'NONE',  ( 8.711985858128686644, 8.079219948824833963, 54.00000000000000711 ) ) ;
#66983=PLANE ( 'NONE',  #37073 ) ;
#66984=VECTOR ( 'NONE', #38594, 1000.000000000000000 ) ;
#66988=DIRECTION ( 'NONE',  ( -1.836970198721029934E-16, 1.836970198721036590E-16, -1.000000000000000000 ) ) ;
#66992=CARTESIAN_POINT ( 'NONE',  ( 6.849523737882818430, 10.49297626211719603, 54.00000000000000711 ) ) ;
#66993=EDGE_CURVE ( 'NONE', #22404, #61284, #26510, .T. ) ;
#66995=CARTESIAN_POINT ( 'NONE',  ( -5.242976262117259978, 5.242976262117182706, 26.00000000000000711 ) ) ;
#66997=CARTESIAN_POINT ( 'NONE',  ( 3.857023737882817827, 9.897976262117204271, 54.00000000000000711 ) ) ;
#67000=ORIENTED_EDGE ( 'NONE', *, *, #49831, .T. ) ;
#67007=VERTEX_POINT ( 'NONE', #25109 ) ;
#67014=FACE_OUTER_BOUND ( 'NONE', #52100, .T. ) ;
#67029=DIRECTION ( 'NONE',  ( -1.836970198721029934E-16, -1.836970198721010706E-16, 1.000000000000000000 ) ) ;
#67030=ORIENTED_EDGE ( 'NONE', *, *, #54846, .F. ) ;
#67035=ORIENTED_EDGE ( 'NONE', *, *, #57874, .F. ) ;
#67038=CARTESIAN_POINT ( 'NONE',  ( -9.547976262117217061, -2.369523737882723857, 26.00000000000000711 ) ) ;
#67048=EDGE_CURVE ( 'NONE', #10751, #10538, #38513, .T. ) ;
#67052=EDGE_CURVE ( 'NONE', #55172, #68234, #12943, .T. ) ;
#67054=CARTESIAN_POINT ( 'NONE',  ( 9.703773737882809058, 8.566576262117189700, 26.00000000000000711 ) ) ;
#67058=DIRECTION ( 'NONE',  ( -0.000000000000000000, 1.000000000000000000, -0.000000000000000000 ) ) ;
#67064=VECTOR ( 'NONE', #61966, 1000.000000000000000 ) ;
#67092=DIRECTION ( 'NONE',  ( -1.000000000000000000, 0.000000000000000000, 0.000000000000000000 ) ) ;
#67095=EDGE_CURVE ( 'NONE', #29034, #68798, #5643, .T. ) ;
#67103=ORIENTED_EDGE ( 'NONE', *, *, #65360, .T. ) ;
#67105=DIRECTION ( 'NONE',  ( 0.000000000000000000, -3.673940397442059868E-16, 1.000000000000000000 ) ) ;
#67108=CARTESIAN_POINT ( 'NONE',  ( -5.242976262117275077, -5.257023737882800418, 26.00000000000000711 ) ) ;
#67110=AXIS2_PLACEMENT_3D ( 'NONE', #33095, #5884, #577 ) ;
#67114=CARTESIAN_POINT ( 'NONE',  ( 10.50702373788281996, -6.849523737882823760, 54.00000000000000711 ) ) ;
#67117=AXIS2_PLACEMENT_3D ( 'NONE', #9928, #20870, #5663 ) ;
#67125=CIRCLE ( 'NONE', #36645, 1.929199999999998028 ) ;
#67126=CARTESIAN_POINT ( 'NONE',  ( 6.789561617636929114, 7.394232575409553476, 26.00000000000000711 ) ) ;
#67134=DIRECTION ( 'NONE',  ( -1.836970198721029934E-16, 1.836970198721036590E-16, -1.000000000000000000 ) ) ;
#67137=CARTESIAN_POINT ( 'NONE',  ( 1.480523737882816437, 9.390476262117212869, 54.00000000000000711 ) ) ;
#67138=DIRECTION ( 'NONE',  ( -3.596772705736694889E-15, -1.000000000000000000, 0.000000000000000000 ) ) ;
#67140=DIRECTION ( 'NONE',  ( 0.000000000000000000, 3.673940397442059868E-16, -1.000000000000000000 ) ) ;
#67141=EDGE_CURVE ( 'NONE', #68930, #355, #21219, .T. ) ;
#67143=ADVANCED_FACE ( 'NONE', ( #59033 ), #21892, .T. ) ;
#67153=CYLINDRICAL_SURFACE ( 'NONE', #22283, 0.3499999999999996447 ) ;
#67154=DIRECTION ( 'NONE',  ( -0.000000000000000000, -0.000000000000000000, -1.000000000000000000 ) ) ;
#67164=CARTESIAN_POINT ( 'NONE',  ( 4.720772854004774643, -6.358413763958971288, 54.00000000000000711 ) ) ;
#67174=CARTESIAN_POINT ( 'NONE',  ( 6.849523737882817542, -10.31452373788282095, 54.00000000000000711 ) ) ;
#67180=VECTOR ( 'NONE', #17070, 1000.000000000000000 ) ;
#67184=EDGE_CURVE ( 'NONE', #37047, #26866, #49468, .T. ) ;
#67187=EDGE_CURVE ( 'NONE', #56487, #21960, #9598, .T. ) ;
#67188=LINE ( 'NONE', #8126, #11795 ) ;
#67189=CARTESIAN_POINT ( 'NONE',  ( 3.682023737882785586, -9.912023737882808661, 54.00000000000000711 ) ) ;
#67194=ORIENTED_EDGE ( 'NONE', *, *, #28797, .F. ) ;
#67200=CARTESIAN_POINT ( 'NONE',  ( -8.821682069070751808, -2.544523737882741887, 54.00000000000000711 ) ) ;
#67201=DIRECTION ( 'NONE',  ( 8.359604446858500663E-15, 1.000000000000000000, 3.673940397442059868E-16 ) ) ;
#67224=VERTEX_POINT ( 'NONE', #34912 ) ;
#67227=DIRECTION ( 'NONE',  ( -0.000000000000000000, -0.000000000000000000, -1.000000000000000000 ) ) ;
#67232=LINE ( 'NONE', #18789, #6403 ) ;
#67241=EDGE_CURVE ( 'NONE', #67224, #64674, #18605, .T. ) ;
#67249=ORIENTED_EDGE ( 'NONE', *, *, #32431, .T. ) ;
#67254=ORIENTED_EDGE ( 'NONE', *, *, #25157, .F. ) ;
#67256=LINE ( 'NONE', #2543, #35698 ) ;
#67257=AXIS2_PLACEMENT_3D ( 'NONE', #67597, #69609, #56966 ) ;
#67258=CYLINDRICAL_SURFACE ( 'NONE', #16720, 0.1749999999999989342 ) ;
#67261=AXIS2_PLACEMENT_3D ( 'NONE', #28565, #57194, #23270 ) ;
#67274=VERTEX_POINT ( 'NONE', #55800 ) ;
#67278=CIRCLE ( 'NONE', #65020, 0.1749999999999993783 ) ;
#67279=ORIENTED_EDGE ( 'NONE', *, *, #8612, .F. ) ;
#67286=PLANE ( 'NONE',  #45252 ) ;
#67296=EDGE_CURVE ( 'NONE', #29966, #28048, #2743, .T. ) ;
#67308=ADVANCED_FACE ( 'NONE', ( #25291 ), #68425, .F. ) ;
#67311=FACE_OUTER_BOUND ( 'NONE', #55570, .T. ) ;
#67321=DIRECTION ( 'NONE',  ( -1.000000000000000000, 1.813998472013049822E-14, -1.836970198720996654E-16 ) ) ;
#67331=CARTESIAN_POINT ( 'NONE',  ( 10.31452373788281562, -6.657023737882825642, 54.00000000000000711 ) ) ;
#67341=VERTEX_POINT ( 'NONE', #4780 ) ;
#67343=ADVANCED_FACE ( 'NONE', ( #32005 ), #177, .T. ) ;
#67345=DIRECTION ( 'NONE',  ( 1.570596175624152290E-15, -1.000000000000000000, 0.000000000000000000 ) ) ;
#67349=CARTESIAN_POINT ( 'NONE',  ( 4.149127210878725158, -3.677663764522648648, 54.00000000000000711 ) ) ;
#67352=VERTEX_POINT ( 'NONE', #20336 ) ;
#67353=CARTESIAN_POINT ( 'NONE',  ( -7.955476262117259445, 9.547976262117179758, 54.00000000000000711 ) ) ;
#67358=LINE ( 'NONE', #45780, #40972 ) ;
#67367=AXIS2_PLACEMENT_3D ( 'NONE', #65762, #50188, #55161 ) ;
#67388=ORIENTED_EDGE ( 'NONE', *, *, #11560, .T. ) ;
#67391=LINE ( 'NONE', #18945, #18332 ) ;
#67394=CARTESIAN_POINT ( 'NONE',  ( 10.50702373788281996, -3.664523737882826815, 54.00000000000000711 ) ) ;
#67407=ORIENTED_EDGE ( 'NONE', *, *, #26984, .F. ) ;
#67408=DIRECTION ( 'NONE',  ( -1.836970198721029934E-16, -1.836970198721010706E-16, 1.000000000000000000 ) ) ;
#67416=CIRCLE ( 'NONE', #53862, 0.3499999999999996447 ) ;
#67417=DIRECTION ( 'NONE',  ( 1.000000000000000000, 0.000000000000000000, 0.000000000000000000 ) ) ;
#67418=DIRECTION ( 'NONE',  ( 0.8660254037844510311, 0.4999999999999786282, 0.000000000000000000 ) ) ;
#67423=ADVANCED_FACE ( 'NONE', ( #33718 ), #55300, .F. ) ;
#67427=CARTESIAN_POINT ( 'NONE',  ( 7.357023737882817827, -4.961189459950053227, 26.00000000000000711 ) ) ;
#67441=DIRECTION ( 'NONE',  ( 3.491481338843133355E-15, 1.000000000000000000, 1.836970198721029934E-16 ) ) ;
#67445=CARTESIAN_POINT ( 'NONE',  ( 8.144523737882817471, -9.562023737882809016, 26.00000000000000000 ) ) ;
#67446=DIRECTION ( 'NONE',  ( 1.836970198721029934E-16, 1.836970198721010706E-16, -1.000000000000000000 ) ) ;
#67469=AXIS2_PLACEMENT_3D ( 'NONE', #8719, #46888, #41944 ) ;
#67496=ORIENTED_EDGE ( 'NONE', *, *, #34059, .F. ) ;
#67507=CARTESIAN_POINT ( 'NONE',  ( 6.657023737882818537, -10.31452373788282095, 54.00000000000000711 ) ) ;
#67515=EDGE_CURVE ( 'NONE', #19689, #43731, #14175, .T. ) ;
#67525=DIRECTION ( 'NONE',  ( 1.000000000000000000, -1.356437060717834379E-15, -1.836970198721032646E-16 ) ) ;
#67534=CIRCLE ( 'NONE', #66410, 0.7112000000000124889 ) ;
#67540=DIRECTION ( 'NONE',  ( -0.000000000000000000, 3.673940397442059868E-16, -1.000000000000000000 ) ) ;
#67552=CARTESIAN_POINT ( 'NONE',  ( 2.420780051175148273, -8.711985858128677762, 54.00000000000000711 ) ) ;
#67558=ORIENTED_EDGE ( 'NONE', *, *, #57429, .T. ) ;
#67574=DIRECTION ( 'NONE',  ( 0.7071067811865474617, -0.7071067811865474617, -2.597868168706479611E-16 ) ) ;
#67584=ORIENTED_EDGE ( 'NONE', *, *, #67095, .F. ) ;
#67591=CARTESIAN_POINT ( 'NONE',  ( -10.03972626211722918, 9.689726262117183353, 54.00000000000000711 ) ) ;
#67592=ADVANCED_FACE ( 'NONE', ( #24510 ), #68342, .F. ) ;
#67597=CARTESIAN_POINT ( 'NONE',  ( -10.30047626211729295, -6.657023737882751924, 54.00000000000000711 ) ) ;
#67599=CARTESIAN_POINT ( 'NONE',  ( 8.711985858128681315, 8.079219948824839292, 26.00000000000000711 ) ) ;
#67609=DIRECTION ( 'NONE',  ( 0.7071067811865411334, -0.7071067811865539010, -2.597868168706484541E-16 ) ) ;
#67617=LINE ( 'NONE', #46047, #29090 ) ;
#67618=AXIS2_PLACEMENT_3D ( 'NONE', #31228, #31915, #64103 ) ;
#67633=EDGE_CURVE ( 'NONE', #38190, #48101, #36156, .T. ) ;
#67635=VERTEX_POINT ( 'NONE', #41472 ) ;
#67637=VECTOR ( 'NONE', #13684, 1000.000000000000000 ) ;
#67642=DIRECTION ( 'NONE',  ( 1.000000000000000000, -3.016910393003147986E-15, 0.000000000000000000 ) ) ;
#67649=ORIENTED_EDGE ( 'NONE', *, *, #53545, .T. ) ;
#67652=EDGE_CURVE ( 'NONE', #34600, #50090, #37573, .T. ) ;
#67660=CARTESIAN_POINT ( 'NONE',  ( -6.817976262117261044, 9.722976262117182245, 26.00000000000000711 ) ) ;
#67667=VERTEX_POINT ( 'NONE', #48522 ) ;
#67669=DIRECTION ( 'NONE',  ( 0.000000000000000000, 0.000000000000000000, -1.000000000000000000 ) ) ;
#67673=ORIENTED_EDGE ( 'NONE', *, *, #19604, .F. ) ;
#67681=VERTEX_POINT ( 'NONE', #42860 ) ;
#67683=AXIS2_PLACEMENT_3D ( 'NONE', #54665, #6221, #49373 ) ;
#67684=CARTESIAN_POINT ( 'NONE',  ( 6.836383711243005479, -4.149127210878733152, 26.00000000000000711 ) ) ;
#67687=DIRECTION ( 'NONE',  ( 0.7671651518153028704, 0.6414496315691539108, -2.309356642088818463E-17 ) ) ;
#67688=LINE ( 'NONE', #19248, #55478 ) ;
#67689=EDGE_CURVE ( 'NONE', #62156, #62419, #57078, .T. ) ;
#67690=CARTESIAN_POINT ( 'NONE',  ( -6.642976262117334940, -10.31452373788278898, 54.00000000000000711 ) ) ;
#67691=ORIENTED_EDGE ( 'NONE', *, *, #28188, .F. ) ;
#67705=CARTESIAN_POINT ( 'NONE',  ( 8.711985858128693749, -2.420780051175180692, 54.00000000000000711 ) ) ;
#67721=EDGE_CURVE ( 'NONE', #19218, #25597, #4694, .T. ) ;
#67742=DIRECTION ( 'NONE',  ( -0.000000000000000000, 3.673940397442059868E-16, -1.000000000000000000 ) ) ;
#67748=ORIENTED_EDGE ( 'NONE', *, *, #43942, .F. ) ;
#67751=CARTESIAN_POINT ( 'NONE',  ( -9.781776262117247711, 9.781776262117171328, 26.00000000000000711 ) ) ;
#67752=DIRECTION ( 'NONE',  ( -4.956352788505168198E-15, -1.000000000000000000, 0.000000000000000000 ) ) ;
#67765=CARTESIAN_POINT ( 'NONE',  ( -2.355476262117319308, -8.835729544836356197, 54.00000000000000711 ) ) ;
#67766=LINE ( 'NONE', #35948, #58484 ) ;
#67770=ORIENTED_EDGE ( 'NONE', *, *, #14065, .T. ) ;
#67771=CARTESIAN_POINT ( 'NONE',  ( -8.697938382363179954, -8.093267424590409931, 26.00000000000000000 ) ) ;
#67777=CARTESIAN_POINT ( 'NONE',  ( -8.697938382363135545, 8.079219948824830411, 54.00000000000000711 ) ) ;
#67786=EDGE_CURVE ( 'NONE', #20416, #43624, #67278, .T. ) ;
#67791=DIRECTION ( 'NONE',  ( 1.000000000000000000, 3.016910393003147986E-15, 0.000000000000000000 ) ) ;
#67793=CARTESIAN_POINT ( 'NONE',  ( -3.663616288757091333, -4.149127210878728711, 54.00000000000000711 ) ) ;
#67802=EDGE_CURVE ( 'NONE', #18238, #56714, #66159, .T. ) ;
#67817=ADVANCED_FACE ( 'NONE', ( #23378 ), #14155, .F. ) ;
#67838=ORIENTED_EDGE ( 'NONE', *, *, #20237, .T. ) ;
#67841=CARTESIAN_POINT ( 'NONE',  ( -3.663616288757090000, -6.364920264886882784, 26.00000000000000711 ) ) ;
#67850=DIRECTION ( 'NONE',  ( -0.000000000000000000, 3.673940397442059868E-16, -1.000000000000000000 ) ) ;
#67852=ORIENTED_EDGE ( 'NONE', *, *, #34646, .T. ) ;
#67854=ORIENTED_EDGE ( 'NONE', *, *, #28508, .F. ) ;
#67857=CARTESIAN_POINT ( 'NONE',  ( -8.697938382363135545, 2.406732575409538111, 26.00000000000000711 ) ) ;
#67863=ORIENTED_EDGE ( 'NONE', *, *, #30269, .T. ) ;
#67869=ORIENTED_EDGE ( 'NONE', *, *, #35385, .T. ) ;
#67872=LINE ( 'NONE', #19425, #66295 ) ;
#67881=EDGE_CURVE ( 'NONE', #51768, #65806, #29363, .T. ) ;
#67882=AXIS2_PLACEMENT_3D ( 'NONE', #22853, #44400, #65975 ) ;
#67889=CARTESIAN_POINT ( 'NONE',  ( -7.172176262117278434, -5.257023737882785319, 54.00000000000000711 ) ) ;
#67903=EDGE_CURVE ( 'NONE', #32604, #28065, #13807, .T. ) ;
#67904=LINE ( 'NONE', #2148, #30420 ) ;
#67910=CARTESIAN_POINT ( 'NONE',  ( 9.562023737882812569, -8.144523737882824577, 54.00000000000000711 ) ) ;
#67913=ORIENTED_EDGE ( 'NONE', *, *, #36667, .T. ) ;
#67915=VERTEX_POINT ( 'NONE', #67910 ) ;
#67923=VERTEX_POINT ( 'NONE', #1803 ) ;
#67935=DIRECTION ( 'NONE',  ( -0.000000000000000000, 3.673940397442059868E-16, -1.000000000000000000 ) ) ;
#67939=EDGE_LOOP ( 'NONE', ( #65557, #37309, #62378, #53084 ) ) ;
#67952=LINE ( 'NONE', #61572, #46010 ) ;
#67964=FACE_OUTER_BOUND ( 'NONE', #69284, .T. ) ;
#67972=ORIENTED_EDGE ( 'NONE', *, *, #59637, .T. ) ;
#67978=VECTOR ( 'NONE', #11606, 1000.000000000000114 ) ;
#67981=ORIENTED_EDGE ( 'NONE', *, *, #50109, .F. ) ;
#67987=EDGE_CURVE ( 'NONE', #26595, #35004, #31160, .T. ) ;
#68000=EDGE_LOOP ( 'NONE', ( #7867, #22020, #45678, #27540 ) ) ;
#68003=DIRECTION ( 'NONE',  ( 0.6414496315691367023, -0.7671651518153173033, -2.309356642089295169E-17 ) ) ;
#68024=DIRECTION ( 'NONE',  ( -0.000000000000000000, -0.000000000000000000, -1.000000000000000000 ) ) ;
#68036=VECTOR ( 'NONE', #4778, 1000.000000000000000 ) ;
#68040=DIRECTION ( 'NONE',  ( -1.836970198721029934E-16, 1.836970198721036590E-16, -1.000000000000000000 ) ) ;
#68044=DIRECTION ( 'NONE',  ( -1.836970198721029934E-16, 1.836970198721036590E-16, -1.000000000000000000 ) ) ;
#68046=CARTESIAN_POINT ( 'NONE',  ( -3.834182069070765309, 7.342976262117171693, 26.00000000000000711 ) ) ;
#68047=VECTOR ( 'NONE', #27516, 1000.000000000000114 ) ;
#68056=LINE ( 'NONE', #41174, #17272 ) ;
#68067=ORIENTED_EDGE ( 'NONE', *, *, #36331, .T. ) ;
#68070=DIRECTION ( 'NONE',  ( -0.000000000000000000, 3.673940397442059868E-16, -1.000000000000000000 ) ) ;
#68076=ORIENTED_EDGE ( 'NONE', *, *, #19413, .F. ) ;
#68079=DIRECTION ( 'NONE',  ( 1.000000000000000000, -1.185108578570163560E-14, 0.000000000000000000 ) ) ;
#68099=VECTOR ( 'NONE', #28267, 1000.000000000000000 ) ;
#68101=EDGE_LOOP ( 'NONE', ( #33307, #46279, #30632, #63079 ) ) ;
#68103=VECTOR ( 'NONE', #16412, 1000.000000000000000 ) ;
#68123=ORIENTED_EDGE ( 'NONE', *, *, #43503, .F. ) ;
#68125=CARTESIAN_POINT ( 'NONE',  ( -3.650476262117329007, -10.31452373788281385, 26.00000000000000000 ) ) ;
#68128=VECTOR ( 'NONE', #19861, 1000.000000000000000 ) ;
#68135=EDGE_LOOP ( 'NONE', ( #14162, #8751, #65179, #41146 ) ) ;
#68139=ORIENTED_EDGE ( 'NONE', *, *, #67689, .F. ) ;
#68141=DIRECTION ( 'NONE',  ( 3.016910393003147986E-15, -1.000000000000000000, 0.000000000000000000 ) ) ;
#68147=ORIENTED_EDGE ( 'NONE', *, *, #27213, .F. ) ;
#68150=CARTESIAN_POINT ( 'NONE',  ( -3.842976262117221875, 10.30047626211716860, 26.00000000000000711 ) ) ;
#68151=DIRECTION ( 'NONE',  ( -1.000000000000000000, 0.000000000000000000, 0.000000000000000000 ) ) ;
#68157=ORIENTED_EDGE ( 'NONE', *, *, #65064, .T. ) ;
#68158=CARTESIAN_POINT ( 'NONE',  ( -8.916576262117258622, 9.689726262117185129, 26.00000000000000711 ) ) ;
#68161=CARTESIAN_POINT ( 'NONE',  ( -7.342976262117259623, 4.947141984184421304, 54.00000000000000711 ) ) ;
#68169=EDGE_CURVE ( 'NONE', #3391, #24260, #22269, .T. ) ;
#68183=EDGE_CURVE ( 'NONE', #42852, #28114, #62831, .T. ) ;
#68184=ORIENTED_EDGE ( 'NONE', *, *, #50087, .F. ) ;
#68187=DIRECTION ( 'NONE',  ( -0.7671651518153065341, -0.6414496315691495809, -2.356647714346224881E-16 ) ) ;
#68188=EDGE_CURVE ( 'NONE', #48595, #68798, #49816, .T. ) ;
#68189=EDGE_LOOP ( 'NONE', ( #83, #57925, #68076, #43029, #37504, #10154, #23434, #39120 ) ) ;
#68202=DIRECTION ( 'NONE',  ( -1.836970198721029934E-16, 1.836970198721036590E-16, -1.000000000000000000 ) ) ;
#68204=VECTOR ( 'NONE', #32260, 1000.000000000000000 ) ;
#68206=DIRECTION ( 'NONE',  ( 5.626525616968433120E-15, 1.000000000000000000, 1.836970198721025990E-16 ) ) ;
#68208=FACE_OUTER_BOUND ( 'NONE', #3114, .T. ) ;
#68212=CARTESIAN_POINT ( 'NONE',  ( 9.562023737882812569, -8.144523737882824577, 54.00000000000000711 ) ) ;
#68234=VERTEX_POINT ( 'NONE', #60077 ) ;
#68245=VERTEX_POINT ( 'NONE', #27913 ) ;
#68250=FACE_OUTER_BOUND ( 'NONE', #32266, .T. ) ;
#68251=CYLINDRICAL_SURFACE ( 'NONE', #50513, 0.3499999999999996447 ) ;
#68266=CARTESIAN_POINT ( 'NONE',  ( -7.342976262117248965, -3.848229544836283100, 26.00000000000000711 ) ) ;
#68267=CARTESIAN_POINT ( 'NONE',  ( -1.620245201994301665, 8.227189898828640935, 54.00000000000000711 ) ) ;
#68278=EDGE_CURVE ( 'NONE', #58489, #1811, #60767, .T. ) ;
#68293=CYLINDRICAL_SURFACE ( 'NONE', #11476, 1.929199999999998916 ) ;
#68296=CARTESIAN_POINT ( 'NONE',  ( 3.664523737882778853, -10.50702373788280219, 26.00000000000000000 ) ) ;
#68299=EDGE_CURVE ( 'NONE', #16950, #2504, #48165, .T. ) ;
#68302=DIRECTION ( 'NONE',  ( -1.836970198721029934E-16, 1.836970198721036590E-16, -1.000000000000000000 ) ) ;
#68312=CARTESIAN_POINT ( 'NONE',  ( 9.703773737882814387, 8.916576262117184015, 54.00000000000000711 ) ) ;
#68314=CARTESIAN_POINT ( 'NONE',  ( -6.822336235477489019, -6.364920264886855250, 54.00000000000000711 ) ) ;
#68315=CARTESIAN_POINT ( 'NONE',  ( -10.49297626211725110, -3.664523737882711352, 54.00000000000000711 ) ) ;
#68321=DIRECTION ( 'NONE',  ( -3.596772705736696467E-15, -1.000000000000000000, 0.000000000000000000 ) ) ;
#68326=CARTESIAN_POINT ( 'NONE',  ( -6.642976262117260333, 10.30047626211718104, 54.00000000000000711 ) ) ;
#68330=FACE_OUTER_BOUND ( 'NONE', #36200, .T. ) ;
#68331=ORIENTED_EDGE ( 'NONE', *, *, #53384, .F. ) ;
#68333=ADVANCED_FACE ( 'NONE', ( #1718 ), #23285, .F. ) ;
#68335=VECTOR ( 'NONE', #5922, 1000.000000000000000 ) ;
#68338=LINE ( 'NONE', #40764, #64006 ) ;
#68342=CYLINDRICAL_SURFACE ( 'NONE', #19768, 0.1749999999999998224 ) ;
#68346=EDGE_CURVE ( 'NONE', #61284, #45166, #17655, .T. ) ;
#68353=CARTESIAN_POINT ( 'NONE',  ( -3.667976262117328190, -9.737023737882820384, 54.00000000000000711 ) ) ;
#68354=ADVANCED_FACE ( 'NONE', ( #44846 ), #66425, .F. ) ;
#68363=DIRECTION ( 'NONE',  ( -1.000000000000000000, 0.000000000000000000, 0.000000000000000000 ) ) ;
#68364=VERTEX_POINT ( 'NONE', #19032 ) ;
#68368=ORIENTED_EDGE ( 'NONE', *, *, #42323, .T. ) ;
#68370=DIRECTION ( 'NONE',  ( 0.000000000000000000, -1.000000000000000000, 0.000000000000000000 ) ) ;
#68372=ORIENTED_EDGE ( 'NONE', *, *, #43616, .F. ) ;
#68381=DIRECTION ( 'NONE',  ( -0.7071067811865446862, 0.7071067811865503483, 0.000000000000000000 ) ) ;
#68383=ORIENTED_EDGE ( 'NONE', *, *, #2181, .T. ) ;
#68394=LINE ( 'NONE', #47182, #58877 ) ;
#68396=AXIS2_PLACEMENT_3D ( 'NONE', #7698, #29259, #2058 ) ;
#68398=DIRECTION ( 'NONE',  ( 2.135044278125299371E-15, 1.000000000000000000, 0.000000000000000000 ) ) ;
#68403=LINE ( 'NONE', #4416, #7848 ) ;
#68407=CARTESIAN_POINT ( 'NONE',  ( 2.369523737882810455, 8.821682069070735821, 26.00000000000000711 ) ) ;
#68408=AXIS2_PLACEMENT_3D ( 'NONE', #44538, #18017, #61489 ) ;
#68419=ORIENTED_EDGE ( 'NONE', *, *, #53802, .T. ) ;
#68424=VERTEX_POINT ( 'NONE', #20430 ) ;
#68425=CYLINDRICAL_SURFACE ( 'NONE', #8458, 0.3499999999999996447 ) ;
#68428=EDGE_CURVE ( 'NONE', #8452, #43101, #26097, .T. ) ;
#68446=DIRECTION ( 'NONE',  ( 1.000000000000000000, -1.047444401652940007E-14, 1.836970198721010706E-16 ) ) ;
#68448=VECTOR ( 'NONE', #34090, 1000.000000000000000 ) ;
#68452=ORIENTED_EDGE ( 'NONE', *, *, #31777, .F. ) ;
#68455=CIRCLE ( 'NONE', #37977, 1.224999999999998757 ) ;
#68473=CARTESIAN_POINT ( 'NONE',  ( 6.665817930929283541, 7.342976262117200115, 26.00000000000000711 ) ) ;
#68476=EDGE_CURVE ( 'NONE', #47021, #7002, #46947, .T. ) ;
#68478=VECTOR ( 'NONE', #42241, 1000.000000000000000 ) ;
#68482=CARTESIAN_POINT ( 'NONE',  ( -10.30047626211724854, -3.664523737882715348, 54.00000000000000711 ) ) ;
#68489=AXIS2_PLACEMENT_3D ( 'NONE', #1950, #23513, #63366 ) ;
#68502=FACE_OUTER_BOUND ( 'NONE', #43639, .T. ) ;
#68519=ORIENTED_EDGE ( 'NONE', *, *, #60892, .F. ) ;
#68525=EDGE_CURVE ( 'NONE', #2503, #46841, #53324, .T. ) ;
#68527=VECTOR ( 'NONE', #67609, 1000.000000000000000 ) ;
#68529=CARTESIAN_POINT ( 'NONE',  ( -6.486996718459913325, -3.157023737882783454, 54.00000000000000711 ) ) ;
#68545=AXIS2_PLACEMENT_3D ( 'NONE', #34943, #55492, #17993 ) ;
#68553=ORIENTED_EDGE ( 'NONE', *, *, #15900, .T. ) ;
#68557=CARTESIAN_POINT ( 'NONE',  ( 7.532023737882783898, 3.834182069070696031, 54.00000000000000711 ) ) ;
#68560=LINE ( 'NONE', #46274, #62875 ) ;
#68569=EDGE_CURVE ( 'NONE', #69196, #56572, #44078, .T. ) ;
#68570=FACE_OUTER_BOUND ( 'NONE', #62647, .T. ) ;
#68576=VERTEX_POINT ( 'NONE', #65654 ) ;
#68577=CARTESIAN_POINT ( 'NONE',  ( -9.689726262117227762, 10.03972626211718300, 54.00000000000000711 ) ) ;
#68585=EDGE_LOOP ( 'NONE', ( #33624, #34663, #45843, #1086 ) ) ;
#68588=AXIS2_PLACEMENT_3D ( 'NONE', #20454, #47326, #69934 ) ;
#68593=CIRCLE ( 'NONE', #31313, 0.1749999999999989342 ) ;
#68609=FACE_OUTER_BOUND ( 'NONE', #23648, .T. ) ;
#68611=ORIENTED_EDGE ( 'NONE', *, *, #18123, .T. ) ;
#68614=DIRECTION ( 'NONE',  ( 0.000000000000000000, 1.000000000000000000, 0.000000000000000000 ) ) ;
#68616=EDGE_CURVE ( 'NONE', #18784, #10363, #16565, .T. ) ;
#68625=ORIENTED_EDGE ( 'NONE', *, *, #38423, .F. ) ;
#68627=FACE_OUTER_BOUND ( 'NONE', #2460, .T. ) ;
#68631=AXIS2_PLACEMENT_3D ( 'NONE', #50646, #12457, #7849 ) ;
#68632=ORIENTED_EDGE ( 'NONE', *, *, #32340, .T. ) ;
#68637=CIRCLE ( 'NONE', #20070, 1.224999999999999423 ) ;
#68643=CARTESIAN_POINT ( 'NONE',  ( 9.912023737882815766, -3.682023737882826886, 54.00000000000000711 ) ) ;
#68647=CARTESIAN_POINT ( 'NONE',  ( -6.835476262117260227, 10.30047626211718104, 54.00000000000000711 ) ) ;
#68648=ORIENTED_EDGE ( 'NONE', *, *, #67881, .F. ) ;
#68650=CARTESIAN_POINT ( 'NONE',  ( 6.665817930929288870, 7.342976262117195674, 54.00000000000000711 ) ) ;
#68652=VECTOR ( 'NONE', #61817, 1000.000000000000000 ) ;
#68669=CARTESIAN_POINT ( 'NONE',  ( 3.857023737882813386, 10.30047626211720768, 26.00000000000000711 ) ) ;
#68673=FACE_OUTER_BOUND ( 'NONE', #40831, .T. ) ;
#68674=EDGE_LOOP ( 'NONE', ( #54213, #7983, #60523, #39568 ) ) ;
#68675=DIRECTION ( 'NONE',  ( 0.7671651518152939886, -0.6414496315691645689, 2.309356642088622481E-17 ) ) ;
#68676=CARTESIAN_POINT ( 'NONE',  ( -4.031976262117261456, 3.142976262117183506, 54.00000000000000711 ) ) ;
#68683=ORIENTED_EDGE ( 'NONE', *, *, #48082, .T. ) ;
#68685=CARTESIAN_POINT ( 'NONE',  ( 5.257023737882819070, -5.257023737882825287, 54.00000000000000711 ) ) ;
#68686=CYLINDRICAL_SURFACE ( 'NONE', #54599, 0.1749999999999980738 ) ;
#68698=ORIENTED_EDGE ( 'NONE', *, *, #21646, .T. ) ;
#68715=DIRECTION ( 'NONE',  ( 0.000000000000000000, -0.000000000000000000, -1.000000000000000000 ) ) ;
#68719=ORIENTED_EDGE ( 'NONE', *, *, #29508, .T. ) ;
#68721=ORIENTED_EDGE ( 'NONE', *, *, #66313, .T. ) ;
#68727=ORIENTED_EDGE ( 'NONE', *, *, #64781, .F. ) ;
#68731=ORIENTED_EDGE ( 'NONE', *, *, #69873, .T. ) ;
#68732=CARTESIAN_POINT ( 'NONE',  ( 9.562023737882812569, -2.369523737882815784, 26.00000000000000711 ) ) ;
#68737=DIRECTION ( 'NONE',  ( -1.836970198721029934E-16, -1.836970198721010706E-16, 1.000000000000000000 ) ) ;
#68749=DIRECTION ( 'NONE',  ( -0.000000000000000000, 3.673940397442059868E-16, -1.000000000000000000 ) ) ;
#68753=ORIENTED_EDGE ( 'NONE', *, *, #25290, .T. ) ;
#68762=PLANE ( 'NONE',  #51163 ) ;
#68771=DIRECTION ( 'NONE',  ( -0.7071067811865474617, -0.7071067811865474617, -0.000000000000000000 ) ) ;
#68774=ORIENTED_EDGE ( 'NONE', *, *, #44317, .T. ) ;
#68777=CARTESIAN_POINT ( 'NONE',  ( 6.665817930929285318, 7.517976262117199937, 26.00000000000000711 ) ) ;
#68789=DIRECTION ( 'NONE',  ( -0.000000000000000000, 3.673940397442059868E-16, -1.000000000000000000 ) ) ;
#68793=ADVANCED_FACE ( 'NONE', ( #46509 ), #9035, .F. ) ;
#68798=VERTEX_POINT ( 'NONE', #41207 ) ;
#68817=DIRECTION ( 'NONE',  ( -0.000000000000000000, -0.000000000000000000, -1.000000000000000000 ) ) ;
#68819=FACE_OUTER_BOUND ( 'NONE', #58271, .T. ) ;
#68823=EDGE_CURVE ( 'NONE', #43477, #523, #25676, .T. ) ;
#68829=ADVANCED_FACE ( 'NONE', ( #3389 ), #57127, .T. ) ;
#68834=AXIS2_PLACEMENT_3D ( 'NONE', #4852, #53304, #25367 ) ;
#68840=DIRECTION ( 'NONE',  ( 0.000000000000000000, -3.673940397442059868E-16, 1.000000000000000000 ) ) ;
#68845=CARTESIAN_POINT ( 'NONE',  ( -9.897976262117291313, -6.657023737882756365, 54.00000000000000711 ) ) ;
#68852=CARTESIAN_POINT ( 'NONE',  ( 4.149127210878741145, 3.663616288756999406, 54.00000000000000711 ) ) ;
#68854=CIRCLE ( 'NONE', #33802, 0.5249999999999994671 ) ;
#68859=CARTESIAN_POINT ( 'NONE',  ( 8.930623737882843471, 8.566576262117187923, 54.00000000000000711 ) ) ;
#68863=DIRECTION ( 'NONE',  ( -4.956352788505180820E-15, -1.000000000000000000, 0.000000000000000000 ) ) ;
#68864=ORIENTED_EDGE ( 'NONE', *, *, #36056, .F. ) ;
#68870=ADVANCED_FACE ( 'NONE', ( #25307 ), #8852, .F. ) ;
#68874=EDGE_CURVE ( 'NONE', #39378, #58511, #61895, .T. ) ;
#68878=CARTESIAN_POINT ( 'NONE',  ( -10.30047626211728939, -6.849523737882745600, 26.00000000000000000 ) ) ;
#68882=EDGE_CURVE ( 'NONE', #59231, #54124, #3206, .T. ) ;
#68887=VECTOR ( 'NONE', #69910, 1000.000000000000000 ) ;
#68888=LINE ( 'NONE', #64285, #19550 ) ;
#68889=ORIENTED_EDGE ( 'NONE', *, *, #20759, .F. ) ;
#68891=AXIS2_PLACEMENT_3D ( 'NONE', #43092, #5625, #27194 ) ;
#68899=CARTESIAN_POINT ( 'NONE',  ( -5.242976262117299946, -7.186223737882804663, 54.00000000000000711 ) ) ;
#68904=DIRECTION ( 'NONE',  ( -1.047444401652940007E-14, -1.000000000000000000, -1.836970198721029934E-16 ) ) ;
#68912=CARTESIAN_POINT ( 'NONE',  ( 7.408280051175172076, -6.789561617636940660, 26.00000000000000000 ) ) ;
#68917=CARTESIAN_POINT ( 'NONE',  ( 10.50702373788281996, -6.849523737882814878, 26.00000000000000000 ) ) ;
#68925=CARTESIAN_POINT ( 'NONE',  ( 3.157023737882819425, -4.046023737882825877, 54.00000000000000711 ) ) ;
#68930=VERTEX_POINT ( 'NONE', #45618 ) ;
#68931=FACE_OUTER_BOUND ( 'NONE', #21416, .T. ) ;
#68940=VERTEX_POINT ( 'NONE', #19797 ) ;
#68941=ORIENTED_EDGE ( 'NONE', *, *, #23393, .T. ) ;
#68952=DIRECTION ( 'NONE',  ( -1.836970198721029934E-16, 1.836970198721036590E-16, -1.000000000000000000 ) ) ;
#68957=LINE ( 'NONE', #31490, #9499 ) ;
#68961=AXIS2_PLACEMENT_3D ( 'NONE', #62995, #18800, #35760 ) ;
#68962=AXIS2_PLACEMENT_3D ( 'NONE', #23121, #40065, #39721 ) ;
#68982=AXIS2_PLACEMENT_3D ( 'NONE', #11318, #32895, #5688 ) ;
#68983=CARTESIAN_POINT ( 'NONE',  ( 8.835729544836285143, 2.530476262117165920, 26.00000000000000711 ) ) ;
#68984=FACE_OUTER_BOUND ( 'NONE', #42061, .T. ) ;
#68995=FACE_OUTER_BOUND ( 'NONE', #64598, .T. ) ;
#68996=CARTESIAN_POINT ( 'NONE',  ( -3.834182069070817711, -7.357023737882814274, 26.00000000000000711 ) ) ;
#69009=ORIENTED_EDGE ( 'NONE', *, *, #64367, .T. ) ;
#69014=ADVANCED_FACE ( 'NONE', ( #14150 ), #68251, .F. ) ;
#69022=CYLINDRICAL_SURFACE ( 'NONE', #69762, 1.224999999999999423 ) ;
#69024=LINE ( 'NONE', #19354, #48037 ) ;
#69028=ORIENTED_EDGE ( 'NONE', *, *, #18459, .F. ) ;
#69030=CARTESIAN_POINT ( 'NONE',  ( 0.9555237378827827754, -9.929523737882790968, 54.00000000000000711 ) ) ;
#69036=EDGE_CURVE ( 'NONE', #330, #66569, #21901, .T. ) ;
#69037=DIRECTION ( 'NONE',  ( -1.079558018506126625E-14, -1.000000000000000000, 0.000000000000000000 ) ) ;
#69065=ORIENTED_EDGE ( 'NONE', *, *, #25074, .T. ) ;
#69074=CARTESIAN_POINT ( 'NONE',  ( 10.31452373788278187, 3.842976262117144159, 54.00000000000000711 ) ) ;
#69079=CARTESIAN_POINT ( 'NONE',  ( -7.342976262117259623, 5.538810540049946773, 54.00000000000000711 ) ) ;
#69082=CARTESIAN_POINT ( 'NONE',  ( -6.835476262117334834, -10.50702373788278798, 54.00000000000000711 ) ) ;
#69086=VECTOR ( 'NONE', #61476, 1000.000000000000000 ) ;
#69087=DIRECTION ( 'NONE',  ( 0.7071067811865486830, 0.7071067811865464625, 0.000000000000000000 ) ) ;
#69092=LINE ( 'NONE', #36209, #50623 ) ;
#69096=DIRECTION ( 'NONE',  ( 1.836970198721029934E-16, -1.836970198721036344E-16, 1.000000000000000000 ) ) ;
#69102=ORIENTED_EDGE ( 'NONE', *, *, #3400, .F. ) ;
#69106=VECTOR ( 'NONE', #32919, 1000.000000000000000 ) ;
#69108=LINE ( 'NONE', #41881, #22927 ) ;
#69112=EDGE_CURVE ( 'NONE', #7825, #50090, #32171, .T. ) ;
#69119=CARTESIAN_POINT ( 'NONE',  ( -6.858227778582867806, 2.989207322240119868, 54.00000000000000711 ) ) ;
#69125=VECTOR ( 'NONE', #61410, 1000.000000000000000 ) ;
#69127=ORIENTED_EDGE ( 'NONE', *, *, #64919, .F. ) ;
#69131=DIRECTION ( 'NONE',  ( 1.000000000000000000, -3.903627567395476653E-15, 0.000000000000000000 ) ) ;
#69148=CARTESIAN_POINT ( 'NONE',  ( -10.49297626211732215, -9.795823737882733084, 26.00000000000000000 ) ) ;
#69150=DIRECTION ( 'NONE',  ( 1.836970198721029934E-16, 1.836970198721010706E-16, -1.000000000000000000 ) ) ;
#69151=AXIS2_PLACEMENT_3D ( 'NONE', #50135, #23605, #23957 ) ;
#69159=EDGE_CURVE ( 'NONE', #29848, #64676, #19989, .T. ) ;
#69161=CARTESIAN_POINT ( 'NONE',  ( 8.930623737882848800, 9.689726262117154931, 54.00000000000000711 ) ) ;
#69165=CARTESIAN_POINT ( 'NONE',  ( 10.50702373788277910, 3.650476262117147375, 26.00000000000000711 ) ) ;
#69166=DIRECTION ( 'NONE',  ( 1.836970198721029934E-16, 1.836970198721010706E-16, -1.000000000000000000 ) ) ;
#69179=EDGE_CURVE ( 'NONE', #4835, #65138, #28583, .T. ) ;
#69185=DIRECTION ( 'NONE',  ( -0.7671651518152963201, -0.6414496315691619044, 0.000000000000000000 ) ) ;
#69196=VERTEX_POINT ( 'NONE', #22263 ) ;
#69198=ORIENTED_EDGE ( 'NONE', *, *, #62600, .F. ) ;
#69201=ORIENTED_EDGE ( 'NONE', *, *, #47286, .F. ) ;
#69203=VECTOR ( 'NONE', #50730, 1000.000000000000000 ) ;
#69206=ORIENTED_EDGE ( 'NONE', *, *, #29069, .F. ) ;
#69225=AXIS2_PLACEMENT_3D ( 'NONE', #20657, #35884, #42226 ) ;
#69233=VECTOR ( 'NONE', #47661, 1000.000000000000000 ) ;
#69234=DIRECTION ( 'NONE',  ( -1.000000000000000000, 0.000000000000000000, 0.000000000000000000 ) ) ;
#69238=ORIENTED_EDGE ( 'NONE', *, *, #43616, .T. ) ;
#69239=ORIENTED_EDGE ( 'NONE', *, *, #14556, .F. ) ;
#69240=AXIS2_PLACEMENT_3D ( 'NONE', #54103, #65060, #48795 ) ;
#69244=CARTESIAN_POINT ( 'NONE',  ( 10.31452373788281562, -6.657023737882815873, 26.00000000000000000 ) ) ;
#69249=CARTESIAN_POINT ( 'NONE',  ( 8.835729544836338434, -2.369523737882816672, 26.00000000000000711 ) ) ;
#69262=VECTOR ( 'NONE', #48657, 1000.000000000000000 ) ;
#69265=FACE_OUTER_BOUND ( 'NONE', #22702, .T. ) ;
#69269=EDGE_CURVE ( 'NONE', #59980, #62873, #7010, .T. ) ;
#69272=EDGE_CURVE ( 'NONE', #15959, #46021, #62943, .T. ) ;
#69280=CARTESIAN_POINT ( 'NONE',  ( -10.49297626211726175, 6.835476262117182955, 26.00000000000000711 ) ) ;
#69284=EDGE_LOOP ( 'NONE', ( #32439, #33901, #57031, #66300 ) ) ;
#69285=ORIENTED_EDGE ( 'NONE', *, *, #40878, .F. ) ;
#69288=ORIENTED_EDGE ( 'NONE', *, *, #4289, .F. ) ;
#69293=ORIENTED_EDGE ( 'NONE', *, *, #52385, .F. ) ;
#69308=VECTOR ( 'NONE', #25643, 1000.000000000000000 ) ;
#69309=AXIS2_PLACEMENT_3D ( 'NONE', #12187, #40094, #12869 ) ;
#69312=VERTEX_POINT ( 'NONE', #2067 ) ;
#69316=EDGE_CURVE ( 'NONE', #17091, #39038, #698, .T. ) ;
#69317=ADVANCED_FACE ( 'NONE', ( #66760 ), #13372, .F. ) ;
#69326=CARTESIAN_POINT ( 'NONE',  ( -9.390476262117196882, -0.9555237378827262651, 26.00000000000000711 ) ) ;
#69332=VECTOR ( 'NONE', #54246, 1000.000000000000000 ) ;
#69342=FACE_OUTER_BOUND ( 'NONE', #9720, .T. ) ;
#69344=ORIENTED_EDGE ( 'NONE', *, *, #38967, .F. ) ;
#69351=LINE ( 'NONE', #20563, #24509 ) ;
#69357=VECTOR ( 'NONE', #8920, 1000.000000000000000 ) ;
#69362=EDGE_CURVE ( 'NONE', #27929, #51881, #8399, .T. ) ;
#69370=VERTEX_POINT ( 'NONE', #35624 ) ;
#69376=DIRECTION ( 'NONE',  ( 2.478176394252584099E-15, 1.000000000000000000, 0.000000000000000000 ) ) ;
#69386=CARTESIAN_POINT ( 'NONE',  ( 9.703773737882812611, 10.03972626211715813, 26.00000000000000711 ) ) ;
#69391=AXIS2_PLACEMENT_3D ( 'NONE', #52841, #47851, #25958 ) ;
#69396=EDGE_CURVE ( 'NONE', #58380, #15894, #51197, .T. ) ;
#69401=EDGE_CURVE ( 'NONE', #56758, #3816, #13716, .T. ) ;
#69403=ORIENTED_EDGE ( 'NONE', *, *, #57575, .T. ) ;
#69407=ORIENTED_EDGE ( 'NONE', *, *, #64313, .F. ) ;
#69413=ORIENTED_EDGE ( 'NONE', *, *, #16537, .T. ) ;
#69426=VERTEX_POINT ( 'NONE', #34920 ) ;
#69427=VECTOR ( 'NONE', #55479, 1000.000000000000000 ) ;
#69432=CARTESIAN_POINT ( 'NONE',  ( 9.912023737882815766, -3.682023737882826886, 54.00000000000000711 ) ) ;
#69451=CARTESIAN_POINT ( 'NONE',  ( 10.50702373788281996, -6.849523737882823760, 54.00000000000000711 ) ) ;
#69452=DIRECTION ( 'NONE',  ( 1.000000000000000000, -6.508391731846281342E-15, -1.836970198721041767E-16 ) ) ;
#69461=CARTESIAN_POINT ( 'NONE',  ( 7.408280051175162306, 6.775514141871318508, 54.00000000000000711 ) ) ;
#69475=CARTESIAN_POINT ( 'NONE',  ( 10.05377373788281581, 9.689726262117151379, 54.00000000000000711 ) ) ;
#69479=ORIENTED_EDGE ( 'NONE', *, *, #35385, .F. ) ;
#69480=FACE_OUTER_BOUND ( 'NONE', #33038, .T. ) ;
#69487=ORIENTED_EDGE ( 'NONE', *, *, #24896, .T. ) ;
#69488=AXIS2_PLACEMENT_3D ( 'NONE', #37381, #9820, #68151 ) ;
#69493=DIRECTION ( 'NONE',  ( 0.000000000000000000, -3.673940397442059868E-16, 1.000000000000000000 ) ) ;
#69508=EDGE_CURVE ( 'NONE', #50527, #17133, #25747, .T. ) ;
#69509=DIRECTION ( 'NONE',  ( -0.000000000000000000, -0.000000000000000000, -1.000000000000000000 ) ) ;
#69518=AXIS2_PLACEMENT_3D ( 'NONE', #47779, #25527, #47089 ) ;
#69524=CYLINDRICAL_SURFACE ( 'NONE', #29725, 1.224999999999998757 ) ;
#69526=DIRECTION ( 'NONE',  ( 0.000000000000000000, 1.000000000000000000, 3.673940397442059868E-16 ) ) ;
#69533=VECTOR ( 'NONE', #10810, 1000.000000000000000 ) ;
#69535=EDGE_CURVE ( 'NONE', #41857, #26334, #4260, .T. ) ;
#69537=CARTESIAN_POINT ( 'NONE',  ( 6.832023737882815695, 9.722976262117192903, 54.00000000000000711 ) ) ;
#69539=CARTESIAN_POINT ( 'NONE',  ( -5.242976262117259978, 5.242976262117182706, 54.00000000000000711 ) ) ;
#69543=LINE ( 'NONE', #47277, #32243 ) ;
#69545=AXIS2_PLACEMENT_3D ( 'NONE', #64938, #37035, #21108 ) ;
#69551=AXIS2_PLACEMENT_3D ( 'NONE', #40548, #30650, #40195 ) ;
#69552=AXIS2_PLACEMENT_3D ( 'NONE', #33319, #22706, #44258 ) ;
#69554=DIRECTION ( 'NONE',  ( 1.836970198721029934E-16, 1.836970198721010706E-16, -1.000000000000000000 ) ) ;
#69566=EDGE_CURVE ( 'NONE', #15881, #12520, #59300, .T. ) ;
#69571=EDGE_LOOP ( 'NONE', ( #6183, #41183, #20990, #56591 ) ) ;
#69576=PLANE ( 'NONE',  #4538 ) ;
#69602=LINE ( 'NONE', #26121, #10967 ) ;
#69609=DIRECTION ( 'NONE',  ( -1.047444401652940007E-14, -1.000000000000000000, -1.836970198721029934E-16 ) ) ;
#69613=DIRECTION ( 'NONE',  ( -1.836970198721029934E-16, -1.836970198721010706E-16, 1.000000000000000000 ) ) ;
#69614=VECTOR ( 'NONE', #65518, 999.9999999999998863 ) ;
#69617=CARTESIAN_POINT ( 'NONE',  ( -8.227189898828699555, -1.634292677759815904, 54.00000000000000711 ) ) ;
#69624=CARTESIAN_POINT ( 'NONE',  ( -9.880476262117236175, 7.447976262117216528, 25.99999580000000421 ) ) ;
#69643=DIRECTION ( 'NONE',  ( -1.836970198721029934E-16, 1.836970198721036590E-16, -1.000000000000000000 ) ) ;
#69650=VERTEX_POINT ( 'NONE', #49728 ) ;
#69658=VECTOR ( 'NONE', #29394, 1000.000000000000000 ) ;
#69660=VERTEX_POINT ( 'NONE', #17895 ) ;
#69661=ORIENTED_EDGE ( 'NONE', *, *, #875, .T. ) ;
#69662=CARTESIAN_POINT ( 'NONE',  ( -5.779227145995327497, -6.358413763958949083, 54.00000000000000711 ) ) ;
#69668=DIRECTION ( 'NONE',  ( 1.836970198721029934E-16, 1.836970198721010706E-16, -1.000000000000000000 ) ) ;
#69676=ORIENTED_EDGE ( 'NONE', *, *, #40530, .F. ) ;
#69677=CARTESIAN_POINT ( 'NONE',  ( -4.947141984184539432, -7.357023737882807168, 54.00000000000000711 ) ) ;
#69679=EDGE_LOOP ( 'NONE', ( #49711, #44089, #18923, #14947 ) ) ;
#69682=EDGE_CURVE ( 'NONE', #50155, #29684, #50568, .T. ) ;
#69686=ORIENTED_EDGE ( 'NONE', *, *, #50818, .T. ) ;
#69697=DIRECTION ( 'NONE',  ( -0.000000000000000000, 3.673940397442059868E-16, -1.000000000000000000 ) ) ;
#69698=AXIS2_PLACEMENT_3D ( 'NONE', #62376, #35871, #62733 ) ;
#69715=AXIS2_PLACEMENT_3D ( 'NONE', #20315, #41880, #27022 ) ;
#69719=DIRECTION ( 'NONE',  ( -1.000000000000000000, 1.047444401652940007E-14, -1.836970198721010706E-16 ) ) ;
#69734=CARTESIAN_POINT ( 'NONE',  ( 10.31452373788277832, 3.842976262117149044, 26.00000000000000711 ) ) ;
#69744=ORIENTED_EDGE ( 'NONE', *, *, #10437, .T. ) ;
#69749=VECTOR ( 'NONE', #15709, 1000.000000000000000 ) ;
#69750=DIRECTION ( 'NONE',  ( -1.000000000000000000, 3.491481338843133355E-15, 1.836970198721036344E-16 ) ) ;
#69751=PLANE ( 'NONE',  #19637 ) ;
#69755=EDGE_LOOP ( 'NONE', ( #13713, #50501, #11637, #64435 ) ) ;
#69757=ORIENTED_EDGE ( 'NONE', *, *, #23521, .T. ) ;
#69761=DIRECTION ( 'NONE',  ( 1.836970198721029934E-16, 1.836970198721010706E-16, -1.000000000000000000 ) ) ;
#69762=AXIS2_PLACEMENT_3D ( 'NONE', #68685, #4344, #20230 ) ;
#69772=VECTOR ( 'NONE', #9831, 1000.000000000000000 ) ;
#69775=DIRECTION ( 'NONE',  ( -0.000000000000000000, 3.673940397442059868E-16, -1.000000000000000000 ) ) ;
#69792=CARTESIAN_POINT ( 'NONE',  ( -1.620245201994368722, -8.241237374594323484, 26.00000000000000711 ) ) ;
#69794=DIRECTION ( 'NONE',  ( -0.7071067811865398012, 0.7071067811865552333, 2.597868168706484541E-16 ) ) ;
#69798=DIRECTION ( 'NONE',  ( -0.000000000000000000, -1.000000000000000000, -0.000000000000000000 ) ) ;
#69830=ORIENTED_EDGE ( 'NONE', *, *, #34942, .T. ) ;
#69850=CARTESIAN_POINT ( 'NONE',  ( 3.724485858128677940, -7.408280051175165859, 54.00000000000000711 ) ) ;
#69855=CYLINDRICAL_SURFACE ( 'NONE', #48108, 0.3499999999999996447 ) ;
#69867=LINE ( 'NONE', #38060, #32025 ) ;
#69873=EDGE_CURVE ( 'NONE', #18995, #24515, #67534, .T. ) ;
#69882=LINE ( 'NONE', #15795, #63282 ) ;
#69887=CARTESIAN_POINT ( 'NONE',  ( -4.947141984184539432, -7.357023737882807168, 54.00000000000000711 ) ) ;
#69888=CARTESIAN_POINT ( 'NONE',  ( 9.795823737882798810, 9.781776262117176657, 26.00000000000000711 ) ) ;
#69895=CARTESIAN_POINT ( 'NONE',  ( -5.779227145995327497, -6.358413763958949083, 54.00000000000000711 ) ) ;
#69896=VERTEX_POINT ( 'NONE', #56420 ) ;
#69898=VECTOR ( 'NONE', #26300, 1000.000000000000000 ) ;
#69901=VECTOR ( 'NONE', #23694, 1000.000000000000000 ) ;
#69903=VERTEX_POINT ( 'NONE', #2675 ) ;
#69910=DIRECTION ( 'NONE',  ( 1.836970198721029934E-16, 1.836970198721010706E-16, -1.000000000000000000 ) ) ;
#69912=EDGE_CURVE ( 'NONE', #64822, #22889, #45809, .T. ) ;
#69916=VECTOR ( 'NONE', #57336, 1000.000000000000000 ) ;
#69928=DIRECTION ( 'NONE',  ( -1.000000000000000000, 0.000000000000000000, 0.000000000000000000 ) ) ;
#69929=ORIENTED_EDGE ( 'NONE', *, *, #47823, .T. ) ;
#69934=DIRECTION ( 'NONE',  ( -4.956352788505168198E-15, -1.000000000000000000, 0.000000000000000000 ) ) ;
#69957=ORIENTED_EDGE ( 'NONE', *, *, #41119, .F. ) ;
#69961=CARTESIAN_POINT ( 'NONE',  ( -3.663616288757055806, 4.135079735113128763, 26.00000000000000711 ) ) ;
#69965=CARTESIAN_POINT ( 'NONE',  ( -9.722976262117246193, -3.682023737882722081, 26.00000000000000000 ) ) ;
#69966=ADVANCED_FACE ( 'NONE', ( #47911 ), #52530, .F. ) ;
#69967=LINE ( 'NONE', #13511, #26972 ) ;
#69968=DIRECTION ( 'NONE',  ( 9.912705577010386883E-15, 1.000000000000000000, 0.000000000000000000 ) ) ;
#69974=CYLINDRICAL_SURFACE ( 'NONE', #68891, 0.1749999999999998224 ) ;
#69977=DIRECTION ( 'NONE',  ( 0.7071067811865475727, -0.7071067811865475727, -2.597868168706480104E-16 ) ) ;
ENDSEC;
END-ISO-10303-21;
